ISO-10303-21;
HEADER;
FILE_DESCRIPTION (('STEP AP214'),
    '1' );
FILE_NAME ('bolt.step',
    '2026-10-06T22:16:42',
    ( '' ),
    ( '' ),
    'SwSTEP 2.0',
    'SolidWorks 2025',
    '' );
FILE_SCHEMA (( 'AUTOMOTIVE_DESIGN' ));
ENDSEC;

DATA;
#1=CARTESIAN_POINT ( 'NONE',  ( -157.2955611005345986, -176.6084106276440195, 41.63779006702063867 ) ) ;
#2=ORIENTED_EDGE ( 'NONE', *, *, #5010, .T. ) ;
#4=CARTESIAN_POINT ( 'NONE',  ( -160.8964159109769696, -164.1584106276440593, 49.65701158161630957 ) ) ;
#8=VERTEX_POINT ( 'NONE', #17420 ) ;
#10=AXIS2_PLACEMENT_3D ( 'NONE', #19848, #7848, #14551 ) ;
#11=CARTESIAN_POINT ( 'NONE',  ( -141.4692556286852891, -192.9891397928654726, 49.65701158161630957 ) ) ;
#20=CARTESIAN_POINT ( 'NONE',  ( -136.4581486297550441, -116.9891397928655010, 49.65701158161631668 ) ) ;
#29=CARTESIAN_POINT ( 'NONE',  ( -154.3824083646099439, -187.5584106276440650, 58.62277379824867296 ) ) ;
#31=CARTESIAN_POINT ( 'NONE',  ( -154.3824083646099439, -178.5584106276440366, 58.62277379824867296 ) ) ;
#45=CARTESIAN_POINT ( 'NONE',  ( -161.4692556286852607, -176.3391397928654669, 52.90620854394536821 ) ) ;
#46=ADVANCED_FACE ( 'NONE', ( #7741 ), #6067, .T. ) ;
#54=CARTESIAN_POINT ( 'NONE',  ( -142.0420953463936087, -174.3938272943107393, 49.65701158161630957 ) ) ;
#58=LINE ( 'NONE', #15385, #4469 ) ;
#64=( BOUNDED_CURVE ( )  B_SPLINE_CURVE ( 2, ( #3303, #16737, #14756, #2855, #19725, #1317, #1648, #14970, #11562, #21497, #6273, #9598, #6734 ),
 .UNSPECIFIED., .F., .F. ) 
 B_SPLINE_CURVE_WITH_KNOTS ( ( 3, 2, 2, 2, 2, 2, 3 ),
 ( 0.1249999999999999584, 0.1285714285714285587, 0.1357142857142857040, 0.1428571428571428492, 0.1499999999999999944, 0.1571428571428571397, 0.1607142857142856984 ),
 .UNSPECIFIED. ) 
 CURVE ( )  GEOMETRIC_REPRESENTATION_ITEM ( )  RATIONAL_B_SPLINE_CURVE ( ( 0.9755282581475768211, 0.9755282581475765991, 1.000000000000000000, 0.9510565162951535312, 1.000000000000000000, 0.9510565162951535312, 1.000000000000000000, 0.9510565162951535312, 1.000000000000000000, 0.9510565162951535312, 1.000000000000000000, 0.9755282581475769321, 0.9755282581475768211 ) ) 
 REPRESENTATION_ITEM ( '' )  );
#72=EDGE_CURVE ( 'NONE', #8233, #846, #19303, .T. ) ;
#74=CARTESIAN_POINT ( 'NONE',  ( -161.4692556286852891, -169.7130981290893317, 46.40781461928724383 ) ) ;
#75=CARTESIAN_POINT ( 'NONE',  ( -143.3790856849358306, -174.3630981290893089, 55.53486410454105027 ) ) ;
#77=CARTESIAN_POINT ( 'NONE',  ( -157.6495955161842062, -167.0130981290893146, 41.15050349809590102 ) ) ;
#94=ADVANCED_FACE ( 'NONE', ( #19971 ), #8063, .F. ) ;
#102=CARTESIAN_POINT ( 'NONE',  ( -148.5561028927606344, -162.0584106276440366, 40.69124936498395328 ) ) ;
#103=CARTESIAN_POINT ( 'NONE',  ( -148.5561028927606344, -192.9938272943107336, 58.62277379824867296 ) ) ;
#111=CARTESIAN_POINT ( 'NONE',  ( -154.3824083646099439, -166.2938272943107165, 58.62277379824867296 ) ) ;
#112=CARTESIAN_POINT ( 'NONE',  ( -143.8425227516148084, -174.9584106276440707, 55.19815736654470584 ) ) ;
#115=CARTESIAN_POINT ( 'NONE',  ( -143.8425227516148084, -159.3584106276440480, 44.11586579668791330 ) ) ;
#131=FACE_OUTER_BOUND ( 'NONE', #2097, .T. ) ;
#132=CARTESIAN_POINT ( 'NONE',  ( -145.2889157411863437, -170.6130981290892805, 41.15050349809589392 ) ) ;
#136=DIRECTION ( 'NONE',  ( 0.000000000000000000, 0.000000000000000000, 1.000000000000000000 ) ) ;
#139=CARTESIAN_POINT ( 'NONE',  ( -159.0959885057557983, -190.8584106276440480, 55.19815736654470584 ) ) ;
#141=CARTESIAN_POINT ( 'NONE',  ( -154.3824083646099439, -173.7584106276440536, 40.69124936498395328 ) ) ;
#157=CARTESIAN_POINT ( 'NONE',  ( -141.4692556286852891, -180.9891397928654726, 49.65701158161630957 ) ) ;
#158=CARTESIAN_POINT ( 'NONE',  ( -154.5594255724347761, -182.1630981290893203, 40.14644641866476604 ) ) ;
#164=CARTESIAN_POINT ( 'NONE',  ( -143.8425227516148084, -174.0938272943107279, 44.11586579668791330 ) ) ;
#178=CARTESIAN_POINT ( 'NONE',  ( -157.6495955161842062, -169.1130981290892805, 58.16351966513671812 ) ) ;
#179=CARTESIAN_POINT ( 'NONE',  ( -143.8425227516148084, -156.6938272943107222, 55.19815736654470584 ) ) ;
#181=CARTESIAN_POINT ( 'NONE',  ( -143.3790856849358306, -165.3630981290893089, 55.53486410454105027 ) ) ;
#191=CARTESIAN_POINT ( 'NONE',  ( -151.4692556286852607, -155.3130981290892976, 39.65701158161629536 ) ) ;
#194=ADVANCED_FACE ( 'NONE', ( #9612 ), #13126, .F. ) ;
#197=CARTESIAN_POINT ( 'NONE',  ( -145.2889157411863437, -167.6130981290893089, 41.15050349809589392 ) ) ;
#202=CARTESIAN_POINT ( 'NONE',  ( -160.8964159109769696, -158.3084106276440650, 46.59394152635518793 ) ) ;
#203=CARTESIAN_POINT ( 'NONE',  ( -145.6429501568359797, -176.9438272943107506, 41.63779006702063867 ) ) ;
#205=CARTESIAN_POINT ( 'NONE',  ( -157.6495955161842062, -194.0130981290893146, 41.15050349809590102 ) ) ;
#208=CARTESIAN_POINT ( 'NONE',  ( -157.6495955161842062, -173.9391397928654328, 41.15050349809589392 ) ) ;
#211=CARTESIAN_POINT ( 'NONE',  ( -151.4692556286852607, -183.8130981290892692, 59.65701158161632378 ) ) ;
#215=CARTESIAN_POINT ( 'NONE',  ( -151.4692556286852891, -155.6438272943107393, 39.74470866294723947 ) ) ;
#216=CARTESIAN_POINT ( 'NONE',  ( -148.5561028927606344, -175.2584106276440536, 58.62277379824867296 ) ) ;
#218=CARTESIAN_POINT ( 'NONE',  ( -154.3824083646099439, -160.5584106276440366, 58.62277379824867296 ) ) ;
#231=AXIS2_PLACEMENT_3D ( 'NONE', #21325, #21217, #9973 ) ;
#239=CARTESIAN_POINT ( 'NONE',  ( -160.8964159109769696, -178.8938272943107393, 49.65701158161630957 ) ) ;
#242=ORIENTED_EDGE ( 'NONE', *, *, #18959, .F. ) ;
#243=CARTESIAN_POINT ( 'NONE',  ( -160.8964159109769696, -185.1584106276440309, 49.65701158161630957 ) ) ;
#246=CARTESIAN_POINT ( 'NONE',  ( -159.0959885057557983, -176.4584106276440707, 44.11586579668791330 ) ) ;
#249=DIRECTION ( 'NONE',  ( 1.000000000000000000, 0.000000000000000000, 4.622506457652817044E-16 ) ) ;
#265=CARTESIAN_POINT ( 'NONE',  ( -143.3790856849358306, -171.6891397928654897, 43.77915905869157598 ) ) ;
#273=CARTESIAN_POINT ( 'NONE',  ( -157.2955611005346270, -173.3438272943107279, 41.63779006702063867 ) ) ;
#277=CARTESIAN_POINT ( 'NONE',  ( -161.4692556286852891, -158.6391397928655067, 46.40781461928724383 ) ) ;
#294=CARTESIAN_POINT ( 'NONE',  ( -149.8854112254399809, -173.3899795514095388, 39.65701158161628825 ) ) ;
#296=CARTESIAN_POINT ( 'NONE',  ( -148.3790856849358306, -173.4630981290893033, 40.14644641866477315 ) ) ;
#308=CARTESIAN_POINT ( 'NONE',  ( -145.2889157411863437, -156.5130981290893146, 58.16351966513671812 ) ) ;
#317=CARTESIAN_POINT ( 'NONE',  ( -151.4692556286852891, -155.9084106276440593, 39.74470866294723947 ) ) ;
#318=CARTESIAN_POINT ( 'NONE',  ( -142.0420953463936087, -177.3938272943107393, 49.65701158161630957 ) ) ;
#319=CARTESIAN_POINT ( 'NONE',  ( -143.3790856849358306, -177.6891397928654612, 43.77915905869157598 ) ) ;
#320=CARTESIAN_POINT ( 'NONE',  ( -143.3790856849358306, -194.7630981290893146, 43.77915905869157598 ) ) ;
#329=CARTESIAN_POINT ( 'NONE',  ( -151.4692556286852891, -176.9084106276440309, 39.74470866294723947 ) ) ;
#336=EDGE_LOOP ( 'NONE', ( #11033, #17342, #3726, #11219 ) ) ;
#349=EDGE_CURVE ( 'NONE', #7574, #19197, #1660, .T. ) ;
#355=CARTESIAN_POINT ( 'NONE',  ( -145.6429501568359797, -179.9438272943107506, 41.63779006702063867 ) ) ;
#358=CARTESIAN_POINT ( 'NONE',  ( -157.2955611005346270, -184.7084106276440423, 57.67623309621198047 ) ) ;
#360=CARTESIAN_POINT ( 'NONE',  ( -160.8964159109769696, -176.1584106276440309, 49.65701158161630957 ) ) ;
#376=CARTESIAN_POINT ( 'NONE',  ( -141.4692556286852891, -179.9130981290893203, 46.40781461928724383 ) ) ;
#377=CARTESIAN_POINT ( 'NONE',  ( -161.4692556286853176, -167.4891397928654726, 49.65701158161630957 ) ) ;
#379=CARTESIAN_POINT ( 'NONE',  ( -153.0531000319306827, -193.8160212151857706, 59.65701158161632378 ) ) ;
#383=CARTESIAN_POINT ( 'NONE',  ( -145.6429501568359797, -176.9438272943107506, 41.63779006702063867 ) ) ;
#393=VERTEX_POINT ( 'NONE', #13983 ) ;
#401=CARTESIAN_POINT ( 'NONE',  ( -148.3790856849358306, -192.6630981290892919, 59.16757674456786020 ) ) ;
#405=CARTESIAN_POINT ( 'NONE',  ( -154.5594255724347761, -173.1630981290893203, 40.14644641866476604 ) ) ;
#415=DIRECTION ( 'NONE',  ( -0.000000000000000000, 1.000000000000000000, -0.000000000000000000 ) ) ;
#420=CARTESIAN_POINT ( 'NONE',  ( -145.2889157411863437, -172.4391397928654612, 58.16351966513671812 ) ) ;
#424=CARTESIAN_POINT ( 'NONE',  ( -159.0959885057557983, -158.4584106276440423, 44.11586579668791330 ) ) ;
#425=CARTESIAN_POINT ( 'NONE',  ( -160.8964159109769696, -184.8938272943107393, 49.65701158161630957 ) ) ;
#436=CIRCLE ( 'NONE', #15899, 10.00000000000000888 ) ;
#438=CARTESIAN_POINT ( 'NONE',  ( -160.8964159109769696, -170.0084106276440252, 52.72008163687743121 ) ) ;
#458=CARTESIAN_POINT ( 'NONE',  ( -159.0959885057557983, -185.1938272943107222, 44.11586579668791330 ) ) ;
#459=DIRECTION ( 'NONE',  ( 0.000000000000000000, 0.000000000000000000, 1.000000000000000000 ) ) ;
#461=CARTESIAN_POINT ( 'NONE',  ( -143.8425227516148084, -177.9584106276440707, 55.19815736654470584 ) ) ;
#479=CARTESIAN_POINT ( 'NONE',  ( -141.4692556286852891, -165.8391397928654669, 46.40781461928724383 ) ) ;
#480=FACE_OUTER_BOUND ( 'NONE', #13932, .T. ) ;
#482=CARTESIAN_POINT ( 'NONE',  ( -154.5594255724347761, -164.1630981290892919, 40.14644641866476604 ) ) ;
#484=CARTESIAN_POINT ( 'NONE',  ( -154.3824083646099439, -161.4938272943107336, 40.69124936498395328 ) ) ;
#491=CARTESIAN_POINT ( 'NONE',  ( -159.5594255724347761, -175.8630981290893089, 43.77915905869157598 ) ) ;
#496=DIRECTION ( 'NONE',  ( -0.000000000000000000, 1.000000000000000000, -0.000000000000000000 ) ) ;
#500=CARTESIAN_POINT ( 'NONE',  ( -151.4692556286852891, -181.7391397928654726, 59.65701158161631668 ) ) ;
#504=CARTESIAN_POINT ( 'NONE',  ( -145.6429501568359797, -155.9438272943106938, 41.63779006702063867 ) ) ;
#506=CARTESIAN_POINT ( 'NONE',  ( -161.4692556286852607, -157.4130981290893203, 52.90620854394536821 ) ) ;
#524=CARTESIAN_POINT ( 'NONE',  ( -149.8854112254399240, -165.7362167067690280, 59.65701158161632378 ) ) ;
#528=CARTESIAN_POINT ( 'NONE',  ( -143.8425227516148084, -183.0938272943107279, 44.11586579668791330 ) ) ;
#529=CARTESIAN_POINT ( 'NONE',  ( -141.4692556286852891, -177.9891397928654442, 49.65701158161630957 ) ) ;
#530=DIRECTION ( 'NONE',  ( -0.000000000000000000, 1.000000000000000000, -0.000000000000000000 ) ) ;
#536=CARTESIAN_POINT ( 'NONE',  ( -142.0420953463935803, -156.2438272943106767, 46.59394152635518793 ) ) ;
#537=CARTESIAN_POINT ( 'NONE',  ( -142.0420953463936087, -162.6584106276440593, 49.65701158161630957 ) ) ;
#544=ORIENTED_EDGE ( 'NONE', *, *, #21756, .T. ) ;
#545=CARTESIAN_POINT ( 'NONE',  ( -153.0531000319306543, -178.8160212151857138, 59.65701158161632378 ) ) ;
#546=ORIENTED_EDGE ( 'NONE', *, *, #10598, .T. ) ;
#558=CARTESIAN_POINT ( 'NONE',  ( -159.0959885057557983, -176.1938272943107506, 44.11586579668791330 ) ) ;
#562=CARTESIAN_POINT ( 'NONE',  ( -160.8964159109769696, -176.3084106276440082, 46.59394152635518793 ) ) ;
#573=ORIENTED_EDGE ( 'NONE', *, *, #1822, .T. ) ;
#582=CARTESIAN_POINT ( 'NONE',  ( -141.4692556286852891, -168.9891397928654726, 49.65701158161630957 ) ) ;
#584=CARTESIAN_POINT ( 'NONE',  ( -145.2889157411863437, -158.6130981290893089, 41.15050349809589392 ) ) ;
#592=CARTESIAN_POINT ( 'NONE',  ( -151.4692556286852891, -167.6438272943107108, 39.74470866294723947 ) ) ;
#595=FACE_OUTER_BOUND ( 'NONE', #8168, .T. ) ;
#608=ADVANCED_FACE ( 'NONE', ( #12767 ), #11547, .T. ) ;
#611=CARTESIAN_POINT ( 'NONE',  ( -145.2889157411863437, -194.6130981290892805, 41.15050349809589392 ) ) ;
#615=CARTESIAN_POINT ( 'NONE',  ( -157.6495955161842062, -164.0130981290892862, 41.15050349809590102 ) ) ;
#622=CARTESIAN_POINT ( 'NONE',  ( -145.6429501568359797, -192.8438272943107563, 57.67623309621198047 ) ) ;
#635=CARTESIAN_POINT ( 'NONE',  ( -145.2889157411863437, -171.5391397928654555, 41.15050349809589392 ) ) ;
#641=CARTESIAN_POINT ( 'NONE',  ( -159.0959885057557983, -179.1938272943107506, 44.11586579668791330 ) ) ;
#643=CARTESIAN_POINT ( 'NONE',  ( -141.4692556286852891, -186.2130981290892748, 52.90620854394536821 ) ) ;
#650=CARTESIAN_POINT ( 'NONE',  ( -145.6429501568359797, -156.8438272943107563, 57.67623309621198047 ) ) ;
#651=CARTESIAN_POINT ( 'NONE',  ( -157.2955611005345986, -169.7084106276440139, 57.67623309621197336 ) ) ;
#652=CARTESIAN_POINT ( 'NONE',  ( -153.0531000319307111, -163.8160212151857706, 59.65701158161632378 ) ) ;
#653=FACE_OUTER_BOUND ( 'NONE', #17209, .T. ) ;
#656=ORIENTED_EDGE ( 'NONE', *, *, #19082, .T. ) ;
#661=EDGE_CURVE ( 'NONE', #393, #1664, #4822, .T. ) ;
#666=CARTESIAN_POINT ( 'NONE',  ( -151.4692556286852891, -196.9891397928655010, 49.65701158161630957 ) ) ;
#667=CARTESIAN_POINT ( 'NONE',  ( -159.5594255724347761, -157.8630981290893089, 43.77915905869157598 ) ) ;
#669=CARTESIAN_POINT ( 'NONE',  ( -159.5594255724347761, -172.2630981290892862, 55.53486410454104316 ) ) ;
#673=CARTESIAN_POINT ( 'NONE',  ( -143.8425227516148084, -180.6938272943107506, 55.19815736654470584 ) ) ;
#674=CARTESIAN_POINT ( 'NONE',  ( -142.0420953463935803, -189.8084106276440366, 52.72008163687743831 ) ) ;
#675=EDGE_LOOP ( 'NONE', ( #12068, #12531, #7663, #2302 ) ) ;
#694=CARTESIAN_POINT ( 'NONE',  ( -157.6495955161842062, -167.0391397928654271, 58.16351966513671812 ) ) ;
#701=CARTESIAN_POINT ( 'NONE',  ( -142.0420953463936087, -162.3938272943107393, 49.65701158161630957 ) ) ;
#705=CARTESIAN_POINT ( 'NONE',  ( -142.0420953463935803, -192.8084106276440650, 52.72008163687743831 ) ) ;
#714=ORIENTED_EDGE ( 'NONE', *, *, #4516, .T. ) ;
#726=CARTESIAN_POINT ( 'NONE',  ( -151.4692556286852891, -161.3130981290892692, 39.14238933923362396 ) ) ;
#732=CARTESIAN_POINT ( 'NONE',  ( -145.6429501568359797, -189.8438272943106995, 57.67623309621198047 ) ) ;
#747=CARTESIAN_POINT ( 'NONE',  ( -145.6429501568359797, -174.8438272943107279, 57.67623309621197336 ) ) ;
#749=CARTESIAN_POINT ( 'NONE',  ( -151.4692556286852891, -188.3130981290892407, 39.14238933923362396 ) ) ;
#757=CARTESIAN_POINT ( 'NONE',  ( -160.8964159109769696, -164.0084106276440536, 52.72008163687743121 ) ) ;
#759=CARTESIAN_POINT ( 'NONE',  ( -151.4692556286852891, -196.9891397928655010, 59.65701158161632378 ) ) ;
#764=EDGE_LOOP ( 'NONE', ( #17589, #5670, #19623, #11053, #11158, #714, #21133, #1352, #4663, #16860, #12738, #15157, #16180, #21181, #544, #656, #18743, #2229, #14338, #3756, #14681, #12360, #12066, #4072, #7203, #7344, #13067, #15491, #10510, #14069, #9237 ) ) ;
#767=( BOUNDED_SURFACE ( )  B_SPLINE_SURFACE ( 1, 2, ( 
 ( #3931, #20794, #12409, #11076, #941, #7787, #10878, #14491, #2382, #21233, #6112, #10766, #14383, #7686, #12735, #9329, #10662, #622, #19458, #17364, #9007, #17791, #17687, #19140, #2485, #2699, #9227, #9444, #2270, #15718, #7357, #15925, #837, #14060, #5686, #9120, #4039, #732, #15818, #7460, #7571, #14271, #21016, #4248, #5898, #19350, #10974, #2589, #21673, #6450, #6568, #8331, #9550, #16253, #3257, #13288, #2812, #11513, #20023, #15040, #16574, #4909, #18013, #14597, #18242, #1162, #4570, #4455, #2924, #17899, #3144, #21337, #1598, #13172, #9987, #16690, #9874, #12955, #9769, #21781, #11186, #19904, #8005, #12842, #19560, #3032, #18353, #14924, #14712, #4792, #7895, #6224, #21448, #16466, #19678, #6338, #9659, #16359, #1493, #1270, #13064, #19791, #4683, #14815, #11398, #1380, #21560, #18122, #8109, #8223, #2035, #8767, #17225, #5440, #1821, #15153, #11732, #12056, #3585, #15482, #18892, #20447, #15380, #383, #20129, #13395, #7112, #8555, #13604, #10527, #20557, #12160, #3799, #10313, #15581, #10206, #15267, #18787, #11846, #5339, #54, #18575, #164, #2141, #13817, #8874, #3482, #273, #6687, #17015, #5236, #1922, #6796, #3368, #16800, #20341, #16909, #5023, #17123, #3690, #11953, #18465, #10093, #18683, #10418, #1713, #8658, #6897, #8448, #7007, #13503, #20235, #5128, #13711, #914, #15896, #4325, #12602, #19324, #2245, #20987, #15685, #17441, #7435, #2458, #592, #7332, #14032, #19431, #9089, #20767, #14357, #12491, #20662, #7221, #14138, #9198, #2352, #12381, #7660, #2669, #8979, #5981, #5658, #4223, #19116, #12707, #20875, #9303, #21098, #5763, #11050, #3908, #13922, #19006, #17765, #808, #15792, #4116, #10952, #701, #19218, #7545, #17660, #4011, #9413, #484, #2566, #5543, #10852, #12270, #10739, #17548, #17338, #4762, #19763, #1465, #17873, #16121, #6196, #4543, #19652, #3227, #21311, #19875, #14461, #1027, #1354, #6087, #8197, #14898, #13146, #3117, #9743, #9848, #11598, #12815, #19534, #6537, #16549, #4428, #14792, #21646, #18328, #11481, #13257, #12927, #2784, #21534 ),
 ( #16440, #19994, #4879, #18212, #16224, #13039, #7764, #21203, #8085, #11265, #11160, #9527, #6312, #1135, #7869, #17984, #6424, #14569, #2898, #9633, #4660, #16332, #1242, #7976, #14683, #21423, #11375, #18096, #3005, #1797, #11926, #16775, #139, #18655, #15010, #10067, #16988, #5316, #12029, #20529, #3559, #7086, #13368, #11704, #17094, #3456, #5102, #20313, #10283, #18763, #13789, #16664, #3664, #10394, #29, #1575, #18440, #3339, #2008, #6982, #5415, #11818, #12133, #8416, #18866, #9961, #1686, #8741, #13685, #15458, #243, #8303, #20105, #358, #21751, #6660, #20419, #8631, #15125, #8528, #4994, #15241, #6767, #13476, #20208, #18549, #6869, #13577, #10179, #16880, #5212, #1895, #15349, #12464, #14332, #7193, #5517, #10927, #19090, #20741, #14112, #4092, #20961, #21073, #10502, #12575, #5846, #15659, #2114, #18978, #3881, #17634, #7520, #5955, #12354, #3773, #2222, #8851, #461, #17310, #2542, #14221, #9279, #15872, #13897, #20636, #15980, #10606, #8953, #562, #7307, #14007, #17418, #3990, #2324, #10715, #9062, #7413, #20850, #19195, #10824, #17524, #14768, #2762, #8170, #1111, #6511, #9502, #1327, #17740, #19404, #4629, #9387, #4737, #11456, #16417, #6396, #13016, #13124, #14875, #16092, #1002, #9825, #19846, #7739, #18071, #18185, #21620, #8060, #3092, #16199, #21174, #2978, #14440, #11136, #11027, #7846, #2645, #9716, #6065, #4301, #19736, #16523, #1441, #21511, #19512, #16308, #12792, #4404, #11348, #14548, #17851, #21291, #9610, #6169, #12903, #19625, #4519, #11241, #17961, #2866, #1219, #7952, #14657, #21397, #6285, #1769, #4969, #8604, #13345, #4, #18523, #6632, #13453, #3432, #11573, #14982, #16855, #20289, #5183, #8281, #18302, #15216, #20187, #11902, #15325, #8503, #10154, #18631, #19969, #4853, #3535, #16749, #15100, #218, #10260, #1874, #16962, #5079, #20395, #18418, #10045, #115, #20082, #6846, #21727, #11681, #1658, #6954, #13661, #13231, #8391, #13554, #3204, #9935, #16640, #1550, #11793, #6745, #3316, #18032, #1177, #13187, #21575, #8127, #9675, #1073, #6586, #2938 ) ),
 .UNSPECIFIED., .F., .F., .F. ) 
 B_SPLINE_SURFACE_WITH_KNOTS ( ( 2, 2 ),
 ( 3, 2, 2, 2, 2, 2, 2, 2, 2, 2, 2, 2, 2, 2, 2, 2, 2, 2, 2, 2, 2, 2, 2, 2, 2, 2, 2, 2, 2, 2, 2, 2, 2, 2, 2, 2, 2, 2, 2, 2, 2, 2, 2, 2, 2, 2, 2, 2, 2, 2, 2, 2, 2, 2, 2, 2, 2, 2, 2, 2, 2, 2, 2, 2, 2, 2, 2, 2, 2, 2, 2, 2, 2, 2, 2, 2, 2, 2, 2, 2, 2, 2, 2, 2, 2, 2, 2, 2, 2, 2, 2, 2, 2, 2, 2, 2, 2, 2, 2, 2, 2, 2, 2, 2, 2, 2, 2, 2, 2, 2, 2, 2, 2, 2, 2, 2, 2, 2, 2, 2, 2, 2, 2, 2, 2, 2, 2, 2, 2, 2, 2, 2, 2, 2, 3 ),
 ( 0.000000000000000000, 1.000000000000000000 ),
 ( 0.000000000000000000, 0.007142857142857142634, 0.01428571428571428527, 0.02142857142857142877, 0.02857142857142857054, 0.03571428571428571230, 0.04285714285714285754, 0.05000000000000000278, 0.05714285714285714107, 0.06428571428571427937, 0.07142857142857142461, 0.07857142857142856984, 0.08571428571428571508, 0.09285714285714286031, 0.1000000000000000056, 0.1071428571428571369, 0.1142857142857142821, 0.1214285714285714274, 0.1285714285714285587, 0.1357142857142857040, 0.1428571428571428492, 0.1499999999999999944, 0.1571428571428571397, 0.1642857142857142849, 0.1714285714285714302, 0.1785714285714285754, 0.1857142857142857206, 0.1928571428571428659, 0.2000000000000000111, 0.2071428571428571563, 0.2142857142857142738, 0.2214285714285714191, 0.2285714285714285643, 0.2357142857142857095, 0.2428571428571428548, 0.2500000000000000000, 0.2571428571428571175, 0.2642857142857142905, 0.2714285714285714080, 0.2785714285714285809, 0.2857142857142856984, 0.2928571428571428714, 0.2999999999999999889, 0.3071428571428571619, 0.3142857142857142794, 0.3214285714285714524, 0.3285714285714285698, 0.3357142857142856873, 0.3428571428571428603, 0.3499999999999999778, 0.3571428571428571508, 0.3642857142857142683, 0.3714285714285714413, 0.3785714285714285587, 0.3857142857142857317, 0.3928571428571428492, 0.4000000000000000222, 0.4071428571428571397, 0.4142857142857143127, 0.4214285714285714302, 0.4285714285714285476, 0.4357142857142857206, 0.4428571428571428381, 0.4500000000000000111, 0.4571428571428571286, 0.4642857142857143016, 0.4714285714285714191, 0.4785714285714285920, 0.4857142857142857095, 0.4928571428571428825, 0.5000000000000000000, 0.5071428571428571175, 0.5142857142857142350, 0.5214285714285714635, 0.5285714285714285809, 0.5357142857142856984, 0.5428571428571428159, 0.5500000000000000444, 0.5571428571428571619, 0.5642857142857142794, 0.5714285714285713969, 0.5785714285714286254, 0.5857142857142857428, 0.5928571428571428603, 0.5999999999999999778, 0.6071428571428570953, 0.6142857142857143238, 0.6214285714285714413, 0.6285714285714285587, 0.6357142857142856762, 0.6428571428571429047, 0.6500000000000000222, 0.6571428571428571397, 0.6642857142857142572, 0.6714285714285713746, 0.6785714285714286031, 0.6857142857142857206, 0.6928571428571428381, 0.6999999999999999556, 0.7071428571428571841, 0.7142857142857143016, 0.7214285714285714191, 0.7285714285714285365, 0.7357142857142857650, 0.7428571428571428825, 0.7500000000000000000, 0.7571428571428571175, 0.7642857142857142350, 0.7714285714285714635, 0.7785714285714285809, 0.7857142857142856984, 0.7928571428571428159, 0.8000000000000000444, 0.8071428571428571619, 0.8142857142857142794, 0.8214285714285713969, 0.8285714285714286254, 0.8357142857142857428, 0.8428571428571428603, 0.8499999999999999778, 0.8571428571428570953, 0.8642857142857143238, 0.8714285714285714413, 0.8785714285714285587, 0.8857142857142856762, 0.8928571428571429047, 0.9000000000000000222, 0.9071428571428571397, 0.9142857142857142572, 0.9214285714285713746, 0.9285714285714286031, 0.9357142857142857206, 0.9428571428571428381, 0.9499999999999999556, 0.9523897249335834259 ),
 .UNSPECIFIED. ) 
 GEOMETRIC_REPRESENTATION_ITEM ( )  RATIONAL_B_SPLINE_SURFACE ( (
 ( 1.000000000000000000, 0.9510565162951535312, 1.000000000000000000, 0.9510565162951535312, 1.000000000000000000, 0.9510565162951535312, 1.000000000000000000, 0.9510565162951535312, 1.000000000000000000, 0.9510565162951535312, 1.000000000000000000, 0.9510565162951535312, 1.000000000000000000, 0.9510565162951535312, 1.000000000000000000, 0.9510565162951535312, 1.000000000000000000, 0.9510565162951535312, 1.000000000000000000, 0.9510565162951535312, 1.000000000000000000, 0.9510565162951535312, 1.000000000000000000, 0.9510565162951535312, 1.000000000000000000, 0.9510565162951535312, 1.000000000000000000, 0.9510565162951535312, 1.000000000000000000, 0.9510565162951535312, 1.000000000000000000, 0.9510565162951535312, 1.000000000000000000, 0.9510565162951535312, 1.000000000000000000, 0.9510565162951535312, 1.000000000000000000, 0.9510565162951535312, 1.000000000000000000, 0.9510565162951535312, 1.000000000000000000, 0.9510565162951535312, 1.000000000000000000, 0.9510565162951535312, 1.000000000000000000, 0.9510565162951535312, 1.000000000000000000, 0.9510565162951535312, 1.000000000000000000, 0.9510565162951535312, 1.000000000000000000, 0.9510565162951535312, 1.000000000000000000, 0.9510565162951535312, 1.000000000000000000, 0.9510565162951535312, 1.000000000000000000, 0.9510565162951535312, 1.000000000000000000, 0.9510565162951535312, 1.000000000000000000, 0.9510565162951535312, 1.000000000000000000, 0.9510565162951535312, 1.000000000000000000, 0.9510565162951535312, 1.000000000000000000, 0.9510565162951535312, 1.000000000000000000, 0.9510565162951535312, 1.000000000000000000, 0.9510565162951535312, 1.000000000000000000, 0.9510565162951535312, 1.000000000000000000, 0.9510565162951535312, 1.000000000000000000, 0.9510565162951535312, 1.000000000000000000, 0.9510565162951535312, 1.000000000000000000, 0.9510565162951535312, 1.000000000000000000, 0.9510565162951535312, 1.000000000000000000, 0.9510565162951535312, 1.000000000000000000, 0.9510565162951535312, 1.000000000000000000, 0.9510565162951535312, 1.000000000000000000, 0.9510565162951535312, 1.000000000000000000, 0.9510565162951535312, 1.000000000000000000, 0.9510565162951535312, 1.000000000000000000, 0.9510565162951535312, 1.000000000000000000, 0.9510565162951535312, 1.000000000000000000, 0.9510565162951535312, 1.000000000000000000, 0.9510565162951535312, 1.000000000000000000, 0.9510565162951535312, 1.000000000000000000, 0.9510565162951535312, 1.000000000000000000, 0.9510565162951535312, 1.000000000000000000, 0.9510565162951535312, 1.000000000000000000, 0.9510565162951535312, 1.000000000000000000, 0.9510565162951535312, 1.000000000000000000, 0.9510565162951535312, 1.000000000000000000, 0.9510565162951535312, 1.000000000000000000, 0.9510565162951535312, 1.000000000000000000, 0.9510565162951535312, 1.000000000000000000, 0.9510565162951535312, 1.000000000000000000, 0.9510565162951535312, 1.000000000000000000, 0.9510565162951535312, 1.000000000000000000, 0.9510565162951535312, 1.000000000000000000, 0.9510565162951535312, 1.000000000000000000, 0.9510565162951535312, 1.000000000000000000, 0.9510565162951535312, 1.000000000000000000, 0.9510565162951535312, 1.000000000000000000, 0.9510565162951535312, 1.000000000000000000, 0.9510565162951535312, 1.000000000000000000, 0.9510565162951535312, 1.000000000000000000, 0.9510565162951535312, 1.000000000000000000, 0.9510565162951535312, 1.000000000000000000, 0.9510565162951535312, 1.000000000000000000, 0.9510565162951535312, 1.000000000000000000, 0.9510565162951535312, 1.000000000000000000, 0.9510565162951535312, 1.000000000000000000, 0.9510565162951535312, 1.000000000000000000, 0.9510565162951535312, 1.000000000000000000, 0.9510565162951535312, 1.000000000000000000, 0.9510565162951535312, 1.000000000000000000, 0.9510565162951535312, 1.000000000000000000, 0.9510565162951535312, 1.000000000000000000, 0.9510565162951535312, 1.000000000000000000, 0.9510565162951535312, 1.000000000000000000, 0.9510565162951535312, 1.000000000000000000, 0.9510565162951535312, 1.000000000000000000, 0.9510565162951535312, 1.000000000000000000, 0.9510565162951535312, 1.000000000000000000, 0.9510565162951535312, 1.000000000000000000, 0.9510565162951535312, 1.000000000000000000, 0.9510565162951535312, 1.000000000000000000, 0.9510565162951535312, 1.000000000000000000, 0.9510565162951535312, 1.000000000000000000, 0.9510565162951535312, 1.000000000000000000, 0.9510565162951535312, 1.000000000000000000, 0.9510565162951535312, 1.000000000000000000, 0.9510565162951535312, 1.000000000000000000, 0.9510565162951535312, 1.000000000000000000, 0.9510565162951535312, 1.000000000000000000, 0.9510565162951535312, 1.000000000000000000, 0.9510565162951535312, 1.000000000000000000, 0.9510565162951535312, 1.000000000000000000, 0.9510565162951535312, 1.000000000000000000, 0.9510565162951535312, 1.000000000000000000, 0.9510565162951535312, 1.000000000000000000, 0.9510565162951535312, 1.000000000000000000, 0.9510565162951535312, 1.000000000000000000, 0.9510565162951535312, 1.000000000000000000, 0.9510565162951535312, 1.000000000000000000, 0.9510565162951535312, 1.000000000000000000, 0.9510565162951535312, 1.000000000000000000, 0.9510565162951535312, 1.000000000000000000, 0.9510565162951535312, 1.000000000000000000, 0.9510565162951535312, 1.000000000000000000, 0.9510565162951535312, 1.000000000000000000, 0.9510565162951535312, 1.000000000000000000, 0.9510565162951535312, 1.000000000000000000, 0.9510565162951535312, 1.000000000000000000, 0.9510565162951535312, 1.000000000000000000, 0.9510565162951535312, 1.000000000000000000, 0.9510565162951535312, 1.000000000000000000, 0.9510565162951535312, 1.000000000000000000, 0.9510565162951535312, 1.000000000000000000, 0.9510565162951535312, 1.000000000000000000, 0.9510565162951535312, 1.000000000000000000, 0.9510565162951535312, 1.000000000000000000, 0.9510565162951535312, 1.000000000000000000, 0.9510565162951535312, 1.000000000000000000, 0.9510565162951535312, 1.000000000000000000, 0.9510565162951535312, 1.000000000000000000, 0.9836253951315730992, 0.9782074146920101132),
 ( 1.000000000000000000, 0.9510565162951535312, 1.000000000000000000, 0.9510565162951535312, 1.000000000000000000, 0.9510565162951535312, 1.000000000000000000, 0.9510565162951535312, 1.000000000000000000, 0.9510565162951535312, 1.000000000000000000, 0.9510565162951535312, 1.000000000000000000, 0.9510565162951535312, 1.000000000000000000, 0.9510565162951535312, 1.000000000000000000, 0.9510565162951535312, 1.000000000000000000, 0.9510565162951535312, 1.000000000000000000, 0.9510565162951535312, 1.000000000000000000, 0.9510565162951535312, 1.000000000000000000, 0.9510565162951535312, 1.000000000000000000, 0.9510565162951535312, 1.000000000000000000, 0.9510565162951535312, 1.000000000000000000, 0.9510565162951535312, 1.000000000000000000, 0.9510565162951535312, 1.000000000000000000, 0.9510565162951535312, 1.000000000000000000, 0.9510565162951535312, 1.000000000000000000, 0.9510565162951535312, 1.000000000000000000, 0.9510565162951535312, 1.000000000000000000, 0.9510565162951535312, 1.000000000000000000, 0.9510565162951535312, 1.000000000000000000, 0.9510565162951535312, 1.000000000000000000, 0.9510565162951535312, 1.000000000000000000, 0.9510565162951535312, 1.000000000000000000, 0.9510565162951535312, 1.000000000000000000, 0.9510565162951535312, 1.000000000000000000, 0.9510565162951535312, 1.000000000000000000, 0.9510565162951535312, 1.000000000000000000, 0.9510565162951535312, 1.000000000000000000, 0.9510565162951535312, 1.000000000000000000, 0.9510565162951535312, 1.000000000000000000, 0.9510565162951535312, 1.000000000000000000, 0.9510565162951535312, 1.000000000000000000, 0.9510565162951535312, 1.000000000000000000, 0.9510565162951535312, 1.000000000000000000, 0.9510565162951535312, 1.000000000000000000, 0.9510565162951535312, 1.000000000000000000, 0.9510565162951535312, 1.000000000000000000, 0.9510565162951535312, 1.000000000000000000, 0.9510565162951535312, 1.000000000000000000, 0.9510565162951535312, 1.000000000000000000, 0.9510565162951535312, 1.000000000000000000, 0.9510565162951535312, 1.000000000000000000, 0.9510565162951535312, 1.000000000000000000, 0.9510565162951535312, 1.000000000000000000, 0.9510565162951535312, 1.000000000000000000, 0.9510565162951535312, 1.000000000000000000, 0.9510565162951535312, 1.000000000000000000, 0.9510565162951535312, 1.000000000000000000, 0.9510565162951535312, 1.000000000000000000, 0.9510565162951535312, 1.000000000000000000, 0.9510565162951535312, 1.000000000000000000, 0.9510565162951535312, 1.000000000000000000, 0.9510565162951535312, 1.000000000000000000, 0.9510565162951535312, 1.000000000000000000, 0.9510565162951535312, 1.000000000000000000, 0.9510565162951535312, 1.000000000000000000, 0.9510565162951535312, 1.000000000000000000, 0.9510565162951535312, 1.000000000000000000, 0.9510565162951535312, 1.000000000000000000, 0.9510565162951535312, 1.000000000000000000, 0.9510565162951535312, 1.000000000000000000, 0.9510565162951535312, 1.000000000000000000, 0.9510565162951535312, 1.000000000000000000, 0.9510565162951535312, 1.000000000000000000, 0.9510565162951535312, 1.000000000000000000, 0.9510565162951535312, 1.000000000000000000, 0.9510565162951535312, 1.000000000000000000, 0.9510565162951535312, 1.000000000000000000, 0.9510565162951535312, 1.000000000000000000, 0.9510565162951535312, 1.000000000000000000, 0.9510565162951535312, 1.000000000000000000, 0.9510565162951535312, 1.000000000000000000, 0.9510565162951535312, 1.000000000000000000, 0.9510565162951535312, 1.000000000000000000, 0.9510565162951535312, 1.000000000000000000, 0.9510565162951535312, 1.000000000000000000, 0.9510565162951535312, 1.000000000000000000, 0.9510565162951535312, 1.000000000000000000, 0.9510565162951535312, 1.000000000000000000, 0.9510565162951535312, 1.000000000000000000, 0.9510565162951535312, 1.000000000000000000, 0.9510565162951535312, 1.000000000000000000, 0.9510565162951535312, 1.000000000000000000, 0.9510565162951535312, 1.000000000000000000, 0.9510565162951535312, 1.000000000000000000, 0.9510565162951535312, 1.000000000000000000, 0.9510565162951535312, 1.000000000000000000, 0.9510565162951535312, 1.000000000000000000, 0.9510565162951535312, 1.000000000000000000, 0.9510565162951535312, 1.000000000000000000, 0.9510565162951535312, 1.000000000000000000, 0.9510565162951535312, 1.000000000000000000, 0.9510565162951535312, 1.000000000000000000, 0.9510565162951535312, 1.000000000000000000, 0.9510565162951535312, 1.000000000000000000, 0.9510565162951535312, 1.000000000000000000, 0.9510565162951535312, 1.000000000000000000, 0.9510565162951535312, 1.000000000000000000, 0.9510565162951535312, 1.000000000000000000, 0.9510565162951535312, 1.000000000000000000, 0.9510565162951535312, 1.000000000000000000, 0.9510565162951535312, 1.000000000000000000, 0.9510565162951535312, 1.000000000000000000, 0.9510565162951535312, 1.000000000000000000, 0.9510565162951535312, 1.000000000000000000, 0.9510565162951535312, 1.000000000000000000, 0.9510565162951535312, 1.000000000000000000, 0.9510565162951535312, 1.000000000000000000, 0.9510565162951535312, 1.000000000000000000, 0.9510565162951535312, 1.000000000000000000, 0.9510565162951535312, 1.000000000000000000, 0.9510565162951535312, 1.000000000000000000, 0.9510565162951535312, 1.000000000000000000, 0.9510565162951535312, 1.000000000000000000, 0.9510565162951535312, 1.000000000000000000, 0.9510565162951535312, 1.000000000000000000, 0.9510565162951535312, 1.000000000000000000, 0.9510565162951535312, 1.000000000000000000, 0.9510565162951535312, 1.000000000000000000, 0.9510565162951535312, 1.000000000000000000, 0.9510565162951535312, 1.000000000000000000, 0.9510565162951535312, 1.000000000000000000, 0.9510565162951535312, 1.000000000000000000, 0.9510565162951535312, 1.000000000000000000, 0.9510565162951535312, 1.000000000000000000, 0.9510565162951535312, 1.000000000000000000, 0.9510565162951535312, 1.000000000000000000, 0.9510565162951535312, 1.000000000000000000, 0.9510565162951535312, 1.000000000000000000, 0.9510565162951535312, 1.000000000000000000, 0.9836253951315730992, 0.9782074146920101132) ) ) 
 REPRESENTATION_ITEM ( '' )  SURFACE ( )  );
#777=CARTESIAN_POINT ( 'NONE',  ( -143.3790856849358306, -183.3630981290893374, 55.53486410454105027 ) ) ;
#778=CARTESIAN_POINT ( 'NONE',  ( -151.4692556286852891, -186.8130981290893260, 59.65701158161632378 ) ) ;
#782=CARTESIAN_POINT ( 'NONE',  ( -154.3824083646099439, -173.4938272943107336, 40.69124936498395328 ) ) ;
#783=CARTESIAN_POINT ( 'NONE',  ( -145.6429501568359797, -195.2084106276440423, 41.63779006702063867 ) ) ;
#794=ORIENTED_EDGE ( 'NONE', *, *, #18272, .F. ) ;
#802=CARTESIAN_POINT ( 'NONE',  ( -148.3790856849358306, -162.3891397928654499, 40.14644641866477315 ) ) ;
#808=CARTESIAN_POINT ( 'NONE',  ( -148.5561028927606344, -162.9938272943107336, 58.62277379824867296 ) ) ;
#810=CARTESIAN_POINT ( 'NONE',  ( -160.8964159109769696, -191.0084106276440821, 52.72008163687743121 ) ) ;
#812=CARTESIAN_POINT ( 'NONE',  ( -154.5594255724347761, -174.9630981290893033, 59.16757674456785310 ) ) ;
#825=CARTESIAN_POINT ( 'NONE',  ( -145.2889157411863437, -191.6130981290893089, 41.15050349809589392 ) ) ;
#826=CARTESIAN_POINT ( 'NONE',  ( -160.8964159109769696, -158.0084106276440536, 52.72008163687743121 ) ) ;
#827=EDGE_CURVE ( 'NONE', #3465, #5698, #13959, .T. ) ;
#828=( BOUNDED_CURVE ( )  B_SPLINE_CURVE ( 2, ( #10493, #14000, #5408, #2107, #20734, #15765, #8844, #5735, #669, #17411, #12126, #17303, #2317 ),
 .UNSPECIFIED., .F., .F. ) 
 B_SPLINE_CURVE_WITH_KNOTS ( ( 3, 2, 2, 2, 2, 2, 3 ),
 ( 0.5178571428571429047, 0.5214285714285714635, 0.5285714285714285809, 0.5357142857142856984, 0.5428571428571428159, 0.5500000000000000444, 0.5535714285714286031 ),
 .UNSPECIFIED. ) 
 CURVE ( )  GEOMETRIC_REPRESENTATION_ITEM ( )  RATIONAL_B_SPLINE_CURVE ( ( 0.9755282581475768211, 0.9755282581475771542, 1.000000000000000000, 0.9510565162951535312, 1.000000000000000000, 0.9510565162951535312, 1.000000000000000000, 0.9510565162951535312, 1.000000000000000000, 0.9510565162951535312, 1.000000000000000000, 0.9755282581475768211, 0.9755282581475768211 ) ) 
 REPRESENTATION_ITEM ( '' )  );
#831=DIRECTION ( 'NONE',  ( -0.000000000000000000, 1.000000000000000000, -0.000000000000000000 ) ) ;
#832=CARTESIAN_POINT ( 'NONE',  ( -161.4692556286853176, -157.5630981290892976, 49.65701158161630957 ) ) ;
#837=CARTESIAN_POINT ( 'NONE',  ( -159.0959885057557983, -190.5938272943107279, 55.19815736654470584 ) ) ;
#846=VERTEX_POINT ( 'NONE', #3620 ) ;
#849=LINE ( 'NONE', #21030, #3140 ) ;
#854=CARTESIAN_POINT ( 'NONE',  ( -160.8964159109769696, -167.0438272943106881, 46.59394152635518083 ) ) ;
#856=CARTESIAN_POINT ( 'NONE',  ( -151.4692556286852891, -183.8130981290892692, 60.17163382399899518 ) ) ;
#864=CARTESIAN_POINT ( 'NONE',  ( -145.6429501568359797, -156.2084106276440423, 41.63779006702063867 ) ) ;
#866=CARTESIAN_POINT ( 'NONE',  ( -159.5594255724347761, -164.1891397928654897, 55.53486410454104316 ) ) ;
#868=EDGE_CURVE ( 'NONE', #19655, #14419, #11582, .T. ) ;
#874=ORIENTED_EDGE ( 'NONE', *, *, #1015, .F. ) ;
#880=CARTESIAN_POINT ( 'NONE',  ( -154.5594255724347761, -167.1630981290892919, 40.14644641866476604 ) ) ;
#881=CARTESIAN_POINT ( 'NONE',  ( -151.4692556286852607, -156.8130981290892692, 59.65701158161632378 ) ) ;
#882=EDGE_CURVE ( 'NONE', #1447, #4126, #15074, .T. ) ;
#888=CARTESIAN_POINT ( 'NONE',  ( -151.4692556286852891, -167.6438272943107108, 39.74470866294723947 ) ) ;
#897=ORIENTED_EDGE ( 'NONE', *, *, #12786, .F. ) ;
#905=EDGE_CURVE ( 'NONE', #6804, #17969, #16936, .T. ) ;
#907=CARTESIAN_POINT ( 'NONE',  ( -141.4692556286852891, -159.9891397928654726, 49.65701158161630957 ) ) ;
#908=CARTESIAN_POINT ( 'NONE',  ( -148.3790856849358306, -159.6630981290892919, 59.16757674456786020 ) ) ;
#914=CARTESIAN_POINT ( 'NONE',  ( -154.3824083646099439, -169.2938272943107165, 58.62277379824867296 ) ) ;
#916=CARTESIAN_POINT ( 'NONE',  ( -157.2955611005346270, -194.6084106276440195, 41.63779006702063867 ) ) ;
#920=CIRCLE ( 'NONE', #13247, 10.00000000000000888 ) ;
#933=CARTESIAN_POINT ( 'NONE',  ( -159.5594255724347761, -188.7891397928654555, 43.77915905869157598 ) ) ;
#936=CARTESIAN_POINT ( 'NONE',  ( -161.4692556286853176, -160.5630981290892976, 49.65701158161630957 ) ) ;
#941=CARTESIAN_POINT ( 'NONE',  ( -148.5561028927606344, -194.7938272943107449, 40.69124936498395328 ) ) ;
#952=ORIENTED_EDGE ( 'NONE', *, *, #905, .F. ) ;
#954=( BOUNDED_CURVE ( )  B_SPLINE_CURVE ( 2, ( #7542, #12488, #482, #12377, #10736, #21095, #17438, #15682, #5541, #5870, #19215, #16001, #12704 ),
 .UNSPECIFIED., .F., .F. ) 
 B_SPLINE_CURVE_WITH_KNOTS ( ( 3, 2, 2, 2, 2, 2, 3 ),
 ( 0.7321428571428572063, 0.7357142857142857650, 0.7428571428571428825, 0.7500000000000000000, 0.7571428571428571175, 0.7642857142857142350, 0.7678571428571427937 ),
 .UNSPECIFIED. ) 
 CURVE ( )  GEOMETRIC_REPRESENTATION_ITEM ( )  RATIONAL_B_SPLINE_CURVE ( ( 0.9755282581475768211, 0.9755282581475771542, 1.000000000000000000, 0.9510565162951535312, 1.000000000000000000, 0.9510565162951535312, 1.000000000000000000, 0.9510565162951535312, 1.000000000000000000, 0.9510565162951535312, 1.000000000000000000, 0.9755282581475771542, 0.9755282581475768211 ) ) 
 REPRESENTATION_ITEM ( '' )  );
#960=CARTESIAN_POINT ( 'NONE',  ( -160.8964159109769696, -166.7438272943107336, 52.72008163687743121 ) ) ;
#962=CARTESIAN_POINT ( 'NONE',  ( -161.4692556286852607, -184.4130981290893203, 52.90620854394536821 ) ) ;
#971=CARTESIAN_POINT ( 'NONE',  ( -142.0420953463936087, -159.6584106276440593, 49.65701158161630957 ) ) ;
#978=EDGE_LOOP ( 'NONE', ( #18658, #5825, #7797, #16450 ) ) ;
#979=VECTOR ( 'NONE', #11785, 1000.000000000000227 ) ;
#981=CARTESIAN_POINT ( 'NONE',  ( -145.2889157411863437, -156.5391397928654555, 41.15050349809589392 ) ) ;
#992=PRESENTATION_STYLE_ASSIGNMENT (( #9054 ) ) ;
#999=CARTESIAN_POINT ( 'NONE',  ( -159.0959885057557983, -167.1938272943107222, 44.11586579668791330 ) ) ;
#1000=CARTESIAN_POINT ( 'NONE',  ( -145.6429501568359797, -181.1084106276440195, 57.67623309621197336 ) ) ;
#1002=CARTESIAN_POINT ( 'NONE',  ( -142.0420953463935803, -171.5084106276440536, 46.59394152635518793 ) ) ;
#1010=ORIENTED_EDGE ( 'NONE', *, *, #20723, .T. ) ;
#1011=EDGE_CURVE ( 'NONE', #20985, #18246, #14067, .T. ) ;
#1015=EDGE_CURVE ( 'NONE', #4150, #16205, #1153, .T. ) ;
#1020=CARTESIAN_POINT ( 'NONE',  ( -143.9637021292202235, -116.9891397928655010, 36.65701158161628825 ) ) ;
#1021=CARTESIAN_POINT ( 'NONE',  ( -148.3790856849358306, -156.3891397928654783, 40.14644641866477315 ) ) ;
#1027=CARTESIAN_POINT ( 'NONE',  ( -154.3824083646099439, -158.4938272943107052, 40.69124936498395328 ) ) ;
#1040=CARTESIAN_POINT ( 'NONE',  ( -154.5594255724347761, -155.1630981290892919, 40.14644641866476604 ) ) ;
#1046=CARTESIAN_POINT ( 'NONE',  ( -154.5594255724347761, -186.0891397928654953, 40.14644641866476604 ) ) ;
#1049=CARTESIAN_POINT ( 'NONE',  ( -148.5561028927606344, -194.7938272943107449, 40.69124936498395328 ) ) ;
#1073=CARTESIAN_POINT ( 'NONE',  ( -154.3824083646099439, -155.7584106276440536, 40.69124936498395328 ) ) ;
#1074=CARTESIAN_POINT ( 'NONE',  ( -142.0420953463936087, -168.3938272943107393, 49.65701158161630957 ) ) ;
#1076=CARTESIAN_POINT ( 'NONE',  ( -143.3790856849358306, -188.7630981290893146, 43.77915905869157598 ) ) ;
#1090=ORIENTED_EDGE ( 'NONE', *, *, #12786, .T. ) ;
#1092=ADVANCED_FACE ( 'NONE', ( #10668 ), #19042, .T. ) ;
#1099=CARTESIAN_POINT ( 'NONE',  ( -151.4692556286852607, -183.8130981290892692, 59.65701158161632378 ) ) ;
#1107=CARTESIAN_POINT ( 'NONE',  ( -151.4692556286852891, -170.6438272943107677, 39.74470866294723947 ) ) ;
#1108=CARTESIAN_POINT ( 'NONE',  ( -159.0959885057557983, -185.4584106276440707, 44.11586579668791330 ) ) ;
#1111=CARTESIAN_POINT ( 'NONE',  ( -151.4692556286852891, -173.9084106276440593, 39.74470866294723947 ) ) ;
#1118=VECTOR ( 'NONE', #4322, 1000.000000000000000 ) ;
#1129=CARTESIAN_POINT ( 'NONE',  ( -157.6495955161842062, -158.0391397928654271, 58.16351966513671812 ) ) ;
#1135=CARTESIAN_POINT ( 'NONE',  ( -157.2955611005346270, -193.7084106276440423, 57.67623309621198047 ) ) ;
#1137=CARTESIAN_POINT ( 'NONE',  ( -160.8964159109769696, -188.1584106276440593, 49.65701158161630957 ) ) ;
#1145=ORIENTED_EDGE ( 'NONE', *, *, #15285, .F. ) ;
#1151=CARTESIAN_POINT ( 'NONE',  ( -157.6495955161842062, -176.0391397928654555, 58.16351966513671812 ) ) ;
#1152=CARTESIAN_POINT ( 'NONE',  ( -151.4692556286852891, -184.7391397928654442, 60.17163382399899518 ) ) ;
#1153=( BOUNDED_CURVE ( )  B_SPLINE_CURVE ( 2, ( #10559, #8800, #5578, #10982, #14279, #12302, #3832, #2171, #9234, #20910, #21025, #3938, #5907 ),
 .UNSPECIFIED., .F., .F. ) 
 B_SPLINE_CURVE_WITH_KNOTS ( ( 3, 2, 2, 2, 2, 2, 3 ),
 ( 0.6250000000000000000, 0.6285714285714285587, 0.6357142857142856762, 0.6428571428571429047, 0.6500000000000000222, 0.6571428571428571397, 0.6607142857142856984 ),
 .UNSPECIFIED. ) 
 CURVE ( )  GEOMETRIC_REPRESENTATION_ITEM ( )  RATIONAL_B_SPLINE_CURVE ( ( 0.9755282581475768211, 0.9755282581475768211, 1.000000000000000000, 0.9510565162951535312, 1.000000000000000000, 0.9510565162951535312, 1.000000000000000000, 0.9510565162951535312, 1.000000000000000000, 0.9510565162951535312, 1.000000000000000000, 0.9755282581475768211, 0.9755282581475768211 ) ) 
 REPRESENTATION_ITEM ( '' )  );
#1156=CARTESIAN_POINT ( 'NONE',  ( -148.5561028927606344, -185.7938272943107449, 40.69124936498395328 ) ) ;
#1162=CARTESIAN_POINT ( 'NONE',  ( -151.4692556286852891, -185.6438272943107393, 39.74470866294723947 ) ) ;
#1177=CARTESIAN_POINT ( 'NONE',  ( -142.0420953463935803, -156.5084106276439968, 46.59394152635518793 ) ) ;
#1178=CARTESIAN_POINT ( 'NONE',  ( -160.8964159109769696, -169.7438272943107052, 52.72008163687743121 ) ) ;
#1180=CARTESIAN_POINT ( 'NONE',  ( -161.4692556286852607, -181.7130981290892464, 46.40781461928724383 ) ) ;
#1187=CARTESIAN_POINT ( 'NONE',  ( -151.4692556286852891, -126.9891397928655010, 39.65701158161630246 ) ) ;
#1188=CARTESIAN_POINT ( 'NONE',  ( -151.4692556286852891, -155.9084106276440593, 39.74470866294723947 ) ) ;
#1201=CARTESIAN_POINT ( 'NONE',  ( -160.8964159109769696, -164.3084106276440650, 46.59394152635518793 ) ) ;
#1214=CARTESIAN_POINT ( 'NONE',  ( -159.0959885057557983, -172.5938272943107279, 55.19815736654470584 ) ) ;
#1215=CARTESIAN_POINT ( 'NONE',  ( -143.8425227516148084, -189.3584106276440480, 44.11586579668791330 ) ) ;
#1219=CARTESIAN_POINT ( 'NONE',  ( -142.0420953463935803, -165.5084106276439968, 46.59394152635518793 ) ) ;
#1234=CARTESIAN_POINT ( 'NONE',  ( -154.5594255724347761, -163.8891397928654499, 59.16757674456785310 ) ) ;
#1242=CARTESIAN_POINT ( 'NONE',  ( -143.8425227516148084, -192.3584106276440480, 44.11586579668791330 ) ) ;
#1244=CARTESIAN_POINT ( 'NONE',  ( -159.0959885057557983, -182.4584106276440707, 44.11586579668791330 ) ) ;
#1245=EDGE_LOOP ( 'NONE', ( #6658, #5520, #15881, #12747 ) ) ;
#1250=CARTESIAN_POINT ( 'NONE',  ( -151.4692556286852891, -185.3130981290893260, 39.65701158161630246 ) ) ;
#1260=CARTESIAN_POINT ( 'NONE',  ( -161.4692556286853176, -191.4891397928654726, 49.65701158161630957 ) ) ;
#1262=CARTESIAN_POINT ( 'NONE',  ( -151.4692556286852891, -196.9891397928655010, 39.65701158161630246 ) ) ;
#1264=CARTESIAN_POINT ( 'NONE',  ( -148.5561028927606344, -188.7938272943107449, 40.69124936498395328 ) ) ;
#1270=CARTESIAN_POINT ( 'NONE',  ( -142.0420953463935803, -180.5438272943106881, 52.72008163687743831 ) ) ;
#1289=CARTESIAN_POINT ( 'NONE',  ( -154.3824083646099439, -161.4938272943107336, 40.69124936498395328 ) ) ;
#1291=CARTESIAN_POINT ( 'NONE',  ( -154.5594255724347761, -174.9630981290893033, 59.16757674456785310 ) ) ;
#1297=CARTESIAN_POINT ( 'NONE',  ( -153.0531000319306827, -168.1622583705451746, 39.65701158161629536 ) ) ;
#1313=CARTESIAN_POINT ( 'NONE',  ( -157.2955611005346270, -166.7084106276440423, 57.67623309621198047 ) ) ;
#1314=CARTESIAN_POINT ( 'NONE',  ( -160.8964159109769696, -187.8938272943107393, 49.65701158161630957 ) ) ;
#1317=CARTESIAN_POINT ( 'NONE',  ( -141.4692556286852891, -189.2130981290893317, 52.90620854394536821 ) ) ;
#1318=CARTESIAN_POINT ( 'NONE',  ( -148.3790856849358306, -174.3891397928654783, 40.14644641866477315 ) ) ;
#1323=CARTESIAN_POINT ( 'NONE',  ( -142.0420953463936087, -165.3938272943107393, 49.65701158161630957 ) ) ;
#1324=CARTESIAN_POINT ( 'NONE',  ( -148.5561028927606344, -184.2584106276440536, 58.62277379824867296 ) ) ;
#1327=CARTESIAN_POINT ( 'NONE',  ( -159.0959885057557983, -173.4584106276440423, 44.11586579668791330 ) ) ;
#1346=CARTESIAN_POINT ( 'NONE',  ( -156.4692864601533131, -155.0638355923473455, 40.99677534440144200 ) ) ;
#1349=EDGE_CURVE ( 'NONE', #2985, #4126, #2691, .T. ) ;
#1351=DIRECTION ( 'NONE',  ( -0.000000000000000000, 1.000000000000000000, -0.000000000000000000 ) ) ;
#1352=ORIENTED_EDGE ( 'NONE', *, *, #661, .T. ) ;
#1354=CARTESIAN_POINT ( 'NONE',  ( -157.2955611005346270, -158.3438272943106995, 41.63779006702063867 ) ) ;
#1356=CARTESIAN_POINT ( 'NONE',  ( -151.4692556286852891, -181.4084106276440025, 59.56931450028537967 ) ) ;
#1358=CARTESIAN_POINT ( 'NONE',  ( -151.4692556286852607, -162.2391397928654442, 39.65701158161629536 ) ) ;
#1361=ORIENTED_EDGE ( 'NONE', *, *, #10597, .F. ) ;
#1363=ORIENTED_EDGE ( 'NONE', *, *, #15641, .T. ) ;
#1367=CARTESIAN_POINT ( 'NONE',  ( -156.4692594822809610, -155.3725178653323553, 40.99675976862926063 ) ) ;
#1370=CARTESIAN_POINT ( 'NONE',  ( -154.5594255724347761, -187.8891397928654783, 59.16757674456785310 ) ) ;
#1372=FACE_OUTER_BOUND ( 'NONE', #14553, .T. ) ;
#1374=CARTESIAN_POINT ( 'NONE',  ( -154.3824083646099439, -191.4938272943107336, 40.69124936498395328 ) ) ;
#1380=CARTESIAN_POINT ( 'NONE',  ( -151.4692556286852891, -179.6438272943107393, 39.74470866294723947 ) ) ;
#1382=CARTESIAN_POINT ( 'NONE',  ( -158.9748091281504401, -126.9891397928655010, 36.65701158161628115 ) ) ;
#1383=ORIENTED_EDGE ( 'NONE', *, *, #20635, .T. ) ;
#1390=ORIENTED_EDGE ( 'NONE', *, *, #18659, .T. ) ;
#1399=CARTESIAN_POINT ( 'NONE',  ( -148.5561028927606344, -158.7938272943107449, 40.69124936498395328 ) ) ;
#1401=CARTESIAN_POINT ( 'NONE',  ( -141.4692556286852891, -183.2130981290892748, 52.90620854394536821 ) ) ;
#1407=CARTESIAN_POINT ( 'NONE',  ( -161.4692556286852891, -167.6391397928654499, 46.40781461928724383 ) ) ;
#1417=CARTESIAN_POINT ( 'NONE',  ( -136.4581486297550441, -126.9891397928655010, 49.65701158161631668 ) ) ;
#1425=CARTESIAN_POINT ( 'NONE',  ( -160.8964159109769696, -170.1584106276440593, 49.65701158161630957 ) ) ;
#1426=CARTESIAN_POINT ( 'NONE',  ( -154.3824083646099439, -188.4938272943107336, 40.69124936498395328 ) ) ;
#1427=CARTESIAN_POINT ( 'NONE',  ( -157.6495955161842062, -167.0130981290893146, 41.15050349809589392 ) ) ;
#1435=CARTESIAN_POINT ( 'NONE',  ( -160.8964159109769696, -157.8938272943107393, 49.65701158161630957 ) ) ;
#1436=CARTESIAN_POINT ( 'NONE',  ( -154.3824083646099439, -184.5584106276440650, 58.62277379824867296 ) ) ;
#1441=CARTESIAN_POINT ( 'NONE',  ( -145.6429501568359797, -168.2084106276440139, 41.63779006702063867 ) ) ;
#1447=VERTEX_POINT ( 'NONE', #18595 ) ;
#1457=CARTESIAN_POINT ( 'NONE',  ( -141.4692556286852891, -171.2130981290893033, 52.90620854394536821 ) ) ;
#1465=CARTESIAN_POINT ( 'NONE',  ( -148.5561028927606344, -159.9938272943107336, 58.62277379824867296 ) ) ;
#1467=CARTESIAN_POINT ( 'NONE',  ( -160.8964159109769696, -185.1584106276440309, 49.65701158161630957 ) ) ;
#1484=CYLINDRICAL_SURFACE ( 'NONE', #8889, 10.00000000000000888 ) ;
#1485=CARTESIAN_POINT ( 'NONE',  ( -148.3790856849358306, -183.3891397928654783, 40.14644641866477315 ) ) ;
#1488=CARTESIAN_POINT ( 'NONE',  ( -159.0959885057557983, -188.1938272943107222, 44.11586579668791330 ) ) ;
#1493=CARTESIAN_POINT ( 'NONE',  ( -143.8425227516148084, -180.6938272943107506, 55.19815736654470584 ) ) ;
#1496=EDGE_LOOP ( 'NONE', ( #21649, #1881, #15539, #573, #5295, #13906, #7867, #3916 ) ) ;
#1511=CARTESIAN_POINT ( 'NONE',  ( -159.0959885057557983, -157.5938272943107279, 55.19815736654470584 ) ) ;
#1513=CARTESIAN_POINT ( 'NONE',  ( -148.3790856849358306, -182.4630981290893033, 40.14644641866477315 ) ) ;
#1514=DIRECTION ( 'NONE',  ( 0.000000000000000000, 0.000000000000000000, 1.000000000000000000 ) ) ;
#1519=CARTESIAN_POINT ( 'NONE',  ( -161.4692556286852891, -182.6391397928654499, 46.40781461928724383 ) ) ;
#1520=CARTESIAN_POINT ( 'NONE',  ( -143.9637021292202235, -126.9891397928655010, 36.65701158161628825 ) ) ;
#1525=VERTEX_POINT ( 'NONE', #17247 ) ;
#1533=CARTESIAN_POINT ( 'NONE',  ( -145.6429501568359797, -165.2084106276440423, 41.63779006702063867 ) ) ;
#1534=CARTESIAN_POINT ( 'NONE',  ( -143.8425227516148084, -186.6938272943107222, 55.19815736654470584 ) ) ;
#1546=CARTESIAN_POINT ( 'NONE',  ( -154.3824083646099439, -157.2938272943107449, 58.62277379824867296 ) ) ;
#1547=CARTESIAN_POINT ( 'NONE',  ( -151.4692556286852891, -179.9084106276440593, 39.74470866294723947 ) ) ;
#1550=CARTESIAN_POINT ( 'NONE',  ( -148.5561028927606344, -157.2584106276440536, 58.62277379824867296 ) ) ;
#1552=CARTESIAN_POINT ( 'NONE',  ( -158.9748091281504401, -126.9891397928655010, 36.65701158161628115 ) ) ;
#1575=CARTESIAN_POINT ( 'NONE',  ( -151.4692556286852891, -187.4084106276440309, 59.56931450028537967 ) ) ;
#1577=CARTESIAN_POINT ( 'NONE',  ( -154.3824083646099439, -185.7584106276440536, 40.69124936498395328 ) ) ;
#1586=ORIENTED_EDGE ( 'NONE', *, *, #14863, .T. ) ;
#1593=CARTESIAN_POINT ( 'NONE',  ( -161.4692556286853176, -176.4891397928654442, 49.65701158161630957 ) ) ;
#1595=CARTESIAN_POINT ( 'NONE',  ( -157.6495955161842062, -194.9391397928654897, 41.15050349809589392 ) ) ;
#1598=CARTESIAN_POINT ( 'NONE',  ( -159.0959885057557983, -184.5938272943107279, 55.19815736654470584 ) ) ;
#1602=ORIENTED_EDGE ( 'NONE', *, *, #13466, .F. ) ;
#1617=CARTESIAN_POINT ( 'NONE',  ( -143.8425227516148084, -165.6938272943107222, 55.19815736654470584 ) ) ;
#1619=CARTESIAN_POINT ( 'NONE',  ( -161.4692556286852607, -178.4130981290893203, 52.90620854394536821 ) ) ;
#1626=CARTESIAN_POINT ( 'NONE',  ( -159.5594255724347761, -167.1891397928654897, 55.53486410454104316 ) ) ;
#1644=CARTESIAN_POINT ( 'NONE',  ( -148.5561028927606344, -168.0584106276440366, 40.69124936498395328 ) ) ;
#1645=CARTESIAN_POINT ( 'NONE',  ( -154.3824083646099439, -191.4938272943107336, 40.69124936498395328 ) ) ;
#1648=CARTESIAN_POINT ( 'NONE',  ( -141.4692556286852891, -189.0630981290892976, 49.65701158161630957 ) ) ;
#1649=ADVANCED_BREP_SHAPE_REPRESENTATION ( '', ( #7211, #12657 ), #7417 ) ;
#1650=CARTESIAN_POINT ( 'NONE',  ( -143.3790856849358306, -176.7630981290893146, 43.77915905869157598 ) ) ;
#1655=CARTESIAN_POINT ( 'NONE',  ( -143.8425227516148084, -162.6938272943107222, 55.19815736654470584 ) ) ;
#1656=CARTESIAN_POINT ( 'NONE',  ( -145.6429501568359797, -175.1084106276440480, 57.67623309621197336 ) ) ;
#1658=CARTESIAN_POINT ( 'NONE',  ( -157.2955611005346270, -158.6084106276440480, 41.63779006702063867 ) ) ;
#1660=LINE ( 'NONE', #8607, #8486 ) ;
#1664=VERTEX_POINT ( 'NONE', #16023 ) ;
#1678=DIRECTION ( 'NONE',  ( -0.000000000000000000, 1.000000000000000000, -0.000000000000000000 ) ) ;
#1686=CARTESIAN_POINT ( 'NONE',  ( -154.3824083646099439, -185.7584106276440536, 40.69124936498395328 ) ) ;
#1688=CARTESIAN_POINT ( 'NONE',  ( -145.6429501568359797, -175.1084106276440480, 57.67623309621198047 ) ) ;
#1689=ORIENTED_EDGE ( 'NONE', *, *, #18515, .T. ) ;
#1706=CARTESIAN_POINT ( 'NONE',  ( -157.6495955161842062, -182.9391397928654612, 41.15050349809590102 ) ) ;
#1713=CARTESIAN_POINT ( 'NONE',  ( -151.4692556286852891, -170.6438272943107677, 39.74470866294723947 ) ) ;
#1728=FACE_OUTER_BOUND ( 'NONE', #336, .T. ) ;
#1730=CARTESIAN_POINT ( 'NONE',  ( -153.0531000319306827, -170.2362167067689995, 39.65701158161629536 ) ) ;
#1731=CARTESIAN_POINT ( 'NONE',  ( -159.0959885057557983, -164.1938272943107222, 44.11586579668791330 ) ) ;
#1732=CARTESIAN_POINT ( 'NONE',  ( -159.5594255724347761, -169.2630981290892862, 55.53486410454104316 ) ) ;
#1748=ORIENTED_EDGE ( 'NONE', *, *, #3444, .T. ) ;
#1749=CARTESIAN_POINT ( 'NONE',  ( -143.3790856849358306, -168.3630981290893089, 55.53486410454105027 ) ) ;
#1755=CARTESIAN_POINT ( 'NONE',  ( -143.8425227516148084, -156.3584106276440480, 44.11586579668791330 ) ) ;
#1756=CARTESIAN_POINT ( 'NONE',  ( -142.0420953463935803, -189.2438272943107052, 46.59394152635518083 ) ) ;
#1765=CARTESIAN_POINT ( 'NONE',  ( -151.4692556286852891, -158.6438272943107108, 39.74470866294723947 ) ) ;
#1766=CARTESIAN_POINT ( 'NONE',  ( -142.0420953463936087, -174.6584106276440593, 49.65701158161630957 ) ) ;
#1769=CARTESIAN_POINT ( 'NONE',  ( -154.3824083646099439, -164.7584106276440536, 40.69124936498395328 ) ) ;
#1789=ADVANCED_FACE ( 'NONE', ( #14377 ), #15918, .T. ) ;
#1793=DIRECTION ( 'NONE',  ( 0.000000000000000000, 0.000000000000000000, 1.000000000000000000 ) ) ;
#1797=CARTESIAN_POINT ( 'NONE',  ( -160.8964159109769696, -191.3084106276440650, 46.59394152635518793 ) ) ;
#1799=CARTESIAN_POINT ( 'NONE',  ( -151.4692556286852891, -173.9084106276440593, 39.74470866294723947 ) ) ;
#1800=VERTEX_POINT ( 'NONE', #17680 ) ;
#1814=CARTESIAN_POINT ( 'NONE',  ( -154.5594255724347761, -181.8891397928654783, 59.16757674456785310 ) ) ;
#1817=CARTESIAN_POINT ( 'NONE',  ( -159.5594255724347761, -194.7891397928654555, 43.77915905869157598 ) ) ;
#1821=CARTESIAN_POINT ( 'NONE',  ( -154.3824083646099439, -178.2938272943107165, 58.62277379824867296 ) ) ;
#1822=EDGE_CURVE ( 'NONE', #20771, #7641, #16744, .T. ) ;
#1824=CARTESIAN_POINT ( 'NONE',  ( -142.0420953463936087, -195.3938272943107393, 49.65701158161630957 ) ) ;
#1825=ORIENTED_EDGE ( 'NONE', *, *, #3006, .F. ) ;
#1833=APPLICATION_CONTEXT ( 'automotive_design' ) ;
#1835=CYLINDRICAL_SURFACE ( 'NONE', #10904, 10.00000000000000888 ) ;
#1839=CARTESIAN_POINT ( 'NONE',  ( -151.4692556286852891, -196.9891397928655010, 49.65701158161630957 ) ) ;
#1842=CARTESIAN_POINT ( 'NONE',  ( -151.4692556286852891, -165.8130981290892692, 60.17163382399899518 ) ) ;
#1861=CARTESIAN_POINT ( 'NONE',  ( -142.0420953463936087, -156.6584106276440593, 49.65701158161630957 ) ) ;
#1862=CARTESIAN_POINT ( 'NONE',  ( -159.0959885057557983, -185.1938272943107222, 44.11586579668791330 ) ) ;
#1872=CARTESIAN_POINT ( 'NONE',  ( -160.8964159109769696, -176.0084106276440536, 52.72008163687743121 ) ) ;
#1874=CARTESIAN_POINT ( 'NONE',  ( -148.5561028927606344, -160.2584106276440536, 58.62277379824867296 ) ) ;
#1881=ORIENTED_EDGE ( 'NONE', *, *, #2823, .T. ) ;
#1889=CARTESIAN_POINT ( 'NONE',  ( -161.4692556286853176, -190.5630981290892976, 49.65701158161630957 ) ) ;
#1895=CARTESIAN_POINT ( 'NONE',  ( -160.8964159109769696, -182.0084106276440821, 52.72008163687743121 ) ) ;
#1897=CARTESIAN_POINT ( 'NONE',  ( -148.5561028927606344, -180.0584106276440366, 40.69124936498395328 ) ) ;
#1904=ORIENTED_EDGE ( 'NONE', *, *, #7576, .F. ) ;
#1908=FACE_OUTER_BOUND ( 'NONE', #2896, .T. ) ;
#1909=DIRECTION ( 'NONE',  ( -0.000000000000000000, 1.000000000000000000, -0.000000000000000000 ) ) ;
#1915=CARTESIAN_POINT ( 'NONE',  ( -159.5594255724347761, -170.1891397928654897, 55.53486410454104316 ) ) ;
#1916=CARTESIAN_POINT ( 'NONE',  ( -161.4692556286852891, -181.4130981290892919, 52.90620854394536821 ) ) ;
#1922=CARTESIAN_POINT ( 'NONE',  ( -160.8964159109769696, -172.7438272943107336, 52.72008163687743121 ) ) ;
#1923=VECTOR ( 'NONE', #9629, 1000.000000000000000 ) ;
#1925=CARTESIAN_POINT ( 'NONE',  ( -161.4692556286853176, -170.4891397928654726, 49.65701158161630957 ) ) ;
#1926=CARTESIAN_POINT ( 'NONE',  ( -153.0531000319306827, -159.1622583705452030, 39.65701158161629536 ) ) ;
#1930=( BOUNDED_CURVE ( )  B_SPLINE_CURVE ( 2, ( #3588, #1926, #8661, #15383, #17126, #277, #7010, #20450, #10422, #5342, #12059, #18791, #15485 ),
 .UNSPECIFIED., .F., .F. ) 
 B_SPLINE_CURVE_WITH_KNOTS ( ( 3, 2, 2, 2, 2, 2, 3 ),
 ( 0.8750000000000000000, 0.8785714285714285587, 0.8857142857142856762, 0.8928571428571429047, 0.9000000000000000222, 0.9071428571428571397, 0.9107142857142856984 ),
 .UNSPECIFIED. ) 
 CURVE ( )  GEOMETRIC_REPRESENTATION_ITEM ( )  RATIONAL_B_SPLINE_CURVE ( ( 0.9755282581475768211, 0.9755282581475768211, 1.000000000000000000, 0.9510565162951535312, 1.000000000000000000, 0.9510565162951535312, 1.000000000000000000, 0.9510565162951535312, 1.000000000000000000, 0.9510565162951535312, 1.000000000000000000, 0.9755282581475768211, 0.9755282581475768211 ) ) 
 REPRESENTATION_ITEM ( '' )  );
#1946=CARTESIAN_POINT ( 'NONE',  ( -151.4692556286852891, -164.3130981290892976, 39.14238933923362396 ) ) ;
#1960=AXIS2_PLACEMENT_3D ( 'NONE', #17358, #831, #10968 ) ;
#1968=CARTESIAN_POINT ( 'NONE',  ( -154.3824083646099439, -157.5584106276440650, 58.62277379824867296 ) ) ;
#1969=CARTESIAN_POINT ( 'NONE',  ( -160.8964159109769696, -181.8938272943107108, 49.65701158161630957 ) ) ;
#1970=CARTESIAN_POINT ( 'NONE',  ( -143.3790856849358306, -178.2891397928654840, 55.53486410454105027 ) ) ;
#1971=CARTESIAN_POINT ( 'NONE',  ( -161.4692556286853176, -193.5630981290892976, 49.65701158161630957 ) ) ;
#1973=CARTESIAN_POINT ( 'NONE',  ( -153.0531000319306827, -172.8160212151857138, 59.65701158161631668 ) ) ;
#1976=ADVANCED_FACE ( 'NONE', ( #1372 ), #11393, .T. ) ;
#1981=CARTESIAN_POINT ( 'NONE',  ( -159.0959885057557983, -178.8584106276440480, 55.19815736654470584 ) ) ;
#1989=VERTEX_POINT ( 'NONE', #8104 ) ;
#2005=CARTESIAN_POINT ( 'NONE',  ( -154.3824083646099439, -185.4938272943107336, 40.69124936498395328 ) ) ;
#2006=DIRECTION ( 'NONE',  ( 0.000000000000000000, 0.000000000000000000, 1.000000000000000000 ) ) ;
#2008=CARTESIAN_POINT ( 'NONE',  ( -143.8425227516148084, -186.9584106276440423, 55.19815736654470584 ) ) ;
#2011=EDGE_CURVE ( 'NONE', #12281, #3209, #3020, .T. ) ;
#2012=CARTESIAN_POINT ( 'NONE',  ( -157.2955611005346270, -175.7084106276440707, 57.67623309621198047 ) ) ;
#2020=EDGE_LOOP ( 'NONE', ( #5798, #10588, #11007, #19307 ) ) ;
#2029=CARTESIAN_POINT ( 'NONE',  ( -141.4692556286852891, -172.1391397928654783, 52.90620854394536821 ) ) ;
#2035=CARTESIAN_POINT ( 'NONE',  ( -160.8964159109769696, -178.8938272943107393, 49.65701158161630957 ) ) ;
#2039=CARTESIAN_POINT ( 'NONE',  ( -151.4692556286852891, -196.9891397928655010, 59.65701158161632378 ) ) ;
#2057=CARTESIAN_POINT ( 'NONE',  ( -161.4692556286852607, -172.7130981290892464, 46.40781461928724383 ) ) ;
#2059=ADVANCED_FACE ( 'NONE', ( #18570 ), #3795, .T. ) ;
#2075=CARTESIAN_POINT ( 'NONE',  ( -151.4692556286852891, -126.9891397928655010, 59.65701158161632378 ) ) ;
#2079=CARTESIAN_POINT ( 'NONE',  ( -145.6429501568359797, -160.1084106276440480, 57.67623309621198047 ) ) ;
#2080=CARTESIAN_POINT ( 'NONE',  ( -157.2955611005345986, -179.3438272943107279, 41.63779006702063867 ) ) ;
#2084=CARTESIAN_POINT ( 'NONE',  ( -151.4692556286853176, -163.7391397928654726, 59.65701158161632378 ) ) ;
#2090=CARTESIAN_POINT ( 'NONE',  ( -143.8425227516148084, -165.9584106276440423, 55.19815736654470584 ) ) ;
#2097=EDGE_LOOP ( 'NONE', ( #20190, #14115, #19384, #1602, #19878, #10429 ) ) ;
#2107=CARTESIAN_POINT ( 'NONE',  ( -157.6495955161842062, -173.0130981290893146, 41.15050349809589392 ) ) ;
#2111=CARTESIAN_POINT ( 'NONE',  ( -151.4692556286852891, -179.6438272943107393, 39.74470866294723947 ) ) ;
#2112=CARTESIAN_POINT ( 'NONE',  ( -157.2955611005345986, -193.7084106276440423, 57.67623309621197336 ) ) ;
#2114=CARTESIAN_POINT ( 'NONE',  ( -159.0959885057557983, -179.4584106276440707, 44.11586579668791330 ) ) ;
#2135=CARTESIAN_POINT ( 'NONE',  ( -151.4692556286852891, -168.2391397928654726, 39.14238933923362396 ) ) ;
#2136=CARTESIAN_POINT ( 'NONE',  ( -151.4692556286852891, -195.2391397928655010, 39.65701158161630246 ) ) ;
#2138=LINE ( 'NONE', #9084, #15414 ) ;
#2141=CARTESIAN_POINT ( 'NONE',  ( -145.6429501568359797, -173.9438272943106938, 41.63779006702063867 ) ) ;
#2147=CARTESIAN_POINT ( 'NONE',  ( -151.4692556286852607, -159.2391397928654726, 39.65701158161629536 ) ) ;
#2155=CARTESIAN_POINT ( 'NONE',  ( -141.4692556286852891, -180.8391397928654385, 46.40781461928724383 ) ) ;
#2162=CARTESIAN_POINT ( 'NONE',  ( -145.2889157411863721, -173.6130981290893089, 41.15050349809590102 ) ) ;
#2171=CARTESIAN_POINT ( 'NONE',  ( -141.4692556286852891, -168.8391397928654385, 46.40781461928724383 ) ) ;
#2173=VECTOR ( 'NONE', #21757, 1000.000000000000000 ) ;
#2182=CARTESIAN_POINT ( 'NONE',  ( -151.4692556286852891, -158.9084106276440025, 39.74470866294723947 ) ) ;
#2183=CARTESIAN_POINT ( 'NONE',  ( -159.0959885057557983, -181.5938272943107279, 55.19815736654470584 ) ) ;
#2197=CARTESIAN_POINT ( 'NONE',  ( -143.8425227516148084, -162.9584106276440423, 55.19815736654470584 ) ) ;
#2199=CARTESIAN_POINT ( 'NONE',  ( 0.000000000000000000, -126.9891397928655010, 0.000000000000000000 ) ) ;
#2219=CARTESIAN_POINT ( 'NONE',  ( -159.0959885057557983, -178.5938272943107279, 55.19815736654470584 ) ) ;
#2220=CARTESIAN_POINT ( 'NONE',  ( -151.4692556286852891, -193.4084106276440593, 59.56931450028537256 ) ) ;
#2222=CARTESIAN_POINT ( 'NONE',  ( -148.5561028927606344, -178.2584106276440536, 58.62277379824867296 ) ) ;
#2229=ORIENTED_EDGE ( 'NONE', *, *, #20799, .T. ) ;
#2230=EDGE_CURVE ( 'NONE', #20856, #18762, #16903, .T. ) ;
#2239=CARTESIAN_POINT ( 'NONE',  ( -151.4692556286852891, -172.7391397928655010, 60.17163382399899518 ) ) ;
#2245=CARTESIAN_POINT ( 'NONE',  ( -142.0420953463935803, -168.5438272943107165, 52.72008163687743831 ) ) ;
#2254=ORIENTED_EDGE ( 'NONE', *, *, #72, .F. ) ;
#2259=DIRECTION ( 'NONE',  ( -0.000000000000000000, -1.000000000000000000, -0.000000000000000000 ) ) ;
#2260=CARTESIAN_POINT ( 'NONE',  ( -141.4692556286852891, -195.0630981290893260, 49.65701158161630957 ) ) ;
#2262=CARTESIAN_POINT ( 'NONE',  ( -148.3790856849358306, -174.6630981290893203, 59.16757674456786020 ) ) ;
#2263=DIRECTION ( 'NONE',  ( 0.000000000000000000, 0.000000000000000000, -1.000000000000000000 ) ) ;
#2264=CARTESIAN_POINT ( 'NONE',  ( -157.6495955161842062, -157.1130981290892521, 58.16351966513671812 ) ) ;
#2266=CARTESIAN_POINT ( 'NONE',  ( -159.5594255724347761, -191.1891397928654897, 55.53486410454104316 ) ) ;
#2270=CARTESIAN_POINT ( 'NONE',  ( -159.0959885057557983, -191.1938272943107222, 44.11586579668791330 ) ) ;
#2272=VERTEX_POINT ( 'NONE', #15262 ) ;
#2285=CARTESIAN_POINT ( 'NONE',  ( -160.8964159109769696, -178.8938272943107393, 49.65701158161630957 ) ) ;
#2287=CARTESIAN_POINT ( 'NONE',  ( -151.4692556286852891, -192.8130981290892692, 60.17163382399899518 ) ) ;
#2295=CARTESIAN_POINT ( 'NONE',  ( -160.8964159109769696, -161.0084106276440252, 52.72008163687743121 ) ) ;
#2299=AXIS2_PLACEMENT_3D ( 'NONE', #9906, #6482, #19938 ) ;
#2302=ORIENTED_EDGE ( 'NONE', *, *, #15475, .F. ) ;
#2306=( BOUNDED_SURFACE ( )  B_SPLINE_SURFACE ( 1, 2, ( 
 ( #10356, #10250, #320, #16949, #8594, #15313, #3738, #205, #20384, #17059, #1971, #7049, #10468, #13755, #17168, #2287, #9026, #17812, #21141, #17382, #4267, #14404, #7806, #9348, #19476, #10785, #7377, #10995, #15738, #19156, #19052, #17492, #10678, #17705, #14078, #16164, #5920, #2723, #9464, #2610, #5706, #2505, #1076, #3952, #12648, #749, #14512, #5591, #17599, #6025, #7705, #7484, #19370, #12316, #11099, #14186, #9246, #12756, #20925, #643, #12430, #16052, #2402, #20816, #4057, #5807, #15946, #4368, #12538, #9138, #15838, #962, #19267, #4167, #10896, #856, #7593, #14292, #21037, #1401, #4477, #21356, #6469, #16595, #1513, #10006, #8129, #18372, #2829, #1180, #6589, #14732, #16378, #9790, #21578, #8242, #3274, #6133, #14944, #21691, #11308, #12862, #7915, #14618, #13308, #18262, #14833, #12974, #11205, #21253, #16710, #1619, #19700, #20045, #3165, #4931, #11535, #8351, #9569, #11643, #19583, #17920, #9895, #19923, #6246, #13082, #16275, #19811, #4588, #18035, #2940, #9679, #4700, #11418, #1291, #8026, #13191, #21467, #18143, #6358, #16485, #3052, #4812, #2162, #296, #5042, #405, #7135, #12077, #2057, #8677, #8788, #10547, #11751, #18483, #5461, #15503, #3387, #13731, #13839, #17248, #18808, #20575, #20254, #16820, #20468, #10113, #6815, #6708, #11865, #20149, #5361, #1732, #3819, #15400, #12183, #18918, #3711, #15175, #11974, #15062, #13415, #7027, #10225, #21799, #8467, #5256, #77, #17143, #16927, #10443, #13521, #18596, #3609, #3501, #1842, #8573, #15288, #181, #6916, #13622, #20360, #18703, #10332, #17035, #1946, #2480, #615, #20683, #8899, #12729, #19453, #7351, #4243, #12622, #10969, #21010, #4344, #12290, #17681, #11072, #5568, #19343, #7566, #9000, #726, #2584, #7456, #9324, #16024, #936, #7681, #14163, #20896, #3926, #19135, #9221, #17359, #5783, #14378, #19240, #19028, #7243, #17786, #15919, #10657, #21117, #5999, #5892, #15600, #832, #506, #13945, #2264, #15710, #14056, #20788, #5679, #14264, #12403, #4033, #10759, #17465, #2376, #9113, #15813, #12514, #4140, #10871 ),
 ( #17573, #2807, #21443, #13284, #1049, #3028, #19672, #11622, #6561, #14707, #18238, #4786, #4566, #9764, #20019, #8219, #11287, #6333, #11507, #18007, #16140, #9545, #16461, #14592, #14919, #7783, #1374, #2919, #4678, #13059, #11394, #14483, #16247, #8105, #19900, #3139, #4904, #18117, #21669, #6108, #4451, #9870, #9653, #16354, #1264, #2694, #16569, #9438, #1488, #19785, #21227, #6219, #8000, #14811, #7890, #21554, #11181, #21333, #6445, #12837, #19555, #17894, #12951, #13167, #1156, #3878, #2005, #14004, #458, #10498, #3660, #7189, #5412, #17415, #3987, #12351, #13894, #5313, #10820, #20632, #20738, #12024, #10603, #20525, #10712, #15555, #19087, #20416, #10391, #5627, #15769, #8949, #19192, #2320, #9059, #17091, #7303, #8737, #673, #2432, #18761, #15346, #15455, #355, #12461, #2111, #7083, #7409, #5514, #13682, #239, #12246, #2219, #17198, #12130, #14109, #17522, #13786, #20847, #18863, #5738, #3770, #4089, #18975, #6979, #8848, #17307, #15656, #558, #12899, #21286, #9384, #14218, #19299, #12789, #19620, #2642, #16089, #2757, #9498, #7627, #11344, #16304, #16195, #11237, #19508, #782, #2539, #14329, #9605, #4514, #4401, #1214, #10925, #9171, #21070, #19401, #7948, #4297, #17631, #20958, #14544, #6062, #17957, #21393, #1107, #17847, #2862, #7517, #15869, #14653, #11024, #5842, #12572, #6279, #13011, #4197, #7842, #19732, #18067, #4625, #9276, #5951, #15977, #6165, #888, #12679, #17736, #999, #7736, #14437, #21171, #11132, #3311, #111, #15212, #21818, #3088, #21723, #13549, #1323, #10041, #19964, #11899, #6843, #14978, #18519, #5074, #4849, #16745, #20286, #8499, #11569, #6627, #11788, #18298, #16413, #9821, #1655, #14871, #5180, #8056, #8387, #3200, #11677, #13341, #18411, #14762, #16519, #15096, #20183, #3428, #2974, #6741, #9712, #6392, #4733, #10149, #9930, #16635, #20078, #13449, #16850, #21505, #13120, #1765, #19842, #21616, #11452, #18181, #1435, #8165, #6507, #13227, #1546, #8277, #18627, #650, #7386, #10365, #13977, #536, #20715, #8926, #14086, #215, #5599, #20822, #8601 ) ),
 .UNSPECIFIED., .F., .F., .F. ) 
 B_SPLINE_SURFACE_WITH_KNOTS ( ( 2, 2 ),
 ( 3, 2, 2, 2, 2, 2, 2, 2, 2, 2, 2, 2, 2, 2, 2, 2, 2, 2, 2, 2, 2, 2, 2, 2, 2, 2, 2, 2, 2, 2, 2, 2, 2, 2, 2, 2, 2, 2, 2, 2, 2, 2, 2, 2, 2, 2, 2, 2, 2, 2, 2, 2, 2, 2, 2, 2, 2, 2, 2, 2, 2, 2, 2, 2, 2, 2, 2, 2, 2, 2, 2, 2, 2, 2, 2, 2, 2, 2, 2, 2, 2, 2, 2, 2, 2, 2, 2, 2, 2, 2, 2, 2, 2, 2, 2, 2, 2, 2, 2, 2, 2, 2, 2, 2, 2, 2, 2, 2, 2, 2, 2, 2, 2, 2, 2, 2, 2, 2, 2, 2, 2, 2, 2, 2, 2, 2, 2, 2, 2, 2, 2, 2, 2, 2, 3 ),
 ( 0.000000000000000000, 1.000000000000000000 ),
 ( 0.000000000000000000, 0.007142857142857142634, 0.01428571428571428527, 0.02142857142857142877, 0.02857142857142857054, 0.03571428571428571230, 0.04285714285714285754, 0.05000000000000000278, 0.05714285714285714107, 0.06428571428571427937, 0.07142857142857142461, 0.07857142857142856984, 0.08571428571428571508, 0.09285714285714286031, 0.1000000000000000056, 0.1071428571428571369, 0.1142857142857142821, 0.1214285714285714274, 0.1285714285714285587, 0.1357142857142857040, 0.1428571428571428492, 0.1499999999999999944, 0.1571428571428571397, 0.1642857142857142849, 0.1714285714285714302, 0.1785714285714285754, 0.1857142857142857206, 0.1928571428571428659, 0.2000000000000000111, 0.2071428571428571563, 0.2142857142857142738, 0.2214285714285714191, 0.2285714285714285643, 0.2357142857142857095, 0.2428571428571428548, 0.2500000000000000000, 0.2571428571428571175, 0.2642857142857142905, 0.2714285714285714080, 0.2785714285714285809, 0.2857142857142856984, 0.2928571428571428714, 0.2999999999999999889, 0.3071428571428571619, 0.3142857142857142794, 0.3214285714285714524, 0.3285714285714285698, 0.3357142857142856873, 0.3428571428571428603, 0.3499999999999999778, 0.3571428571428571508, 0.3642857142857142683, 0.3714285714285714413, 0.3785714285714285587, 0.3857142857142857317, 0.3928571428571428492, 0.4000000000000000222, 0.4071428571428571397, 0.4142857142857143127, 0.4214285714285714302, 0.4285714285714285476, 0.4357142857142857206, 0.4428571428571428381, 0.4500000000000000111, 0.4571428571428571286, 0.4642857142857143016, 0.4714285714285714191, 0.4785714285714285920, 0.4857142857142857095, 0.4928571428571428825, 0.5000000000000000000, 0.5071428571428571175, 0.5142857142857142350, 0.5214285714285714635, 0.5285714285714285809, 0.5357142857142856984, 0.5428571428571428159, 0.5500000000000000444, 0.5571428571428571619, 0.5642857142857142794, 0.5714285714285713969, 0.5785714285714286254, 0.5857142857142857428, 0.5928571428571428603, 0.5999999999999999778, 0.6071428571428570953, 0.6142857142857143238, 0.6214285714285714413, 0.6285714285714285587, 0.6357142857142856762, 0.6428571428571429047, 0.6500000000000000222, 0.6571428571428571397, 0.6642857142857142572, 0.6714285714285713746, 0.6785714285714286031, 0.6857142857142857206, 0.6928571428571428381, 0.6999999999999999556, 0.7071428571428571841, 0.7142857142857143016, 0.7214285714285714191, 0.7285714285714285365, 0.7357142857142857650, 0.7428571428571428825, 0.7500000000000000000, 0.7571428571428571175, 0.7642857142857142350, 0.7714285714285714635, 0.7785714285714285809, 0.7857142857142856984, 0.7928571428571428159, 0.8000000000000000444, 0.8071428571428571619, 0.8142857142857142794, 0.8214285714285713969, 0.8285714285714286254, 0.8357142857142857428, 0.8428571428571428603, 0.8499999999999999778, 0.8571428571428570953, 0.8642857142857143238, 0.8714285714285714413, 0.8785714285714285587, 0.8857142857142856762, 0.8928571428571429047, 0.9000000000000000222, 0.9071428571428571397, 0.9142857142857142572, 0.9214285714285713746, 0.9285714285714286031, 0.9357142857142857206, 0.9428571428571428381, 0.9499999999999999556, 0.9523897199067097308 ),
 .UNSPECIFIED. ) 
 GEOMETRIC_REPRESENTATION_ITEM ( )  RATIONAL_B_SPLINE_SURFACE ( (
 ( 1.000000000000000000, 0.9510565162951535312, 1.000000000000000000, 0.9510565162951535312, 1.000000000000000000, 0.9510565162951535312, 1.000000000000000000, 0.9510565162951535312, 1.000000000000000000, 0.9510565162951535312, 1.000000000000000000, 0.9510565162951535312, 1.000000000000000000, 0.9510565162951535312, 1.000000000000000000, 0.9510565162951535312, 1.000000000000000000, 0.9510565162951535312, 1.000000000000000000, 0.9510565162951535312, 1.000000000000000000, 0.9510565162951535312, 1.000000000000000000, 0.9510565162951535312, 1.000000000000000000, 0.9510565162951535312, 1.000000000000000000, 0.9510565162951535312, 1.000000000000000000, 0.9510565162951535312, 1.000000000000000000, 0.9510565162951535312, 1.000000000000000000, 0.9510565162951535312, 1.000000000000000000, 0.9510565162951535312, 1.000000000000000000, 0.9510565162951535312, 1.000000000000000000, 0.9510565162951535312, 1.000000000000000000, 0.9510565162951535312, 1.000000000000000000, 0.9510565162951535312, 1.000000000000000000, 0.9510565162951535312, 1.000000000000000000, 0.9510565162951535312, 1.000000000000000000, 0.9510565162951535312, 1.000000000000000000, 0.9510565162951535312, 1.000000000000000000, 0.9510565162951535312, 1.000000000000000000, 0.9510565162951535312, 1.000000000000000000, 0.9510565162951535312, 1.000000000000000000, 0.9510565162951535312, 1.000000000000000000, 0.9510565162951535312, 1.000000000000000000, 0.9510565162951535312, 1.000000000000000000, 0.9510565162951535312, 1.000000000000000000, 0.9510565162951535312, 1.000000000000000000, 0.9510565162951535312, 1.000000000000000000, 0.9510565162951535312, 1.000000000000000000, 0.9510565162951535312, 1.000000000000000000, 0.9510565162951535312, 1.000000000000000000, 0.9510565162951535312, 1.000000000000000000, 0.9510565162951535312, 1.000000000000000000, 0.9510565162951535312, 1.000000000000000000, 0.9510565162951535312, 1.000000000000000000, 0.9510565162951535312, 1.000000000000000000, 0.9510565162951535312, 1.000000000000000000, 0.9510565162951535312, 1.000000000000000000, 0.9510565162951535312, 1.000000000000000000, 0.9510565162951535312, 1.000000000000000000, 0.9510565162951535312, 1.000000000000000000, 0.9510565162951535312, 1.000000000000000000, 0.9510565162951535312, 1.000000000000000000, 0.9510565162951535312, 1.000000000000000000, 0.9510565162951535312, 1.000000000000000000, 0.9510565162951535312, 1.000000000000000000, 0.9510565162951535312, 1.000000000000000000, 0.9510565162951535312, 1.000000000000000000, 0.9510565162951535312, 1.000000000000000000, 0.9510565162951535312, 1.000000000000000000, 0.9510565162951535312, 1.000000000000000000, 0.9510565162951535312, 1.000000000000000000, 0.9510565162951535312, 1.000000000000000000, 0.9510565162951535312, 1.000000000000000000, 0.9510565162951535312, 1.000000000000000000, 0.9510565162951535312, 1.000000000000000000, 0.9510565162951535312, 1.000000000000000000, 0.9510565162951535312, 1.000000000000000000, 0.9510565162951535312, 1.000000000000000000, 0.9510565162951535312, 1.000000000000000000, 0.9510565162951535312, 1.000000000000000000, 0.9510565162951535312, 1.000000000000000000, 0.9510565162951535312, 1.000000000000000000, 0.9510565162951535312, 1.000000000000000000, 0.9510565162951535312, 1.000000000000000000, 0.9510565162951535312, 1.000000000000000000, 0.9510565162951535312, 1.000000000000000000, 0.9510565162951535312, 1.000000000000000000, 0.9510565162951535312, 1.000000000000000000, 0.9510565162951535312, 1.000000000000000000, 0.9510565162951535312, 1.000000000000000000, 0.9510565162951535312, 1.000000000000000000, 0.9510565162951535312, 1.000000000000000000, 0.9510565162951535312, 1.000000000000000000, 0.9510565162951535312, 1.000000000000000000, 0.9510565162951535312, 1.000000000000000000, 0.9510565162951535312, 1.000000000000000000, 0.9510565162951535312, 1.000000000000000000, 0.9510565162951535312, 1.000000000000000000, 0.9510565162951535312, 1.000000000000000000, 0.9510565162951535312, 1.000000000000000000, 0.9510565162951535312, 1.000000000000000000, 0.9510565162951535312, 1.000000000000000000, 0.9510565162951535312, 1.000000000000000000, 0.9510565162951535312, 1.000000000000000000, 0.9510565162951535312, 1.000000000000000000, 0.9510565162951535312, 1.000000000000000000, 0.9510565162951535312, 1.000000000000000000, 0.9510565162951535312, 1.000000000000000000, 0.9510565162951535312, 1.000000000000000000, 0.9510565162951535312, 1.000000000000000000, 0.9510565162951535312, 1.000000000000000000, 0.9510565162951535312, 1.000000000000000000, 0.9510565162951535312, 1.000000000000000000, 0.9510565162951535312, 1.000000000000000000, 0.9510565162951535312, 1.000000000000000000, 0.9510565162951535312, 1.000000000000000000, 0.9510565162951535312, 1.000000000000000000, 0.9510565162951535312, 1.000000000000000000, 0.9510565162951535312, 1.000000000000000000, 0.9510565162951535312, 1.000000000000000000, 0.9510565162951535312, 1.000000000000000000, 0.9510565162951535312, 1.000000000000000000, 0.9510565162951535312, 1.000000000000000000, 0.9510565162951535312, 1.000000000000000000, 0.9510565162951535312, 1.000000000000000000, 0.9510565162951535312, 1.000000000000000000, 0.9510565162951535312, 1.000000000000000000, 0.9510565162951535312, 1.000000000000000000, 0.9510565162951535312, 1.000000000000000000, 0.9510565162951535312, 1.000000000000000000, 0.9510565162951535312, 1.000000000000000000, 0.9510565162951535312, 1.000000000000000000, 0.9510565162951535312, 1.000000000000000000, 0.9510565162951535312, 1.000000000000000000, 0.9510565162951535312, 1.000000000000000000, 0.9510565162951535312, 1.000000000000000000, 0.9510565162951535312, 1.000000000000000000, 0.9510565162951535312, 1.000000000000000000, 0.9510565162951535312, 1.000000000000000000, 0.9510565162951535312, 1.000000000000000000, 0.9510565162951535312, 1.000000000000000000, 0.9510565162951535312, 1.000000000000000000, 0.9510565162951535312, 1.000000000000000000, 0.9510565162951535312, 1.000000000000000000, 0.9510565162951535312, 1.000000000000000000, 0.9836254295761526212, 0.9782074374858980015),
 ( 1.000000000000000000, 0.9510565162951535312, 1.000000000000000000, 0.9510565162951535312, 1.000000000000000000, 0.9510565162951535312, 1.000000000000000000, 0.9510565162951535312, 1.000000000000000000, 0.9510565162951535312, 1.000000000000000000, 0.9510565162951535312, 1.000000000000000000, 0.9510565162951535312, 1.000000000000000000, 0.9510565162951535312, 1.000000000000000000, 0.9510565162951535312, 1.000000000000000000, 0.9510565162951535312, 1.000000000000000000, 0.9510565162951535312, 1.000000000000000000, 0.9510565162951535312, 1.000000000000000000, 0.9510565162951535312, 1.000000000000000000, 0.9510565162951535312, 1.000000000000000000, 0.9510565162951535312, 1.000000000000000000, 0.9510565162951535312, 1.000000000000000000, 0.9510565162951535312, 1.000000000000000000, 0.9510565162951535312, 1.000000000000000000, 0.9510565162951535312, 1.000000000000000000, 0.9510565162951535312, 1.000000000000000000, 0.9510565162951535312, 1.000000000000000000, 0.9510565162951535312, 1.000000000000000000, 0.9510565162951535312, 1.000000000000000000, 0.9510565162951535312, 1.000000000000000000, 0.9510565162951535312, 1.000000000000000000, 0.9510565162951535312, 1.000000000000000000, 0.9510565162951535312, 1.000000000000000000, 0.9510565162951535312, 1.000000000000000000, 0.9510565162951535312, 1.000000000000000000, 0.9510565162951535312, 1.000000000000000000, 0.9510565162951535312, 1.000000000000000000, 0.9510565162951535312, 1.000000000000000000, 0.9510565162951535312, 1.000000000000000000, 0.9510565162951535312, 1.000000000000000000, 0.9510565162951535312, 1.000000000000000000, 0.9510565162951535312, 1.000000000000000000, 0.9510565162951535312, 1.000000000000000000, 0.9510565162951535312, 1.000000000000000000, 0.9510565162951535312, 1.000000000000000000, 0.9510565162951535312, 1.000000000000000000, 0.9510565162951535312, 1.000000000000000000, 0.9510565162951535312, 1.000000000000000000, 0.9510565162951535312, 1.000000000000000000, 0.9510565162951535312, 1.000000000000000000, 0.9510565162951535312, 1.000000000000000000, 0.9510565162951535312, 1.000000000000000000, 0.9510565162951535312, 1.000000000000000000, 0.9510565162951535312, 1.000000000000000000, 0.9510565162951535312, 1.000000000000000000, 0.9510565162951535312, 1.000000000000000000, 0.9510565162951535312, 1.000000000000000000, 0.9510565162951535312, 1.000000000000000000, 0.9510565162951535312, 1.000000000000000000, 0.9510565162951535312, 1.000000000000000000, 0.9510565162951535312, 1.000000000000000000, 0.9510565162951535312, 1.000000000000000000, 0.9510565162951535312, 1.000000000000000000, 0.9510565162951535312, 1.000000000000000000, 0.9510565162951535312, 1.000000000000000000, 0.9510565162951535312, 1.000000000000000000, 0.9510565162951535312, 1.000000000000000000, 0.9510565162951535312, 1.000000000000000000, 0.9510565162951535312, 1.000000000000000000, 0.9510565162951535312, 1.000000000000000000, 0.9510565162951535312, 1.000000000000000000, 0.9510565162951535312, 1.000000000000000000, 0.9510565162951535312, 1.000000000000000000, 0.9510565162951535312, 1.000000000000000000, 0.9510565162951535312, 1.000000000000000000, 0.9510565162951535312, 1.000000000000000000, 0.9510565162951535312, 1.000000000000000000, 0.9510565162951535312, 1.000000000000000000, 0.9510565162951535312, 1.000000000000000000, 0.9510565162951535312, 1.000000000000000000, 0.9510565162951535312, 1.000000000000000000, 0.9510565162951535312, 1.000000000000000000, 0.9510565162951535312, 1.000000000000000000, 0.9510565162951535312, 1.000000000000000000, 0.9510565162951535312, 1.000000000000000000, 0.9510565162951535312, 1.000000000000000000, 0.9510565162951535312, 1.000000000000000000, 0.9510565162951535312, 1.000000000000000000, 0.9510565162951535312, 1.000000000000000000, 0.9510565162951535312, 1.000000000000000000, 0.9510565162951535312, 1.000000000000000000, 0.9510565162951535312, 1.000000000000000000, 0.9510565162951535312, 1.000000000000000000, 0.9510565162951535312, 1.000000000000000000, 0.9510565162951535312, 1.000000000000000000, 0.9510565162951535312, 1.000000000000000000, 0.9510565162951535312, 1.000000000000000000, 0.9510565162951535312, 1.000000000000000000, 0.9510565162951535312, 1.000000000000000000, 0.9510565162951535312, 1.000000000000000000, 0.9510565162951535312, 1.000000000000000000, 0.9510565162951535312, 1.000000000000000000, 0.9510565162951535312, 1.000000000000000000, 0.9510565162951535312, 1.000000000000000000, 0.9510565162951535312, 1.000000000000000000, 0.9510565162951535312, 1.000000000000000000, 0.9510565162951535312, 1.000000000000000000, 0.9510565162951535312, 1.000000000000000000, 0.9510565162951535312, 1.000000000000000000, 0.9510565162951535312, 1.000000000000000000, 0.9510565162951535312, 1.000000000000000000, 0.9510565162951535312, 1.000000000000000000, 0.9510565162951535312, 1.000000000000000000, 0.9510565162951535312, 1.000000000000000000, 0.9510565162951535312, 1.000000000000000000, 0.9510565162951535312, 1.000000000000000000, 0.9510565162951535312, 1.000000000000000000, 0.9510565162951535312, 1.000000000000000000, 0.9510565162951535312, 1.000000000000000000, 0.9510565162951535312, 1.000000000000000000, 0.9510565162951535312, 1.000000000000000000, 0.9510565162951535312, 1.000000000000000000, 0.9510565162951535312, 1.000000000000000000, 0.9510565162951535312, 1.000000000000000000, 0.9510565162951535312, 1.000000000000000000, 0.9510565162951535312, 1.000000000000000000, 0.9510565162951535312, 1.000000000000000000, 0.9510565162951535312, 1.000000000000000000, 0.9510565162951535312, 1.000000000000000000, 0.9510565162951535312, 1.000000000000000000, 0.9510565162951535312, 1.000000000000000000, 0.9510565162951535312, 1.000000000000000000, 0.9510565162951535312, 1.000000000000000000, 0.9510565162951535312, 1.000000000000000000, 0.9510565162951535312, 1.000000000000000000, 0.9510565162951535312, 1.000000000000000000, 0.9510565162951535312, 1.000000000000000000, 0.9510565162951535312, 1.000000000000000000, 0.9510565162951535312, 1.000000000000000000, 0.9836254295761526212, 0.9782074374858980015) ) ) 
 REPRESENTATION_ITEM ( '' )  SURFACE ( )  );
#2315=FILL_AREA_STYLE ('',( #9166 ) ) ;
#2317=CARTESIAN_POINT ( 'NONE',  ( -151.4692556286852607, -171.8130981290892976, 59.65701158161632378 ) ) ;
#2320=CARTESIAN_POINT ( 'NONE',  ( -157.2955611005346270, -181.4438272943107506, 57.67623309621198047 ) ) ;
#2321=CARTESIAN_POINT ( 'NONE',  ( -148.5561028927606344, -190.2584106276440536, 58.62277379824867296 ) ) ;
#2323=ORIENTED_EDGE ( 'NONE', *, *, #20650, .F. ) ;
#2324=CARTESIAN_POINT ( 'NONE',  ( -154.3824083646099439, -175.5584106276440366, 58.62277379824867296 ) ) ;
#2332=VECTOR ( 'NONE', #19954, 1000.000000000000000 ) ;
#2342=CARTESIAN_POINT ( 'NONE',  ( -149.8854112254399240, -179.3899795514095672, 39.65701158161629536 ) ) ;
#2343=CARTESIAN_POINT ( 'NONE',  ( -148.3790856849358306, -169.5891397928654669, 59.16757674456786020 ) ) ;
#2348=ADVANCED_FACE ( 'NONE', ( #131 ), #10058, .T. ) ;
#2352=CARTESIAN_POINT ( 'NONE',  ( -145.6429501568359797, -165.8438272943107563, 57.67623309621198047 ) ) ;
#2355=CARTESIAN_POINT ( 'NONE',  ( -142.0420953463936087, -195.6584106276440593, 49.65701158161630957 ) ) ;
#2369=LINE ( 'NONE', #10754, #11322 ) ;
#2371=( BOUNDED_CURVE ( )  B_SPLINE_CURVE ( 2, ( #4987, #8520, #16872, #16656, #15233, #1457, #5203, #14784, #11697, #132, #8296, #6416, #21638 ),
 .UNSPECIFIED., .F., .F. ) 
 B_SPLINE_CURVE_WITH_KNOTS ( ( 3, 2, 2, 2, 2, 2, 3 ),
 ( 0.5535714285714286031, 0.5571428571428571619, 0.5642857142857142794, 0.5714285714285713969, 0.5785714285714286254, 0.5857142857142857428, 0.5892857142857143016 ),
 .UNSPECIFIED. ) 
 CURVE ( )  GEOMETRIC_REPRESENTATION_ITEM ( )  RATIONAL_B_SPLINE_CURVE ( ( 0.9755282581475768211, 0.9755282581475768211, 1.000000000000000000, 0.9510565162951535312, 1.000000000000000000, 0.9510565162951535312, 1.000000000000000000, 0.9510565162951535312, 1.000000000000000000, 0.9510565162951535312, 1.000000000000000000, 0.9755282581475768211, 0.9755282581475768211 ) ) 
 REPRESENTATION_ITEM ( '' )  );
#2376=CARTESIAN_POINT ( 'NONE',  ( -145.2889157411863721, -155.6130981290893089, 41.15050349809590102 ) ) ;
#2382=CARTESIAN_POINT ( 'NONE',  ( -159.0959885057557983, -194.1938272943107222, 44.11586579668791330 ) ) ;
#2385=CARTESIAN_POINT ( 'NONE',  ( -149.8854112254399809, -162.7362167067690564, 59.65701158161633089 ) ) ;
#2395=CARTESIAN_POINT ( 'NONE',  ( -141.4692556286852891, -165.0630981290893260, 49.65701158161630957 ) ) ;
#2400=CARTESIAN_POINT ( 'NONE',  ( -159.0959885057557983, -169.5938272943107279, 55.19815736654470584 ) ) ;
#2402=CARTESIAN_POINT ( 'NONE',  ( -143.3790856849358306, -185.7630981290893146, 43.77915905869157598 ) ) ;
#2403=CARTESIAN_POINT ( 'NONE',  ( 0.000000000000000000, 0.000000000000000000, 0.000000000000000000 ) ) ;
#2409=CARTESIAN_POINT ( 'NONE',  ( -148.5561028927606344, -168.0584106276440366, 40.69124936498395328 ) ) ;
#2429=CARTESIAN_POINT ( 'NONE',  ( -154.5594255724347761, -189.9630981290893317, 59.16757674456785310 ) ) ;
#2432=CARTESIAN_POINT ( 'NONE',  ( -142.0420953463935803, -180.5438272943106881, 52.72008163687743831 ) ) ;
#2439=VERTEX_POINT ( 'NONE', #16766 ) ;
#2442=ADVANCED_FACE ( 'NONE', ( #15116 ), #3447, .T. ) ;
#2450=CARTESIAN_POINT ( 'NONE',  ( -143.3790856849358306, -180.3630981290893089, 55.53486410454105027 ) ) ;
#2451=CARTESIAN_POINT ( 'NONE',  ( -154.5594255724347761, -159.0891397928654953, 40.14644641866476604 ) ) ;
#2458=CARTESIAN_POINT ( 'NONE',  ( -148.5561028927606344, -167.7938272943107165, 40.69124936498395328 ) ) ;
#2460=CARTESIAN_POINT ( 'NONE',  ( -151.4692556286852891, -191.9084106276440025, 39.74470866294723947 ) ) ;
#2462=CARTESIAN_POINT ( 'NONE',  ( -161.4692556286853176, -175.5630981290893260, 49.65701158161630957 ) ) ;
#2473=ADVANCED_FACE ( 'NONE', ( #13359 ), #13030, .F. ) ;
#2480=CARTESIAN_POINT ( 'NONE',  ( -154.5594255724347761, -164.1630981290892919, 40.14644641866476604 ) ) ;
#2485=CARTESIAN_POINT ( 'NONE',  ( -148.5561028927606344, -191.7938272943107449, 40.69124936498395328 ) ) ;
#2495=ORIENTED_EDGE ( 'NONE', *, *, #12654, .T. ) ;
#2498=( BOUNDED_CURVE ( )  B_SPLINE_CURVE ( 2, ( #10653, #15499, #401, #5778, #5456, #9217, #15915, #4135, #7239, #825, #18912, #10544, #17244 ),
 .UNSPECIFIED., .F., .F. ) 
 B_SPLINE_CURVE_WITH_KNOTS ( ( 3, 2, 2, 2, 2, 2, 3 ),
 ( 0.05357142857142858927, 0.05714285714285714107, 0.06428571428571427937, 0.07142857142857142461, 0.07857142857142856984, 0.08571428571428571508, 0.08928571428571425994 ),
 .UNSPECIFIED. ) 
 CURVE ( )  GEOMETRIC_REPRESENTATION_ITEM ( )  RATIONAL_B_SPLINE_CURVE ( ( 0.9755282581475767101, 0.9755282581475768211, 1.000000000000000000, 0.9510565162951535312, 1.000000000000000000, 0.9510565162951535312, 1.000000000000000000, 0.9510565162951535312, 1.000000000000000000, 0.9510565162951535312, 1.000000000000000000, 0.9755282581475769321, 0.9755282581475768211 ) ) 
 REPRESENTATION_ITEM ( '' )  );
#2503=CARTESIAN_POINT ( 'NONE',  ( -142.0420953463936087, -174.3938272943107393, 49.65701158161630957 ) ) ;
#2505=CARTESIAN_POINT ( 'NONE',  ( -141.4692556286852891, -188.9130981290893487, 46.40781461928724383 ) ) ;
#2508=CARTESIAN_POINT ( 'NONE',  ( -145.2889157411863437, -162.5391397928654271, 41.15050349809589392 ) ) ;
#2513=CARTESIAN_POINT ( 'NONE',  ( -148.5561028927606344, -165.0584106276440366, 40.69124936498395328 ) ) ;
#2521=CARTESIAN_POINT ( 'NONE',  ( -143.3790856849358306, -157.2891397928654555, 55.53486410454105027 ) ) ;
#2525=VECTOR ( 'NONE', #1351, 1000.000000000000000 ) ;
#2534=SURFACE_SIDE_STYLE ('',( #15865 ) ) ;
#2535=CARTESIAN_POINT ( 'NONE',  ( -166.4803626276155626, -116.9891397928655010, 49.65701158161629536 ) ) ;
#2539=CARTESIAN_POINT ( 'NONE',  ( -157.2955611005346270, -173.3438272943107279, 41.63779006702063867 ) ) ;
#2540=CARTESIAN_POINT ( 'NONE',  ( -159.0959885057557983, -191.4584106276440423, 44.11586579668791330 ) ) ;
#2542=CARTESIAN_POINT ( 'NONE',  ( -142.0420953463936087, -177.6584106276440309, 49.65701158161630957 ) ) ;
#2548=VERTEX_POINT ( 'NONE', #16654 ) ;
#2551=ORIENTED_EDGE ( 'NONE', *, *, #8145, .T. ) ;
#2559=CARTESIAN_POINT ( 'NONE',  ( -141.4692556286852891, -156.9891397928654726, 49.65701158161630957 ) ) ;
#2566=CARTESIAN_POINT ( 'NONE',  ( -157.2955611005346270, -161.3438272943107563, 41.63779006702063867 ) ) ;
#2572=ORIENTED_EDGE ( 'NONE', *, *, #9917, .F. ) ;
#2581=CARTESIAN_POINT ( 'NONE',  ( -141.4692556286852891, -189.9891397928654726, 49.65701158161630957 ) ) ;
#2584=CARTESIAN_POINT ( 'NONE',  ( -154.5594255724347761, -161.1630981290892919, 40.14644641866476604 ) ) ;
#2589=CARTESIAN_POINT ( 'NONE',  ( -157.2955611005346270, -188.3438272943107279, 41.63779006702063867 ) ) ;
#2608=CARTESIAN_POINT ( 'NONE',  ( -148.5561028927606344, -170.7938272943107165, 40.69124936498395328 ) ) ;
#2610=CARTESIAN_POINT ( 'NONE',  ( -141.4692556286852891, -189.2130981290893317, 52.90620854394536821 ) ) ;
#2617=CARTESIAN_POINT ( 'NONE',  ( -142.0420953463935803, -156.5084106276439968, 46.59394152635518083 ) ) ;
#2636=CARTESIAN_POINT ( 'NONE',  ( -161.4692556286852891, -187.4130981290893203, 52.90620854394536821 ) ) ;
#2642=CARTESIAN_POINT ( 'NONE',  ( -148.5561028927606344, -174.9938272943107336, 58.62277379824867296 ) ) ;
#2643=CARTESIAN_POINT ( 'NONE',  ( -160.8964159109769696, -185.3084106276440366, 46.59394152635518083 ) ) ;
#2645=CARTESIAN_POINT ( 'NONE',  ( -145.6429501568359797, -169.1084106276440480, 57.67623309621198047 ) ) ;
#2661=CARTESIAN_POINT ( 'NONE',  ( -161.4692556286852607, -164.3391397928654385, 52.90620854394536821 ) ) ;
#2662=CARTESIAN_POINT ( 'NONE',  ( -149.8854112254399240, -158.3899795514095672, 39.65701158161629536 ) ) ;
#2669=CARTESIAN_POINT ( 'NONE',  ( -142.0420953463936087, -165.3938272943107393, 49.65701158161630957 ) ) ;
#2690=CARTESIAN_POINT ( 'NONE',  ( -143.3790856849358306, -190.2891397928654555, 55.53486410454105027 ) ) ;
#2691=( BOUNDED_CURVE ( )  B_SPLINE_CURVE ( 2, ( #13190, #4587, #14832, #4811, #12973, #19699, #18261, #6588, #13307, #11307, #3164, #18034, #9678 ),
 .UNSPECIFIED., .F., .F. ) 
 B_SPLINE_CURVE_WITH_KNOTS ( ( 3, 2, 2, 2, 2, 2, 3 ),
 ( 0.6964285714285713969, 0.6999999999999999556, 0.7071428571428571841, 0.7142857142857143016, 0.7214285714285714191, 0.7285714285714285365, 0.7321428571428572063 ),
 .UNSPECIFIED. ) 
 CURVE ( )  GEOMETRIC_REPRESENTATION_ITEM ( )  RATIONAL_B_SPLINE_CURVE ( ( 0.9755282581475768211, 0.9755282581475768211, 1.000000000000000000, 0.9510565162951535312, 1.000000000000000000, 0.9510565162951535312, 1.000000000000000000, 0.9510565162951535312, 1.000000000000000000, 0.9510565162951535312, 1.000000000000000000, 0.9755282581475763770, 0.9755282581475768211 ) ) 
 REPRESENTATION_ITEM ( '' )  );
#2694=CARTESIAN_POINT ( 'NONE',  ( -151.4692556286852891, -188.6438272943107393, 39.74470866294723947 ) ) ;
#2699=CARTESIAN_POINT ( 'NONE',  ( -151.4692556286852891, -191.6438272943107108, 39.74470866294723947 ) ) ;
#2714=CARTESIAN_POINT ( 'NONE',  ( -151.4692556286852891, -196.9891397928655010, 49.65701158161630957 ) ) ;
#2720=CARTESIAN_POINT ( 'NONE',  ( -142.0420953463936087, -171.3938272943107393, 49.65701158161630957 ) ) ;
#2723=CARTESIAN_POINT ( 'NONE',  ( -145.2889157411863721, -189.5130981290893146, 58.16351966513671812 ) ) ;
#2757=CARTESIAN_POINT ( 'NONE',  ( -143.8425227516148084, -174.6938272943107506, 55.19815736654470584 ) ) ;
#2758=CARTESIAN_POINT ( 'NONE',  ( -160.8964159109769696, -188.3084106276440650, 46.59394152635518083 ) ) ;
#2762=CARTESIAN_POINT ( 'NONE',  ( -145.6429501568359797, -174.2084106276440423, 41.63779006702063867 ) ) ;
#2767=EDGE_CURVE ( 'NONE', #6804, #8, #21056, .T. ) ;
#2780=CARTESIAN_POINT ( 'NONE',  ( -161.4692556286852607, -161.3391397928654669, 52.90620854394536821 ) ) ;
#2784=CARTESIAN_POINT ( 'NONE',  ( -155.3247660971250923, -155.4453047235116969, 40.99743995317548695 ) ) ;
#2787=CARTESIAN_POINT ( 'NONE',  ( -143.8425227516148084, -189.9584106276440423, 55.19815736654470584 ) ) ;
#2789=FACE_OUTER_BOUND ( 'NONE', #6009, .T. ) ;
#2791=CARTESIAN_POINT ( 'NONE',  ( -156.1828684652451784, -155.6591478762521206, 41.49287016839741682 ) ) ;
#2803=CARTESIAN_POINT ( 'NONE',  ( -159.5594255724347761, -176.7891397928654840, 43.77915905869157598 ) ) ;
#2804=CARTESIAN_POINT ( 'NONE',  ( -161.4692556286852607, -188.3391397928654953, 52.90620854394536821 ) ) ;
#2807=CARTESIAN_POINT ( 'NONE',  ( -142.0420953463935803, -195.2438272943107336, 46.59394152635518793 ) ) ;
#2812=CARTESIAN_POINT ( 'NONE',  ( -148.5561028927606344, -186.9938272943107336, 58.62277379824867296 ) ) ;
#2823=EDGE_CURVE ( 'NONE', #12361, #3465, #12741, .T. ) ;
#2827=CARTESIAN_POINT ( 'NONE',  ( -145.6429501568359797, -173.9438272943107222, 41.63779006702063867 ) ) ;
#2829=CARTESIAN_POINT ( 'NONE',  ( -159.5594255724347761, -181.8630981290893374, 43.77915905869157598 ) ) ;
#2851=CARTESIAN_POINT ( 'NONE',  ( -148.5561028927606344, -169.2584106276440536, 58.62277379824867296 ) ) ;
#2854=CARTESIAN_POINT ( 'NONE',  ( -149.8854112254399240, -183.7362167067689995, 59.65701158161632378 ) ) ;
#2855=CARTESIAN_POINT ( 'NONE',  ( -145.2889157411863437, -189.5130981290893146, 58.16351966513671812 ) ) ;
#2862=CARTESIAN_POINT ( 'NONE',  ( -157.2955611005346270, -170.3438272943107563, 41.63779006702063867 ) ) ;
#2863=CARTESIAN_POINT ( 'NONE',  ( -143.8425227516148084, -180.3584106276440480, 44.11586579668791330 ) ) ;
#2866=CARTESIAN_POINT ( 'NONE',  ( -142.0420953463936087, -165.6584106276440593, 49.65701158161630957 ) ) ;
#2879=DIRECTION ( 'NONE',  ( 0.000000000000000000, 1.000000000000000000, 0.000000000000000000 ) ) ;
#2888=CARTESIAN_POINT ( 'NONE',  ( -143.3790856849358306, -163.2891397928654555, 55.53486410454105027 ) ) ;
#2896=EDGE_LOOP ( 'NONE', ( #11907, #1390, #19035, #5979 ) ) ;
#2898=CARTESIAN_POINT ( 'NONE',  ( -143.8425227516148084, -192.9584106276440423, 55.19815736654470584 ) ) ;
#2900=CARTESIAN_POINT ( 'NONE',  ( -143.8425227516148084, -186.3584106276440480, 44.11586579668791330 ) ) ;
#2906=ORIENTED_EDGE ( 'NONE', *, *, #7281, .F. ) ;
#2916=CARTESIAN_POINT ( 'NONE',  ( -157.6495955161842062, -191.0391397928654271, 58.16351966513671812 ) ) ;
#2919=CARTESIAN_POINT ( 'NONE',  ( -157.2955611005346270, -191.3438272943106995, 41.63779006702063867 ) ) ;
#2924=CARTESIAN_POINT ( 'NONE',  ( -159.0959885057557983, -185.1938272943107222, 44.11586579668791330 ) ) ;
#2938=CARTESIAN_POINT ( 'NONE',  ( -156.1828684652451500, -155.6591478762520921, 41.49287016839741682 ) ) ;
#2939=CARTESIAN_POINT ( 'NONE',  ( -143.8425227516148084, -162.6938272943107222, 55.19815736654470584 ) ) ;
#2940=CARTESIAN_POINT ( 'NONE',  ( -161.4692556286853176, -175.5630981290893260, 49.65701158161630957 ) ) ;
#2951=CARTESIAN_POINT ( 'NONE',  ( -143.3790856849358306, -186.6891397928654612, 43.77915905869157598 ) ) ;
#2962=CARTESIAN_POINT ( 'NONE',  ( -148.5561028927606344, -172.2584106276440536, 58.62277379824867296 ) ) ;
#2963=CARTESIAN_POINT ( 'NONE',  ( -143.8425227516148084, -189.6938272943107222, 55.19815736654470584 ) ) ;
#2968=CARTESIAN_POINT ( 'NONE',  ( -143.3790856849358306, -174.6891397928654612, 43.77915905869157598 ) ) ;
#2974=CARTESIAN_POINT ( 'NONE',  ( -159.0959885057557983, -160.5938272943107279, 55.19815736654470584 ) ) ;
#2975=CARTESIAN_POINT ( 'NONE',  ( -148.5561028927606344, -186.0584106276440650, 40.69124936498395328 ) ) ;
#2978=CARTESIAN_POINT ( 'NONE',  ( -159.0959885057557983, -169.8584106276440764, 55.19815736654470584 ) ) ;
#2985=VERTEX_POINT ( 'NONE', #16627 ) ;
#2993=CARTESIAN_POINT ( 'NONE',  ( -151.4692556286852891, -196.9891397928655010, 49.65701158161630957 ) ) ;
#3005=CARTESIAN_POINT ( 'NONE',  ( -159.0959885057557983, -191.4584106276440423, 44.11586579668791330 ) ) ;
#3006=EDGE_CURVE ( 'NONE', #10856, #8233, #16511, .T. ) ;
#3008=CARTESIAN_POINT ( 'NONE',  ( -142.0420953463935803, -183.8084106276440366, 52.72008163687743831 ) ) ;
#3013=ORIENTED_EDGE ( 'NONE', *, *, #14327, .F. ) ;
#3020=( BOUNDED_CURVE ( )  B_SPLINE_CURVE ( 2, ( #8761, #6891, #15036, #1595, #1817, #3581, #11840, #6791, #10413, #18887, #3362, #379, #16796 ),
 .UNSPECIFIED., .F., .F. ) 
 B_SPLINE_CURVE_WITH_KNOTS ( ( 3, 2, 2, 2, 2, 2, 3 ),
 ( 0.01785714285714286656, 0.02142857142857142877, 0.02857142857142857054, 0.03571428571428571230, 0.04285714285714285754, 0.05000000000000000278, 0.05357142857142854764 ),
 .UNSPECIFIED. ) 
 CURVE ( )  GEOMETRIC_REPRESENTATION_ITEM ( )  RATIONAL_B_SPLINE_CURVE ( ( 0.9755282581475768211, 0.9755282581475768211, 1.000000000000000000, 0.9510565162951535312, 1.000000000000000000, 0.9510565162951535312, 1.000000000000000000, 0.9510565162951535312, 1.000000000000000000, 0.9510565162951535312, 1.000000000000000000, 0.9755282581475768211, 0.9755282581475765991 ) ) 
 REPRESENTATION_ITEM ( '' )  );
#3021=VECTOR ( 'NONE', #4706, 1000.000000000000000 ) ;
#3025=CARTESIAN_POINT ( 'NONE',  ( -143.3790856849358306, -192.6891397928654897, 43.77915905869157598 ) ) ;
#3028=CARTESIAN_POINT ( 'NONE',  ( -151.4692556286852891, -194.6438272943107393, 39.74470866294723947 ) ) ;
#3032=CARTESIAN_POINT ( 'NONE',  ( -151.4692556286852891, -182.6438272943107108, 39.74470866294723947 ) ) ;
#3050=CARTESIAN_POINT ( 'NONE',  ( -142.0420953463935803, -159.2438272943107336, 46.59394152635518083 ) ) ;
#3052=CARTESIAN_POINT ( 'NONE',  ( -141.4692556286852891, -173.9130981290893203, 46.40781461928724383 ) ) ;
#3056=CONICAL_SURFACE ( 'NONE', #5867, 9.000000000000007105, 0.7853981633974346233 ) ;
#3058=CARTESIAN_POINT ( 'NONE',  ( -151.4692556286852891, -196.9891397928655010, 39.65701158161630246 ) ) ;
#3075=CARTESIAN_POINT ( 'NONE',  ( -151.4692556286852891, -164.9084106276440593, 39.74470866294723947 ) ) ;
#3076=CARTESIAN_POINT ( 'NONE',  ( -160.8964159109769696, -193.8938272943107393, 49.65701158161630957 ) ) ;
#3077=CARTESIAN_POINT ( 'NONE',  ( -161.4692556286852891, -178.4130981290893203, 52.90620854394536821 ) ) ;
#3080=CARTESIAN_POINT ( 'NONE',  ( -148.3790856849358306, -175.5891397928654669, 59.16757674456786020 ) ) ;
#3088=CARTESIAN_POINT ( 'NONE',  ( -145.6429501568359797, -165.8438272943107563, 57.67623309621198047 ) ) ;
#3089=CARTESIAN_POINT ( 'NONE',  ( -154.3824083646099439, -182.7584106276440536, 40.69124936498395328 ) ) ;
#3092=CARTESIAN_POINT ( 'NONE',  ( -160.8964159109769696, -170.3084106276440082, 46.59394152635518793 ) ) ;
#3094=AXIS2_PLACEMENT_3D ( 'NONE', #3137, #9543, #6559 ) ;
#3112=UNCERTAINTY_MEASURE_WITH_UNIT (LENGTH_MEASURE( 1.000000000000000082E-05 ), #15176, 'distance_accuracy_value', 'NONE');
#3114=CARTESIAN_POINT ( 'NONE',  ( -159.5594255724347761, -185.1891397928654612, 55.53486410454104316 ) ) ;
#3117=CARTESIAN_POINT ( 'NONE',  ( -159.0959885057557983, -157.5938272943107279, 55.19815736654470584 ) ) ;
#3119=CARTESIAN_POINT ( 'NONE',  ( -148.5561028927606344, -186.0584106276440650, 40.69124936498395328 ) ) ;
#3121=CARTESIAN_POINT ( 'NONE',  ( -154.5594255724347761, -160.8891397928654499, 59.16757674456785310 ) ) ;
#3134=CARTESIAN_POINT ( 'NONE',  ( -151.4692556286852607, -183.8130981290892692, 59.65701158161632378 ) ) ;
#3136=CARTESIAN_POINT ( 'NONE',  ( -151.4692556286852891, -178.7391397928655010, 60.17163382399899518 ) ) ;
#3137=CARTESIAN_POINT ( 'NONE',  ( -151.4692556286852891, -195.9891397928654726, 49.65701158161630957 ) ) ;
#3139=CARTESIAN_POINT ( 'NONE',  ( -151.4692556286852891, -190.1438272943107393, 59.56931450028537967 ) ) ;
#3140=VECTOR ( 'NONE', #5913, 1000.000000000000000 ) ;
#3144=CARTESIAN_POINT ( 'NONE',  ( -160.8964159109769696, -184.8938272943107393, 49.65701158161630957 ) ) ;
#3153=( BOUNDED_CURVE ( )  B_SPLINE_CURVE ( 2, ( #8472, #3506, #10447, #20580, #5466, #5572, #5366, #7250, #13525, #11870, #10552, #18708, #3615 ),
 .UNSPECIFIED., .F., .F. ) 
 B_SPLINE_CURVE_WITH_KNOTS ( ( 3, 2, 2, 2, 2, 2, 3 ),
 ( 0.2678571428571429047, 0.2714285714285714080, 0.2785714285714285809, 0.2857142857142856984, 0.2928571428571428714, 0.2999999999999999889, 0.3035714285714286031 ),
 .UNSPECIFIED. ) 
 CURVE ( )  GEOMETRIC_REPRESENTATION_ITEM ( )  RATIONAL_B_SPLINE_CURVE ( ( 0.9755282581475768211, 0.9755282581475771542, 1.000000000000000000, 0.9510565162951535312, 1.000000000000000000, 0.9510565162951535312, 1.000000000000000000, 0.9510565162951535312, 1.000000000000000000, 0.9510565162951535312, 1.000000000000000000, 0.9755282581475765991, 0.9755282581475768211 ) ) 
 REPRESENTATION_ITEM ( '' )  );
#3158=CARTESIAN_POINT ( 'NONE',  ( -151.4692556286852891, -192.8130981290892692, 59.65701158161632378 ) ) ;
#3163=CARTESIAN_POINT ( 'NONE',  ( -160.8964159109769696, -158.0438272943107165, 46.59394152635518083 ) ) ;
#3164=CARTESIAN_POINT ( 'NONE',  ( -148.3790856849358306, -165.3891397928654499, 40.14644641866477315 ) ) ;
#3165=CARTESIAN_POINT ( 'NONE',  ( -154.5594255724347761, -177.9630981290893033, 59.16757674456785310 ) ) ;
#3166=SHAPE_REPRESENTATION_RELATIONSHIP ( 'NONE' , 'NONE' ,  #8609, #1649 ) ;
#3167=CARTESIAN_POINT ( 'NONE',  ( -151.4692556286852891, -196.9891397928655010, 49.65701158161630957 ) ) ;
#3172=CARTESIAN_POINT ( 'NONE',  ( -159.5594255724347761, -170.7891397928654840, 43.77915905869157598 ) ) ;
#3173=PRODUCT_DEFINITION_FORMATION_WITH_SPECIFIED_SOURCE ( 'ANY', '', #15187, .NOT_KNOWN. ) ;
#3177=CARTESIAN_POINT ( 'NONE',  ( -141.4692556286852891, -186.9891397928654726, 49.65701158161630957 ) ) ;
#3188=CARTESIAN_POINT ( 'NONE',  ( -156.1828648351502409, -155.3945647575687872, 41.49286807254280518 ) ) ;
#3189=CARTESIAN_POINT ( 'NONE',  ( -160.8964159109769696, -167.0084106276440536, 52.72008163687743121 ) ) ;
#3190=CARTESIAN_POINT ( 'NONE',  ( -143.8425227516148084, -192.0938272943107279, 44.11586579668791330 ) ) ;
#3191=CARTESIAN_POINT ( 'NONE',  ( -161.4692556286853176, -178.5630981290893260, 49.65701158161630957 ) ) ;
#3194=CARTESIAN_POINT ( 'NONE',  ( -141.4692556286852891, -177.2130981290892748, 52.90620854394536821 ) ) ;
#3200=CARTESIAN_POINT ( 'NONE',  ( -145.6429501568359797, -161.9438272943107222, 41.63779006702063867 ) ) ;
#3201=CARTESIAN_POINT ( 'NONE',  ( -154.3824083646099439, -173.7584106276440536, 40.69124936498395328 ) ) ;
#3204=CARTESIAN_POINT ( 'NONE',  ( -157.2955611005346270, -157.7084106276440423, 57.67623309621198047 ) ) ;
#3207=EDGE_CURVE ( 'NONE', #8340, #4358, #8952, .T. ) ;
#3209=VERTEX_POINT ( 'NONE', #18831 ) ;
#3210=EDGE_LOOP ( 'NONE', ( #14662, #4234, #21319, #10321 ) ) ;
#3221=LINE ( 'NONE', #16433, #15274 ) ;
#3224=CARTESIAN_POINT ( 'NONE',  ( -157.6495955161842062, -185.9391397928654612, 41.15050349809589392 ) ) ;
#3227=CARTESIAN_POINT ( 'NONE',  ( -143.8425227516148084, -159.0938272943107279, 44.11586579668791330 ) ) ;
#3230=CARTESIAN_POINT ( 'NONE',  ( -159.0959885057557983, -188.4584106276440423, 44.11586579668791330 ) ) ;
#3249=FACE_OUTER_BOUND ( 'NONE', #2020, .T. ) ;
#3250=CARTESIAN_POINT ( 'NONE',  ( -148.3790856849358306, -178.5891397928654669, 59.16757674456786020 ) ) ;
#3257=CARTESIAN_POINT ( 'NONE',  ( -154.3824083646099439, -187.2938272943107449, 58.62277379824867296 ) ) ;
#3264=EDGE_CURVE ( 'NONE', #2548, #5724, #3734, .T. ) ;
#3272=CARTESIAN_POINT ( 'NONE',  ( -159.0959885057557983, -166.5938272943107563, 55.19815736654470584 ) ) ;
#3274=CARTESIAN_POINT ( 'NONE',  ( -148.3790856849358306, -180.6630981290893203, 59.16757674456786020 ) ) ;
#3299=CARTESIAN_POINT ( 'NONE',  ( -151.4692556286852891, -170.9084106276440593, 39.74470866294723947 ) ) ;
#3300=CARTESIAN_POINT ( 'NONE',  ( -148.5561028927606344, -194.7938272943107449, 40.69124936498395328 ) ) ;
#3301=CARTESIAN_POINT ( 'NONE',  ( -161.4692556286852891, -166.4130981290892919, 52.90620854394536821 ) ) ;
#3303=CARTESIAN_POINT ( 'NONE',  ( -151.4692556286852891, -189.8130981290892976, 59.65701158161632378 ) ) ;
#3305=CARTESIAN_POINT ( 'NONE',  ( -141.4692556286852891, -174.9891397928654726, 49.65701158161630957 ) ) ;
#3311=CARTESIAN_POINT ( 'NONE',  ( -157.2955611005346270, -166.4438272943107506, 57.67623309621198047 ) ) ;
#3312=CARTESIAN_POINT ( 'NONE',  ( -148.5561028927606344, -172.2584106276440536, 58.62277379824867296 ) ) ;
#3316=CARTESIAN_POINT ( 'NONE',  ( -142.0420953463935803, -156.8084106276440366, 52.72008163687743831 ) ) ;
#3320=ORIENTED_EDGE ( 'NONE', *, *, #2823, .F. ) ;
#3339=CARTESIAN_POINT ( 'NONE',  ( -145.6429501568359797, -187.1084106276440480, 57.67623309621198047 ) ) ;
#3341=CARTESIAN_POINT ( 'NONE',  ( -148.5561028927606344, -175.2584106276440536, 58.62277379824867296 ) ) ;
#3342=ORIENTED_EDGE ( 'NONE', *, *, #10504, .F. ) ;
#3348=ADVANCED_FACE ( 'NONE', ( #2789 ), #9531, .T. ) ;
#3350=( BOUNDED_CURVE ( )  B_SPLINE_CURVE ( 2, ( #13006, #11020, #7940, #5836, #19294, #17843, #17730, #2636, #7730, #4395, #10920, #6157, #778 ),
 .UNSPECIFIED., .F., .F. ) 
 B_SPLINE_CURVE_WITH_KNOTS ( ( 3, 2, 2, 2, 2, 2, 3 ),
 ( 0.1607142857142856984, 0.1642857142857142849, 0.1714285714285714302, 0.1785714285714285754, 0.1857142857142857206, 0.1928571428571428659, 0.1964285714285714524 ),
 .UNSPECIFIED. ) 
 CURVE ( )  GEOMETRIC_REPRESENTATION_ITEM ( )  RATIONAL_B_SPLINE_CURVE ( ( 0.9755282581475768211, 0.9755282581475767101, 1.000000000000000000, 0.9510565162951535312, 1.000000000000000000, 0.9510565162951535312, 1.000000000000000000, 0.9510565162951535312, 1.000000000000000000, 0.9510565162951535312, 1.000000000000000000, 0.9755282581475765991, 0.9755282581475767101 ) ) 
 REPRESENTATION_ITEM ( '' )  );
#3359=CARTESIAN_POINT ( 'NONE',  ( -148.3790856849358306, -175.5891397928654669, 59.16757674456786020 ) ) ;
#3362=CARTESIAN_POINT ( 'NONE',  ( -154.5594255724347761, -193.8891397928654783, 59.16757674456785310 ) ) ;
#3368=CARTESIAN_POINT ( 'NONE',  ( -157.2955611005346270, -172.4438272943107506, 57.67623309621198047 ) ) ;
#3376=B_SPLINE_CURVE_WITH_KNOTS ( 'NONE', 3,
 ( #14477, #1367, #18231, #4897 ),
 .UNSPECIFIED., .F., .F.,
 ( 4, 4 ),
 ( 0.000000000000000000, 1.000000000000000000 ),
 .UNSPECIFIED. ) ;
#3385=CARTESIAN_POINT ( 'NONE',  ( -157.2955611005345986, -161.3438272943107279, 41.63779006702063867 ) ) ;
#3387=CARTESIAN_POINT ( 'NONE',  ( -145.2889157411863721, -171.5130981290893430, 58.16351966513671812 ) ) ;
#3388=( NAMED_UNIT ( * ) PLANE_ANGLE_UNIT ( ) SI_UNIT ( $, .RADIAN. ) );
#3389=CARTESIAN_POINT ( 'NONE',  ( -151.4692556286852891, -186.8130981290893260, 59.65701158161632378 ) ) ;
#3397=CARTESIAN_POINT ( 'NONE',  ( -143.9637021292202235, -116.9891397928655010, 36.65701158161628825 ) ) ;
#3417=CARTESIAN_POINT ( 'NONE',  ( -160.8964159109769696, -161.1584106276440593, 49.65701158161630957 ) ) ;
#3418=CARTESIAN_POINT ( 'NONE',  ( -160.8964159109769696, -191.0438272943107449, 46.59394152635518083 ) ) ;
#3423=VECTOR ( 'NONE', #10749, 1000.000000000000000 ) ;
#3428=CARTESIAN_POINT ( 'NONE',  ( -160.8964159109769696, -160.7438272943107052, 52.72008163687743121 ) ) ;
#3429=CARTESIAN_POINT ( 'NONE',  ( -148.5561028927606344, -174.0584106276440366, 40.69124936498395328 ) ) ;
#3432=CARTESIAN_POINT ( 'NONE',  ( -154.3824083646099439, -163.5584106276440366, 58.62277379824867296 ) ) ;
#3444=EDGE_CURVE ( 'NONE', #20510, #12850, #16759, .T. ) ;
#3447=CYLINDRICAL_SURFACE ( 'NONE', #12876, 10.00000000000000888 ) ;
#3456=CARTESIAN_POINT ( 'NONE',  ( -151.4692556286852891, -188.9084106276440593, 39.74470866294723947 ) ) ;
#3458=CARTESIAN_POINT ( 'NONE',  ( -142.0420953463935803, -177.5084106276440536, 46.59394152635518793 ) ) ;
#3465=VERTEX_POINT ( 'NONE', #15747 ) ;
#3468=ORIENTED_EDGE ( 'NONE', *, *, #8693, .F. ) ;
#3474=CARTESIAN_POINT ( 'NONE',  ( -148.3790856849358306, -184.5891397928654669, 59.16757674456786020 ) ) ;
#3482=CARTESIAN_POINT ( 'NONE',  ( -154.3824083646099439, -173.4938272943107336, 40.69124936498395328 ) ) ;
#3498=CARTESIAN_POINT ( 'NONE',  ( -151.4692556286852607, -157.7391397928654726, 59.65701158161632378 ) ) ;
#3499=CARTESIAN_POINT ( 'NONE',  ( -143.8425227516148084, -156.0938272943107279, 44.11586579668791330 ) ) ;
#3501=CARTESIAN_POINT ( 'NONE',  ( -154.5594255724347761, -165.9630981290893033, 59.16757674456785310 ) ) ;
#3506=CARTESIAN_POINT ( 'NONE',  ( -149.8854112254399240, -184.6622583705452030, 59.65701158161632378 ) ) ;
#3511=CARTESIAN_POINT ( 'NONE',  ( -149.8854112254399524, -185.3899795514095388, 39.65701158161630246 ) ) ;
#3515=CARTESIAN_POINT ( 'NONE',  ( -145.2889157411863437, -168.5130981290892578, 58.16351966513671812 ) ) ;
#3521=CARTESIAN_POINT ( 'NONE',  ( -142.0420953463935803, -162.8084106276440650, 52.72008163687743831 ) ) ;
#3522=CARTESIAN_POINT ( 'NONE',  ( -148.5561028927606344, -179.7938272943107449, 40.69124936498395328 ) ) ;
#3524=FACE_OUTER_BOUND ( 'NONE', #7367, .T. ) ;
#3527=CARTESIAN_POINT ( 'NONE',  ( -153.0531000319307111, -174.1622583705452314, 39.65701158161631668 ) ) ;
#3533=CARTESIAN_POINT ( 'NONE',  ( -159.0959885057557983, -176.4584106276440707, 44.11586579668791330 ) ) ;
#3535=CARTESIAN_POINT ( 'NONE',  ( -160.8964159109769696, -161.0084106276440252, 52.72008163687743121 ) ) ;
#3542=EDGE_LOOP ( 'NONE', ( #16227, #19650, #5450, #16336 ) ) ;
#3551=CARTESIAN_POINT ( 'NONE',  ( -161.4692556286852891, -190.7130981290893033, 46.40781461928724383 ) ) ;
#3556=DIRECTION ( 'NONE',  ( -0.000000000000000000, 1.000000000000000000, -0.000000000000000000 ) ) ;
#3557=EDGE_CURVE ( 'NONE', #4126, #19197, #17936, .T. ) ;
#3559=CARTESIAN_POINT ( 'NONE',  ( -142.0420953463936087, -189.6584106276440593, 49.65701158161630957 ) ) ;
#3561=CARTESIAN_POINT ( 'NONE',  ( -142.0420953463935803, -180.8084106276440366, 52.72008163687743831 ) ) ;
#3573=LINE ( 'NONE', #10298, #21348 ) ;
#3578=CARTESIAN_POINT ( 'NONE',  ( -159.5594255724347761, -182.1891397928654612, 55.53486410454104316 ) ) ;
#3581=CARTESIAN_POINT ( 'NONE',  ( -161.4692556286852891, -194.6391397928654783, 46.40781461928724383 ) ) ;
#3585=CARTESIAN_POINT ( 'NONE',  ( -143.8425227516148084, -177.6938272943107506, 55.19815736654470584 ) ) ;
#3588=CARTESIAN_POINT ( 'NONE',  ( -151.4692556286852607, -159.2391397928654726, 39.65701158161629536 ) ) ;
#3594=ORIENTED_EDGE ( 'NONE', *, *, #16609, .F. ) ;
#3607=CARTESIAN_POINT ( 'NONE',  ( -148.3790856849358306, -173.4630981290893033, 40.14644641866477315 ) ) ;
#3609=CARTESIAN_POINT ( 'NONE',  ( -157.6495955161842062, -166.1130981290892521, 58.16351966513671812 ) ) ;
#3613=( BOUNDED_CURVE ( )  B_SPLINE_CURVE ( 2, ( #9155, #7068, #9044, #20511, #15856, #5398, #10483, #13987, #12116, #7395, #20724, #545, #12335 ),
 .UNSPECIFIED., .F., .F. ) 
 B_SPLINE_CURVE_WITH_KNOTS ( ( 3, 2, 2, 2, 2, 2, 3 ),
 ( 0.3750000000000000000, 0.3785714285714285587, 0.3857142857142857317, 0.3928571428571428492, 0.4000000000000000222, 0.4071428571428571397, 0.4107142857142857539 ),
 .UNSPECIFIED. ) 
 CURVE ( )  GEOMETRIC_REPRESENTATION_ITEM ( )  RATIONAL_B_SPLINE_CURVE ( ( 0.9755282581475768211, 0.9755282581475768211, 1.000000000000000000, 0.9510565162951535312, 1.000000000000000000, 0.9510565162951535312, 1.000000000000000000, 0.9510565162951535312, 1.000000000000000000, 0.9510565162951535312, 1.000000000000000000, 0.9755282581475765991, 0.9755282581475768211 ) ) 
 REPRESENTATION_ITEM ( '' )  );
#3615=CARTESIAN_POINT ( 'NONE',  ( -151.4692556286852891, -183.2391397928654726, 39.65701158161629536 ) ) ;
#3620=CARTESIAN_POINT ( 'NONE',  ( -166.4803626276155626, -126.9891397928655010, 49.65701158161629536 ) ) ;
#3629=CARTESIAN_POINT ( 'NONE',  ( -161.4692556286852607, -194.3391397928654669, 52.90620854394536821 ) ) ;
#3631=CARTESIAN_POINT ( 'NONE',  ( -154.3824083646099439, -176.4938272943107336, 40.69124936498395328 ) ) ;
#3632=CARTESIAN_POINT ( 'NONE',  ( -149.8854112254399524, -178.6622583705452314, 59.65701158161632378 ) ) ;
#3635=PLANE ( 'NONE',  #18550 ) ;
#3640=CARTESIAN_POINT ( 'NONE',  ( -151.4692556286852891, -178.4084106276440593, 59.56931450028537256 ) ) ;
#3647=EDGE_LOOP ( 'NONE', ( #9210, #9558, #9741, #13451 ) ) ;
#3660=CARTESIAN_POINT ( 'NONE',  ( -160.8964159109769696, -184.8938272943107393, 49.65701158161630957 ) ) ;
#3664=CARTESIAN_POINT ( 'NONE',  ( -159.0959885057557983, -187.8584106276440480, 55.19815736654470584 ) ) ;
#3666=CARTESIAN_POINT ( 'NONE',  ( -154.3824083646099439, -176.7584106276440536, 40.69124936498395328 ) ) ;
#3669=CARTESIAN_POINT ( 'NONE',  ( -166.4803626276155626, -116.9891397928655010, 49.65701158161629536 ) ) ;
#3683=CARTESIAN_POINT ( 'NONE',  ( -151.4692556286852891, -174.2391397928655010, 39.14238933923362396 ) ) ;
#3685=CARTESIAN_POINT ( 'NONE',  ( -159.5594255724347761, -181.2630981290893146, 55.53486410454104316 ) ) ;
#3686=DIRECTION ( 'NONE',  ( 0.000000000000000000, 0.000000000000000000, 1.000000000000000000 ) ) ;
#3690=CARTESIAN_POINT ( 'NONE',  ( -142.0420953463935803, -171.5438272943106881, 52.72008163687743831 ) ) ;
#3691=AXIS2_PLACEMENT_3D ( 'NONE', #3167, #16597, #1514 ) ;
#3696=CARTESIAN_POINT ( 'NONE',  ( -149.8854112254398956, -189.3160212151857422, 39.65701158161630246 ) ) ;
#3707=DIRECTION ( 'NONE',  ( -0.000000000000000000, 1.000000000000000000, -0.000000000000000000 ) ) ;
#3711=CARTESIAN_POINT ( 'NONE',  ( -145.2889157411863721, -168.5130981290892578, 58.16351966513671812 ) ) ;
#3714=CARTESIAN_POINT ( 'NONE',  ( -153.0531000319306543, -190.8160212151857422, 59.65701158161630957 ) ) ;
#3724=CARTESIAN_POINT ( 'NONE',  ( -148.3790856849358306, -156.6630981290892919, 59.16757674456786020 ) ) ;
#3726=ORIENTED_EDGE ( 'NONE', *, *, #349, .T. ) ;
#3728=CARTESIAN_POINT ( 'NONE',  ( -143.9637021292201950, -116.9891397928655010, 62.65701158161630957 ) ) ;
#3734=( BOUNDED_CURVE ( )  B_SPLINE_CURVE ( 2, ( #1358, #16444, #9747, #7874, #14573, #6428, #11379, #21209, #4766, #19538, #3121, #6091, #19767 ),
 .UNSPECIFIED., .F., .F. ) 
 B_SPLINE_CURVE_WITH_KNOTS ( ( 3, 2, 2, 2, 2, 2, 3 ),
 ( 0.8035714285714286031, 0.8071428571428571619, 0.8142857142857142794, 0.8214285714285713969, 0.8285714285714286254, 0.8357142857142857428, 0.8392857142857143016 ),
 .UNSPECIFIED. ) 
 CURVE ( )  GEOMETRIC_REPRESENTATION_ITEM ( )  RATIONAL_B_SPLINE_CURVE ( ( 0.9755282581475768211, 0.9755282581475768211, 1.000000000000000000, 0.9510565162951535312, 1.000000000000000000, 0.9510565162951535312, 1.000000000000000000, 0.9510565162951535312, 1.000000000000000000, 0.9510565162951535312, 1.000000000000000000, 0.9755282581475768211, 0.9755282581475768211 ) ) 
 REPRESENTATION_ITEM ( '' )  );
#3735=CARTESIAN_POINT ( 'NONE',  ( -151.4692556286852891, -161.9084106276440593, 39.74470866294723947 ) ) ;
#3736=CARTESIAN_POINT ( 'NONE',  ( -157.2955611005345986, -184.4438272943107506, 57.67623309621197336 ) ) ;
#3738=CARTESIAN_POINT ( 'NONE',  ( -154.5594255724347761, -194.1630981290892919, 40.14644641866476604 ) ) ;
#3740=CARTESIAN_POINT ( 'NONE',  ( 0.000000000000000000, -116.9891397928655010, 0.000000000000000000 ) ) ;
#3746=CARTESIAN_POINT ( 'NONE',  ( -157.6495955161842062, -188.9391397928654328, 41.15050349809589392 ) ) ;
#3747=CARTESIAN_POINT ( 'NONE',  ( -154.3824083646099439, -161.7584106276440252, 40.69124936498395328 ) ) ;
#3756=ORIENTED_EDGE ( 'NONE', *, *, #1015, .T. ) ;
#3770=CARTESIAN_POINT ( 'NONE',  ( -142.0420953463935803, -177.2438272943107620, 46.59394152635518793 ) ) ;
#3771=CARTESIAN_POINT ( 'NONE',  ( -160.8964159109769696, -194.3084106276440366, 46.59394152635518083 ) ) ;
#3773=CARTESIAN_POINT ( 'NONE',  ( -151.4692556286852891, -178.4084106276440878, 59.56931450028537967 ) ) ;
#3793=CARTESIAN_POINT ( 'NONE',  ( -161.4692556286853176, -170.4891397928654726, 49.65701158161630957 ) ) ;
#3794=CARTESIAN_POINT ( 'NONE',  ( -157.6495955161842062, -182.0130981290893146, 41.15050349809589392 ) ) ;
#3795=CYLINDRICAL_SURFACE ( 'NONE', #8313, 10.00000000000000888 ) ;
#3797=EDGE_CURVE ( 'NONE', #18561, #13046, #19819, .T. ) ;
#3799=CARTESIAN_POINT ( 'NONE',  ( -159.0959885057557983, -175.5938272943107279, 55.19815736654470584 ) ) ;
#3814=CARTESIAN_POINT ( 'NONE',  ( -143.3790856849358306, -181.2891397928654840, 55.53486410454105027 ) ) ;
#3815=CARTESIAN_POINT ( 'NONE',  ( -141.4692556286852891, -195.9891397928654726, 49.65701158161630957 ) ) ;
#3817=CARTESIAN_POINT ( 'NONE',  ( -148.5561028927606344, -156.9938272943107052, 58.62277379824867296 ) ) ;
#3819=CARTESIAN_POINT ( 'NONE',  ( -157.6495955161842062, -169.1130981290893374, 58.16351966513671812 ) ) ;
#3832=CARTESIAN_POINT ( 'NONE',  ( -141.4692556286852891, -168.9891397928654726, 49.65701158161630957 ) ) ;
#3838=LINE ( 'NONE', #17160, #20393 ) ;
#3842=CARTESIAN_POINT ( 'NONE',  ( -159.0959885057557983, -157.8584106276440480, 55.19815736654470584 ) ) ;
#3843=CARTESIAN_POINT ( 'NONE',  ( -142.0420953463935803, -183.5438272943107449, 52.72008163687743831 ) ) ;
#3848=CARTESIAN_POINT ( 'NONE',  ( -151.4692556286852891, -195.9891397928654726, 59.65701158161632378 ) ) ;
#3854=CARTESIAN_POINT ( 'NONE',  ( -159.0959885057557983, -163.8584106276440480, 55.19815736654470584 ) ) ;
#3878=CARTESIAN_POINT ( 'NONE',  ( -151.4692556286852891, -185.6438272943107393, 39.74470866294723947 ) ) ;
#3879=CARTESIAN_POINT ( 'NONE',  ( -154.3824083646099439, -194.7584106276440536, 40.69124936498395328 ) ) ;
#3881=CARTESIAN_POINT ( 'NONE',  ( -160.8964159109769696, -179.1584106276440309, 49.65701158161630957 ) ) ;
#3901=CARTESIAN_POINT ( 'NONE',  ( -154.5594255724347761, -168.0891397928654669, 40.14644641866476604 ) ) ;
#3904=DIRECTION ( 'NONE',  ( -0.000000000000000000, 1.000000000000000000, -0.000000000000000000 ) ) ;
#3905=CARTESIAN_POINT ( 'NONE',  ( -141.4692556286852891, -196.9891397928655010, 49.65701158161630957 ) ) ;
#3908=CARTESIAN_POINT ( 'NONE',  ( -159.0959885057557983, -163.5938272943107279, 55.19815736654470584 ) ) ;
#3916=ORIENTED_EDGE ( 'NONE', *, *, #17917, .F. ) ;
#3926=CARTESIAN_POINT ( 'NONE',  ( -154.5594255724347761, -159.9630981290893317, 59.16757674456785310 ) ) ;
#3931=CARTESIAN_POINT ( 'NONE',  ( -142.0420953463936087, -195.3938272943107393, 49.65701158161630957 ) ) ;
#3938=CARTESIAN_POINT ( 'NONE',  ( -149.8854112254399240, -168.3160212151857138, 39.65701158161629536 ) ) ;
#3939=AXIS2_PLACEMENT_3D ( 'NONE', #14788, #9739, #2006 ) ;
#3943=CONICAL_SURFACE ( 'NONE', #21189, 9.000000000000007105, 0.7853981633974346233 ) ;
#3945=CARTESIAN_POINT ( 'NONE',  ( -151.4692556286852607, -172.7391397928654726, 59.65701158161632378 ) ) ;
#3950=CARTESIAN_POINT ( 'NONE',  ( -143.8425227516148084, -183.6938272943107506, 55.19815736654470584 ) ) ;
#3952=CARTESIAN_POINT ( 'NONE',  ( -145.2889157411863721, -188.6130981290893089, 41.15050349809590102 ) ) ;
#3964=CARTESIAN_POINT ( 'NONE',  ( -160.8964159109769696, -161.1584106276440593, 49.65701158161630957 ) ) ;
#3965=CARTESIAN_POINT ( 'NONE',  ( -159.5594255724347761, -164.7891397928654555, 43.77915905869157598 ) ) ;
#3972=CARTESIAN_POINT ( 'NONE',  ( -154.5594255724347761, -159.9630981290893317, 59.16757674456785310 ) ) ;
#3987=CARTESIAN_POINT ( 'NONE',  ( -154.3824083646099439, -184.2938272943107449, 58.62277379824867296 ) ) ;
#3988=CARTESIAN_POINT ( 'NONE',  ( -154.3824083646099439, -190.5584106276440650, 58.62277379824867296 ) ) ;
#3990=CARTESIAN_POINT ( 'NONE',  ( -157.2955611005346270, -175.7084106276440707, 57.67623309621198047 ) ) ;
#3999=EDGE_LOOP ( 'NONE', ( #6371, #11578, #9584, #16256 ) ) ;
#4004=CARTESIAN_POINT ( 'NONE',  ( -151.4692556286853176, -162.8130981290893260, 59.65701158161632378 ) ) ;
#4005=CARTESIAN_POINT ( 'NONE',  ( -161.4692556286852607, -170.6391397928654499, 46.40781461928724383 ) ) ;
#4006=CARTESIAN_POINT ( 'NONE',  ( -143.3790856849358306, -159.3630981290893089, 55.53486410454105027 ) ) ;
#4011=CARTESIAN_POINT ( 'NONE',  ( -148.5561028927606344, -161.7938272943107449, 40.69124936498395328 ) ) ;
#4014=CARTESIAN_POINT ( 'NONE',  ( -154.3824083646099439, -193.5584106276440650, 58.62277379824867296 ) ) ;
#4017=LINE ( 'NONE', #8986, #10632 ) ;
#4022=VERTEX_POINT ( 'NONE', #20476 ) ;
#4033=CARTESIAN_POINT ( 'NONE',  ( -141.4692556286852891, -156.0630981290892976, 49.65701158161630957 ) ) ;
#4039=CARTESIAN_POINT ( 'NONE',  ( -148.5561028927606344, -189.9938272943107336, 58.62277379824867296 ) ) ;
#4048=ORIENTED_EDGE ( 'NONE', *, *, #16598, .T. ) ;
#4055=CARTESIAN_POINT ( 'NONE',  ( -142.0420953463935803, -174.5438272943107165, 52.72008163687743831 ) ) ;
#4057=CARTESIAN_POINT ( 'NONE',  ( -148.3790856849358306, -185.4630981290893033, 40.14644641866477315 ) ) ;
#4065=CARTESIAN_POINT ( 'NONE',  ( -151.4692556286852891, -169.4084106276440593, 59.56931450028537256 ) ) ;
#4067=EDGE_CURVE ( 'NONE', #18469, #16234, #5049, .T. ) ;
#4068=LINE ( 'NONE', #759, #7828 ) ;
#4072=ORIENTED_EDGE ( 'NONE', *, *, #9917, .T. ) ;
#4073=CARTESIAN_POINT ( 'NONE',  ( -159.5594255724347761, -160.2630981290893146, 55.53486410454104316 ) ) ;
#4089=CARTESIAN_POINT ( 'NONE',  ( -143.8425227516148084, -177.0938272943107279, 44.11586579668791330 ) ) ;
#4090=CARTESIAN_POINT ( 'NONE',  ( -159.0959885057557983, -194.4584106276440423, 44.11586579668791330 ) ) ;
#4092=CARTESIAN_POINT ( 'NONE',  ( -142.0420953463935803, -180.5084106276440536, 46.59394152635518793 ) ) ;
#4108=CARTESIAN_POINT ( 'NONE',  ( -148.3790856849358306, -179.4630981290893033, 40.14644641866477315 ) ) ;
#4109=CARTESIAN_POINT ( 'NONE',  ( -141.4692556286852891, -174.8391397928654669, 46.40781461928724383 ) ) ;
#4116=CARTESIAN_POINT ( 'NONE',  ( -143.8425227516148084, -162.6938272943107222, 55.19815736654470584 ) ) ;
#4119=CARTESIAN_POINT ( 'NONE',  ( -159.0959885057557983, -191.4584106276440423, 44.11586579668791330 ) ) ;
#4126=VERTEX_POINT ( 'NONE', #7691 ) ;
#4127=LINE ( 'NONE', #9752, #21365 ) ;
#4132=LINE ( 'NONE', #10866, #7747 ) ;
#4135=CARTESIAN_POINT ( 'NONE',  ( -141.4692556286852891, -191.9130981290892919, 46.40781461928724383 ) ) ;
#4140=CARTESIAN_POINT ( 'NONE',  ( -155.5590433672037989, -155.1145756620584564, 40.47124192889010885 ) ) ;
#4147=VECTOR ( 'NONE', #18159, 1000.000000000000114 ) ;
#4150=VERTEX_POINT ( 'NONE', #9231 ) ;
#4155=DIRECTION ( 'NONE',  ( -0.000000000000000000, 1.000000000000000000, -0.000000000000000000 ) ) ;
#4165=CARTESIAN_POINT ( 'NONE',  ( -143.8425227516148084, -174.6938272943107506, 55.19815736654470584 ) ) ;
#4167=CARTESIAN_POINT ( 'NONE',  ( -157.6495955161842062, -184.1130981290893089, 58.16351966513671812 ) ) ;
#4175=CARTESIAN_POINT ( 'NONE',  ( -143.8425227516148084, -168.9584106276440423, 55.19815736654470584 ) ) ;
#4182=CARTESIAN_POINT ( 'NONE',  ( -141.4692556286852891, -157.1391397928654783, 52.90620854394536821 ) ) ;
#4197=CARTESIAN_POINT ( 'NONE',  ( -148.5561028927606344, -168.9938272943107336, 58.62277379824867296 ) ) ;
#4216=CARTESIAN_POINT ( 'NONE',  ( -161.4692556286852607, -164.6391397928654499, 46.40781461928724383 ) ) ;
#4223=CARTESIAN_POINT ( 'NONE',  ( -148.5561028927606344, -164.7938272943107449, 40.69124936498395328 ) ) ;
#4234=ORIENTED_EDGE ( 'NONE', *, *, #13263, .T. ) ;
#4240=CARTESIAN_POINT ( 'NONE',  ( -141.4692556286852891, -193.1391397928654783, 52.90620854394536821 ) ) ;
#4243=CARTESIAN_POINT ( 'NONE',  ( -157.6495955161842062, -163.1130981290892805, 58.16351966513671812 ) ) ;
#4248=CARTESIAN_POINT ( 'NONE',  ( -145.6429501568359797, -188.9438272943106938, 41.63779006702063867 ) ) ;
#4265=CARTESIAN_POINT ( 'NONE',  ( -148.5561028927606344, -171.9938272943107336, 58.62277379824867296 ) ) ;
#4267=CARTESIAN_POINT ( 'NONE',  ( -141.4692556286852891, -192.0630981290892976, 49.65701158161630957 ) ) ;
#4273=CARTESIAN_POINT ( 'NONE',  ( -151.4692556286852891, -160.4084106276440593, 59.56931450028537256 ) ) ;
#4275=CARTESIAN_POINT ( 'NONE',  ( -156.4692903108300186, -155.9898770414735623, 40.99677756761010272 ) ) ;
#4297=CARTESIAN_POINT ( 'NONE',  ( -143.8425227516148084, -171.6938272943107222, 55.19815736654470584 ) ) ;
#4298=CARTESIAN_POINT ( 'NONE',  ( -159.0959885057557983, -181.8584106276440480, 55.19815736654470584 ) ) ;
#4300=( BOUNDED_CURVE ( )  B_SPLINE_CURVE ( 2, ( #15303, #5160, #11881, #3515, #1749, #14850, #11769, #6486, #18610, #197, #9806, #13100, #13206 ),
 .UNSPECIFIED., .F., .F. ) 
 B_SPLINE_CURVE_WITH_KNOTS ( ( 3, 2, 2, 2, 2, 2, 3 ),
 ( 0.6250000000000000000, 0.6285714285714285587, 0.6357142857142856762, 0.6428571428571429047, 0.6500000000000000222, 0.6571428571428571397, 0.6607142857142856984 ),
 .UNSPECIFIED. ) 
 CURVE ( )  GEOMETRIC_REPRESENTATION_ITEM ( )  RATIONAL_B_SPLINE_CURVE ( ( 0.9755282581475768211, 0.9755282581475768211, 1.000000000000000000, 0.9510565162951535312, 1.000000000000000000, 0.9510565162951535312, 1.000000000000000000, 0.9510565162951535312, 1.000000000000000000, 0.9510565162951535312, 1.000000000000000000, 0.9755282581475768211, 0.9755282581475768211 ) ) 
 REPRESENTATION_ITEM ( '' )  );
#4301=CARTESIAN_POINT ( 'NONE',  ( -142.0420953463936087, -168.6584106276440593, 49.65701158161630957 ) ) ;
#4319=CARTESIAN_POINT ( 'NONE',  ( -145.2889157411863721, -156.5391397928654840, 41.15050349809590102 ) ) ;
#4322=DIRECTION ( 'NONE',  ( -0.000000000000000000, 1.000000000000000000, -0.000000000000000000 ) ) ;
#4325=CARTESIAN_POINT ( 'NONE',  ( -148.5561028927606344, -168.9938272943107336, 58.62277379824867296 ) ) ;
#4341=CARTESIAN_POINT ( 'NONE',  ( -151.4692556286852891, -194.3130981290893260, 39.65701158161630246 ) ) ;
#4342=CARTESIAN_POINT ( 'NONE',  ( -143.3790856849358306, -186.6891397928654612, 43.77915905869157598 ) ) ;
#4344=CARTESIAN_POINT ( 'NONE',  ( -145.2889157411863721, -162.5130981290893430, 58.16351966513671812 ) ) ;
#4358=VERTEX_POINT ( 'NONE', #9554 ) ;
#4366=CARTESIAN_POINT ( 'NONE',  ( -148.5561028927606344, -173.7938272943107165, 40.69124936498395328 ) ) ;
#4368=CARTESIAN_POINT ( 'NONE',  ( -157.6495955161842062, -185.0130981290893146, 41.15050349809590102 ) ) ;
#4376=CARTESIAN_POINT ( 'NONE',  ( -161.4692556286853176, -164.4891397928654726, 49.65701158161630957 ) ) ;
#4384=CARTESIAN_POINT ( 'NONE',  ( -141.4692556286852891, -156.9891397928654726, 49.65701158161630957 ) ) ;
#4393=CARTESIAN_POINT ( 'NONE',  ( -141.4692556286852891, -183.2130981290892748, 52.90620854394536821 ) ) ;
#4395=CARTESIAN_POINT ( 'NONE',  ( -157.6495955161842062, -187.1130981290893089, 58.16351966513671812 ) ) ;
#4401=CARTESIAN_POINT ( 'NONE',  ( -160.8964159109769696, -172.7438272943107336, 52.72008163687743121 ) ) ;
#4402=CARTESIAN_POINT ( 'NONE',  ( -145.6429501568359797, -183.2084106276440423, 41.63779006702063867 ) ) ;
#4404=CARTESIAN_POINT ( 'NONE',  ( -159.0959885057557983, -167.4584106276440423, 44.11586579668791330 ) ) ;
#4411=ORIENTED_EDGE ( 'NONE', *, *, #7925, .F. ) ;
#4414=ORIENTED_EDGE ( 'NONE', *, *, #12977, .F. ) ;
#4423=CARTESIAN_POINT ( 'NONE',  ( -148.3790856849358306, -165.3891397928654499, 40.14644641866477315 ) ) ;
#4428=CARTESIAN_POINT ( 'NONE',  ( -142.0420953463936087, -156.3938272943107393, 49.65701158161630957 ) ) ;
#4430=CARTESIAN_POINT ( 'NONE',  ( -142.0420953463935803, -186.5084106276440536, 46.59394152635518793 ) ) ;
#4435=CARTESIAN_POINT ( 'NONE',  ( -156.4692903108300186, -155.9898770414735623, 40.99677756761010272 ) ) ;
#4445=CARTESIAN_POINT ( 'NONE',  ( -142.0420953463936087, -195.3938272943107393, 49.65701158161630957 ) ) ;
#4448=CARTESIAN_POINT ( 'NONE',  ( -161.4692556286852607, -188.6391397928654783, 46.40781461928724383 ) ) ;
#4451=CARTESIAN_POINT ( 'NONE',  ( -142.0420953463936087, -189.3938272943107393, 49.65701158161630957 ) ) ;
#4455=CARTESIAN_POINT ( 'NONE',  ( -157.2955611005346270, -185.3438272943106995, 41.63779006702063867 ) ) ;
#4468=CARTESIAN_POINT ( 'NONE',  ( -161.4692556286853176, -193.5630981290892976, 49.65701158161630957 ) ) ;
#4469=VECTOR ( 'NONE', #6800, 1000.000000000000000 ) ;
#4474=CARTESIAN_POINT ( 'NONE',  ( -157.2955611005345986, -175.4438272943107506, 57.67623309621197336 ) ) ;
#4475=VECTOR ( 'NONE', #16939, 1000.000000000000000 ) ;
#4477=CARTESIAN_POINT ( 'NONE',  ( -141.4692556286852891, -183.0630981290892976, 49.65701158161630957 ) ) ;
#4484=CARTESIAN_POINT ( 'NONE',  ( -145.6429501568359797, -159.2084106276439854, 41.63779006702063867 ) ) ;
#4502=CARTESIAN_POINT ( 'NONE',  ( -143.8425227516148084, -171.3584106276440764, 44.11586579668791330 ) ) ;
#4509=LINE ( 'NONE', #7514, #7635 ) ;
#4514=CARTESIAN_POINT ( 'NONE',  ( -160.8964159109769696, -172.8938272943107393, 49.65701158161630957 ) ) ;
#4515=CARTESIAN_POINT ( 'NONE',  ( -151.4692556286852891, -188.9084106276440593, 39.74470866294723947 ) ) ;
#4516=EDGE_CURVE ( 'NONE', #14601, #19802, #20478, .T. ) ;
#4519=CARTESIAN_POINT ( 'NONE',  ( -145.6429501568359797, -166.1084106276440480, 57.67623309621198047 ) ) ;
#4536=CARTESIAN_POINT ( 'NONE',  ( -148.3790856849358306, -163.5891397928654669, 59.16757674456786020 ) ) ;
#4539=CYLINDRICAL_SURFACE ( 'NONE', #13184, 10.00000000000000888 ) ;
#4543=CARTESIAN_POINT ( 'NONE',  ( -142.0420953463936087, -159.3938272943107393, 49.65701158161630957 ) ) ;
#4546=CARTESIAN_POINT ( 'NONE',  ( -142.0420953463936087, -186.6584106276440309, 49.65701158161630957 ) ) ;
#4556=FACE_OUTER_BOUND ( 'NONE', #10267, .T. ) ;
#4563=CARTESIAN_POINT ( 'NONE',  ( -157.6495955161842062, -191.9391397928654612, 41.15050349809590102 ) ) ;
#4566=CARTESIAN_POINT ( 'NONE',  ( -159.0959885057557983, -193.5938272943107279, 55.19815736654470584 ) ) ;
#4570=CARTESIAN_POINT ( 'NONE',  ( -154.3824083646099439, -185.4938272943107336, 40.69124936498395328 ) ) ;
#4586=CARTESIAN_POINT ( 'NONE',  ( -160.8964159109769696, -160.8938272943107393, 49.65701158161630957 ) ) ;
#4587=CARTESIAN_POINT ( 'NONE',  ( -149.8854112254399240, -166.6622583705451746, 59.65701158161632378 ) ) ;
#4588=CARTESIAN_POINT ( 'NONE',  ( -159.5594255724347761, -175.8630981290893089, 43.77915905869157598 ) ) ;
#4598=CARTESIAN_POINT ( 'NONE',  ( -143.8425227516148084, -159.3584106276440480, 44.11586579668791330 ) ) ;
#4612=EDGE_CURVE ( 'NONE', #18469, #10856, #58, .T. ) ;
#4613=CARTESIAN_POINT ( 'NONE',  ( -159.0959885057557983, -166.8584106276440480, 55.19815736654470584 ) ) ;
#4615=CARTESIAN_POINT ( 'NONE',  ( -151.4692556286852607, -165.8130981290893260, 59.65701158161632378 ) ) ;
#4620=( BOUNDED_CURVE ( )  B_SPLINE_CURVE ( 2, ( #8159, #11782, #20279, #11447, #20177, #3194, #18405, #8052, #1650, #5173, #8271, #15090, #18061 ),
 .UNSPECIFIED., .F., .F. ) 
 B_SPLINE_CURVE_WITH_KNOTS ( ( 3, 2, 2, 2, 2, 2, 3 ),
 ( 0.4107142857142857539, 0.4142857142857143127, 0.4214285714285714302, 0.4285714285714285476, 0.4357142857142857206, 0.4428571428571428381, 0.4464285714285714524 ),
 .UNSPECIFIED. ) 
 CURVE ( )  GEOMETRIC_REPRESENTATION_ITEM ( )  RATIONAL_B_SPLINE_CURVE ( ( 0.9755282581475768211, 0.9755282581475769321, 1.000000000000000000, 0.9510565162951535312, 1.000000000000000000, 0.9510565162951535312, 1.000000000000000000, 0.9510565162951535312, 1.000000000000000000, 0.9510565162951535312, 1.000000000000000000, 0.9755282581475765991, 0.9755282581475768211 ) ) 
 REPRESENTATION_ITEM ( '' )  );
#4625=CARTESIAN_POINT ( 'NONE',  ( -142.0420953463936087, -168.3938272943107393, 49.65701158161630957 ) ) ;
#4626=CARTESIAN_POINT ( 'NONE',  ( -160.8964159109769696, -188.0084106276440252, 52.72008163687743121 ) ) ;
#4629=CARTESIAN_POINT ( 'NONE',  ( -160.8964159109769696, -173.0084106276440821, 52.72008163687743121 ) ) ;
#4650=CARTESIAN_POINT ( 'NONE',  ( -141.4692556286852891, -163.1391397928655067, 52.90620854394536821 ) ) ;
#4657=FACE_OUTER_BOUND ( 'NONE', #17184, .T. ) ;
#4660=CARTESIAN_POINT ( 'NONE',  ( -142.0420953463936087, -192.6584106276440593, 49.65701158161630957 ) ) ;
#4662=CARTESIAN_POINT ( 'NONE',  ( -159.0959885057557983, -181.8584106276440480, 55.19815736654470584 ) ) ;
#4663=ORIENTED_EDGE ( 'NONE', *, *, #15541, .T. ) ;
#4670=CYLINDRICAL_SURFACE ( 'NONE', #231, 10.00000000000000888 ) ;
#4675=CARTESIAN_POINT ( 'NONE',  ( -145.2889157411863721, -190.4391397928654612, 58.16351966513671812 ) ) ;
#4678=CARTESIAN_POINT ( 'NONE',  ( -159.0959885057557983, -191.1938272943107222, 44.11586579668791330 ) ) ;
#4683=CARTESIAN_POINT ( 'NONE',  ( -143.8425227516148084, -180.0938272943107279, 44.11586579668791330 ) ) ;
#4689=EDGE_CURVE ( 'NONE', #20856, #7746, #10501, .T. ) ;
#4694=CARTESIAN_POINT ( 'NONE',  ( -151.4692556286852891, -189.8130981290892976, 59.65701158161632378 ) ) ;
#4697=DIRECTION ( 'NONE',  ( 0.000000000000000000, 0.000000000000000000, -1.000000000000000000 ) ) ;
#4698=CARTESIAN_POINT ( 'NONE',  ( -160.8964159109769696, -164.0438272943107165, 46.59394152635518083 ) ) ;
#4700=CARTESIAN_POINT ( 'NONE',  ( -159.5594255724347761, -175.2630981290893146, 55.53486410454104316 ) ) ;
#4706=DIRECTION ( 'NONE',  ( -0.000000000000000000, 1.000000000000000000, -0.000000000000000000 ) ) ;
#4722=CARTESIAN_POINT ( 'NONE',  ( -143.8425227516148084, -165.9584106276440423, 55.19815736654470584 ) ) ;
#4723=CARTESIAN_POINT ( 'NONE',  ( -143.8425227516148084, -192.6938272943107222, 55.19815736654470584 ) ) ;
#4733=CARTESIAN_POINT ( 'NONE',  ( -148.5561028927606344, -159.9938272943107336, 58.62277379824867296 ) ) ;
#4734=CARTESIAN_POINT ( 'NONE',  ( -157.2955611005345986, -188.6084106276440480, 41.63779006702063867 ) ) ;
#4737=CARTESIAN_POINT ( 'NONE',  ( -157.2955611005346270, -172.7084106276440423, 57.67623309621198047 ) ) ;
#4751=( BOUNDED_CURVE ( )  B_SPLINE_CURVE ( 2, ( #20343, #7114, #8876, #5341, #3172, #13819, #1925, #11955, #4819, #15382, #6899, #18894, #5444 ),
 .UNSPECIFIED., .F., .F. ) 
 B_SPLINE_CURVE_WITH_KNOTS ( ( 3, 2, 2, 2, 2, 2, 3 ),
 ( 0.5892857142857143016, 0.5928571428571428603, 0.5999999999999999778, 0.6071428571428570953, 0.6142857142857143238, 0.6214285714285714413, 0.6250000000000000000 ),
 .UNSPECIFIED. ) 
 CURVE ( )  GEOMETRIC_REPRESENTATION_ITEM ( )  RATIONAL_B_SPLINE_CURVE ( ( 0.9755282581475768211, 0.9755282581475768211, 1.000000000000000000, 0.9510565162951535312, 1.000000000000000000, 0.9510565162951535312, 1.000000000000000000, 0.9510565162951535312, 1.000000000000000000, 0.9510565162951535312, 1.000000000000000000, 0.9755282581475768211, 0.9755282581475768211 ) ) 
 REPRESENTATION_ITEM ( '' )  );
#4762=CARTESIAN_POINT ( 'NONE',  ( -154.3824083646099439, -160.2938272943107449, 58.62277379824867296 ) ) ;
#4764=CARTESIAN_POINT ( 'NONE',  ( -151.4692556286852891, -184.4084106276440593, 59.56931450028537967 ) ) ;
#4766=CARTESIAN_POINT ( 'NONE',  ( -159.5594255724347761, -161.1891397928654897, 55.53486410454104316 ) ) ;
#4774=CARTESIAN_POINT ( 'NONE',  ( -151.4692556286852891, -194.3130981290893260, 39.65701158161630246 ) ) ;
#4783=CARTESIAN_POINT ( 'NONE',  ( -161.4692556286852891, -176.3391397928654385, 52.90620854394536821 ) ) ;
#4784=CARTESIAN_POINT ( 'NONE',  ( -143.3790856849358306, -180.6891397928654612, 43.77915905869157598 ) ) ;
#4786=CARTESIAN_POINT ( 'NONE',  ( -160.8964159109769696, -193.7438272943106767, 52.72008163687743121 ) ) ;
#4792=CARTESIAN_POINT ( 'NONE',  ( -160.8964159109769696, -182.0438272943107449, 46.59394152635518793 ) ) ;
#4795=ORIENTED_EDGE ( 'NONE', *, *, #7281, .T. ) ;
#4810=CARTESIAN_POINT ( 'NONE',  ( -157.2955611005345986, -160.4438272943106654, 57.67623309621197336 ) ) ;
#4811=CARTESIAN_POINT ( 'NONE',  ( -145.2889157411863437, -166.4391397928654897, 58.16351966513671812 ) ) ;
#4812=CARTESIAN_POINT ( 'NONE',  ( -143.3790856849358306, -173.7630981290892862, 43.77915905869157598 ) ) ;
#4819=CARTESIAN_POINT ( 'NONE',  ( -159.5594255724347761, -170.1891397928654897, 55.53486410454104316 ) ) ;
#4822=( BOUNDED_CURVE ( )  B_SPLINE_CURVE ( 2, ( #19711, #16286, #8142, #14846, #18045, #11321, #3177, #21592, #2951, #13202, #16176, #11430, #7819 ),
 .UNSPECIFIED., .F., .F. ) 
 B_SPLINE_CURVE_WITH_KNOTS ( ( 3, 2, 2, 2, 2, 2, 3 ),
 ( 0.1964285714285714524, 0.2000000000000000111, 0.2071428571428571563, 0.2142857142857142738, 0.2214285714285714191, 0.2285714285714285643, 0.2321428571428571508 ),
 .UNSPECIFIED. ) 
 CURVE ( )  GEOMETRIC_REPRESENTATION_ITEM ( )  RATIONAL_B_SPLINE_CURVE ( ( 0.9755282581475767101, 0.9755282581475768211, 1.000000000000000000, 0.9510565162951535312, 1.000000000000000000, 0.9510565162951535312, 1.000000000000000000, 0.9510565162951535312, 1.000000000000000000, 0.9510565162951535312, 1.000000000000000000, 0.9755282581475765991, 0.9755282581475767101 ) ) 
 REPRESENTATION_ITEM ( '' )  );
#4836=CARTESIAN_POINT ( 'NONE',  ( -159.0959885057557983, -163.8584106276440480, 55.19815736654470584 ) ) ;
#4838=CARTESIAN_POINT ( 'NONE',  ( -151.4692556286852891, -187.1438272943107108, 59.56931450028537256 ) ) ;
#4845=CARTESIAN_POINT ( 'NONE',  ( -159.5594255724347761, -184.2630981290893146, 55.53486410454104316 ) ) ;
#4849=CARTESIAN_POINT ( 'NONE',  ( -159.0959885057557983, -164.1938272943107222, 44.11586579668791330 ) ) ;
#4850=CARTESIAN_POINT ( 'NONE',  ( -157.2955611005345986, -179.6084106276440480, 41.63779006702063867 ) ) ;
#4853=CARTESIAN_POINT ( 'NONE',  ( -160.8964159109769696, -161.1584106276440593, 49.65701158161630957 ) ) ;
#4856=CARTESIAN_POINT ( 'NONE',  ( -141.7556754875394631, -195.8237752102547518, 49.65701158161630957 ) ) ;
#4861=CARTESIAN_POINT ( 'NONE',  ( -151.4692556286852891, -190.7391397928654726, 59.65701158161632378 ) ) ;
#4876=CARTESIAN_POINT ( 'NONE',  ( -161.4692556286852891, -185.6391397928654783, 46.40781461928724383 ) ) ;
#4879=CARTESIAN_POINT ( 'NONE',  ( -143.8425227516148084, -195.3584106276440480, 44.11586579668791330 ) ) ;
#4881=CARTESIAN_POINT ( 'NONE',  ( -142.0420953463936087, -189.6584106276440593, 49.65701158161630957 ) ) ;
#4887=ORIENTED_EDGE ( 'NONE', *, *, #20748, .F. ) ;
#4897=CARTESIAN_POINT ( 'NONE',  ( -156.4692903108300186, -155.9898770414735623, 40.99677756761010272 ) ) ;
#4898=LINE ( 'NONE', #17410, #18597 ) ;
#4900=CARTESIAN_POINT ( 'NONE',  ( -154.5594255724347761, -177.0891397928654669, 40.14644641866476604 ) ) ;
#4904=CARTESIAN_POINT ( 'NONE',  ( -148.5561028927606344, -189.9938272943107336, 58.62277379824867296 ) ) ;
#4909=CARTESIAN_POINT ( 'NONE',  ( -142.0420953463935803, -186.2438272943107620, 46.59394152635518793 ) ) ;
#4919=ORIENTED_EDGE ( 'NONE', *, *, #21455, .F. ) ;
#4929=CARTESIAN_POINT ( 'NONE',  ( -151.4692556286852891, -166.1438272943107393, 59.56931450028537256 ) ) ;
#4931=CARTESIAN_POINT ( 'NONE',  ( -151.4692556286852891, -177.8130981290892976, 60.17163382399899518 ) ) ;
#4933=CARTESIAN_POINT ( 'NONE',  ( -151.4692556286852607, -170.3130981290892692, 39.65701158161629536 ) ) ;
#4938=CARTESIAN_POINT ( 'NONE',  ( -161.4692556286852891, -182.3391397928654385, 52.90620854394536821 ) ) ;
#4942=CARTESIAN_POINT ( 'NONE',  ( -151.4692556286852891, -196.9891397928655010, 39.65701158161630246 ) ) ;
#4949=CARTESIAN_POINT ( 'NONE',  ( -151.4692556286852891, -196.9891397928655010, 49.65701158161630957 ) ) ;
#4950=CLOSED_SHELL ( 'NONE', ( #10873, #10138, #6282, #13013, #2348, #17992, #15657, #2442, #16692, #12304, #1789, #15809, #15911, #20972, #20534, #19831, #12928, #46, #14237, #12373, #3348, #608, #2059, #18168, #20063, #1976, #21204, #19748, #15670, #15275, #194, #17379, #2473, #17286, #13109, #9879, #17618, #1092, #18235, #6306, #94, #8807, #8836, #6026, #7509 ) ) ;
#4954=CARTESIAN_POINT ( 'NONE',  ( -145.6429501568359797, -172.1084106276439911, 57.67623309621198047 ) ) ;
#4955=CARTESIAN_POINT ( 'NONE',  ( -154.3824083646099439, -194.4938272943107336, 40.69124936498395328 ) ) ;
#4956=CARTESIAN_POINT ( 'NONE',  ( -161.4692556286852891, -166.7130981290893317, 46.40781461928724383 ) ) ;
#4966=CARTESIAN_POINT ( 'NONE',  ( -154.3824083646099439, -179.7584106276440536, 40.69124936498395328 ) ) ;
#4969=CARTESIAN_POINT ( 'NONE',  ( -157.2955611005346270, -164.6084106276440764, 41.63779006702063867 ) ) ;
#4977=VERTEX_POINT ( 'NONE', #20658 ) ;
#4987=CARTESIAN_POINT ( 'NONE',  ( -151.4692556286852607, -171.8130981290892976, 59.65701158161632378 ) ) ;
#4994=CARTESIAN_POINT ( 'NONE',  ( -142.0420953463936087, -183.6584106276440309, 49.65701158161630957 ) ) ;
#4996=CARTESIAN_POINT ( 'NONE',  ( -151.4692556286852891, -175.4084106276440878, 59.56931450028537967 ) ) ;
#4998=AXIS2_PLACEMENT_3D ( 'NONE', #8976, #20982, #7432 ) ;
#5001=CARTESIAN_POINT ( 'NONE',  ( -148.3790856849358306, -160.5891397928654953, 59.16757674456786020 ) ) ;
#5010=EDGE_CURVE ( 'NONE', #8, #4022, #2138, .T. ) ;
#5016=CARTESIAN_POINT ( 'NONE',  ( -154.5594255724347761, -175.8891397928654783, 59.16757674456785310 ) ) ;
#5023=CARTESIAN_POINT ( 'NONE',  ( -145.6429501568359797, -171.8438272943107279, 57.67623309621198047 ) ) ;
#5040=CARTESIAN_POINT ( 'NONE',  ( -142.0420953463935803, -162.5438272943106881, 52.72008163687743831 ) ) ;
#5042=CARTESIAN_POINT ( 'NONE',  ( -151.4692556286852891, -173.3130981290893544, 39.14238933923362396 ) ) ;
#5048=CARTESIAN_POINT ( 'NONE',  ( -151.4692556286852891, -183.2391397928654726, 39.65701158161629536 ) ) ;
#5049=LINE ( 'NONE', #3397, #12237 ) ;
#5056=LINE ( 'NONE', #10130, #4475 ) ;
#5064=CARTESIAN_POINT ( 'NONE',  ( -157.6495955161842062, -194.9391397928654897, 41.15050349809590102 ) ) ;
#5065=CARTESIAN_POINT ( 'NONE',  ( -157.2955611005345986, -193.4438272943106938, 57.67623309621197336 ) ) ;
#5068=CARTESIAN_POINT ( 'NONE',  ( -141.4692556286852891, -174.8391397928654669, 46.40781461928724383 ) ) ;
#5074=CARTESIAN_POINT ( 'NONE',  ( -157.2955611005346270, -164.3438272943107279, 41.63779006702063867 ) ) ;
#5075=CARTESIAN_POINT ( 'NONE',  ( -148.5561028927606344, -177.0584106276440366, 40.69124936498395328 ) ) ;
#5079=CARTESIAN_POINT ( 'NONE',  ( -143.8425227516148084, -159.9584106276440423, 55.19815736654470584 ) ) ;
#5100=ORIENTED_EDGE ( 'NONE', *, *, #20576, .F. ) ;
#5102=CARTESIAN_POINT ( 'NONE',  ( -154.3824083646099439, -188.7584106276440536, 40.69124936498395328 ) ) ;
#5104=CARTESIAN_POINT ( 'NONE',  ( -143.8425227516148084, -177.3584106276440480, 44.11586579668791330 ) ) ;
#5120=CARTESIAN_POINT ( 'NONE',  ( -154.5594255724347761, -183.0891397928654669, 40.14644641866476604 ) ) ;
#5128=CARTESIAN_POINT ( 'NONE',  ( -159.0959885057557983, -169.5938272943107279, 55.19815736654470584 ) ) ;
#5130=CARTESIAN_POINT ( 'NONE',  ( -141.4692556286852891, -195.8391397928654385, 46.40781461928724383 ) ) ;
#5160=CARTESIAN_POINT ( 'NONE',  ( -149.8854112254399240, -168.7362167067690280, 59.65701158161632378 ) ) ;
#5162=CARTESIAN_POINT ( 'NONE',  ( -151.4692556286852891, -196.9891397928655010, 40.65701158161630246 ) ) ;
#5168=CARTESIAN_POINT ( 'NONE',  ( -143.8425227516148084, -156.9584106276440423, 55.19815736654470584 ) ) ;
#5169=CARTESIAN_POINT ( 'NONE',  ( -151.4692556286852891, -188.6438272943107393, 39.74470866294723947 ) ) ;
#5170=CARTESIAN_POINT ( 'NONE',  ( -151.4692556286852891, -178.7391397928654726, 59.65701158161631668 ) ) ;
#5173=CARTESIAN_POINT ( 'NONE',  ( -145.2889157411863437, -176.6130981290892805, 41.15050349809589392 ) ) ;
#5176=CARTESIAN_POINT ( 'NONE',  ( -153.0531000319306827, -185.2362167067690280, 39.65701158161629536 ) ) ;
#5180=CARTESIAN_POINT ( 'NONE',  ( -142.0420953463936087, -162.3938272943107393, 49.65701158161630957 ) ) ;
#5181=CARTESIAN_POINT ( 'NONE',  ( -159.0959885057557983, -173.4584106276440423, 44.11586579668791330 ) ) ;
#5183=CARTESIAN_POINT ( 'NONE',  ( -142.0420953463935803, -162.8084106276440650, 52.72008163687743831 ) ) ;
#5190=B_SPLINE_CURVE_WITH_KNOTS ( 'NONE', 1,
 ( #16725, #6722 ),
 .UNSPECIFIED., .F., .F.,
 ( 2, 2 ),
 ( 0.000000000000000000, 1.000000000000000000 ),
 .UNSPECIFIED. ) ;
#5203=CARTESIAN_POINT ( 'NONE',  ( -141.4692556286852891, -171.0630981290893260, 49.65701158161630957 ) ) ;
#5204=CARTESIAN_POINT ( 'NONE',  ( -157.6495955161842062, -191.0130981290893146, 41.15050349809589392 ) ) ;
#5212=CARTESIAN_POINT ( 'NONE',  ( -160.8964159109769696, -182.1584106276440309, 49.65701158161630957 ) ) ;
#5214=CARTESIAN_POINT ( 'NONE',  ( -157.2955611005346270, -173.6084106276440480, 41.63779006702063867 ) ) ;
#5231=CARTESIAN_POINT ( 'NONE',  ( -159.5594255724347761, -179.1891397928654612, 55.53486410454104316 ) ) ;
#5236=CARTESIAN_POINT ( 'NONE',  ( -160.8964159109769696, -172.8938272943107393, 49.65701158161630957 ) ) ;
#5253=CARTESIAN_POINT ( 'NONE',  ( -154.5594255724347761, -168.9630981290893033, 59.16757674456785310 ) ) ;
#5256=CARTESIAN_POINT ( 'NONE',  ( -154.5594255724347761, -167.1630981290892919, 40.14644641866476604 ) ) ;
#5267=CARTESIAN_POINT ( 'NONE',  ( -149.8854112254399240, -186.7362167067690564, 59.65701158161632378 ) ) ;
#5271=CARTESIAN_POINT ( 'NONE',  ( -151.4692556286852891, -196.9891397928655010, 49.65701158161630957 ) ) ;
#5273=FACE_OUTER_BOUND ( 'NONE', #19908, .T. ) ;
#5278=CARTESIAN_POINT ( 'NONE',  ( -148.5561028927606344, -156.0584106276440650, 40.69124936498395328 ) ) ;
#5279=CARTESIAN_POINT ( 'NONE',  ( -142.0420953463935803, -180.5438272943107165, 52.72008163687743831 ) ) ;
#5283=CARTESIAN_POINT ( 'NONE',  ( -161.4692556286853176, -173.4891397928654726, 49.65701158161630957 ) ) ;
#5289=CARTESIAN_POINT ( 'NONE',  ( -151.4692556286852891, -175.4084106276440593, 59.56931450028537256 ) ) ;
#5295=ORIENTED_EDGE ( 'NONE', *, *, #19202, .F. ) ;
#5298=CARTESIAN_POINT ( 'NONE',  ( -151.4692556286853176, -193.7391397928655010, 59.65701158161632378 ) ) ;
#5313=CARTESIAN_POINT ( 'NONE',  ( -145.6429501568359797, -183.8438272943107563, 57.67623309621198047 ) ) ;
#5316=CARTESIAN_POINT ( 'NONE',  ( -145.6429501568359797, -190.1084106276440195, 57.67623309621198047 ) ) ;
#5318=CARTESIAN_POINT ( 'NONE',  ( -159.0959885057557983, -172.8584106276440764, 55.19815736654470584 ) ) ;
#5332=CARTESIAN_POINT ( 'NONE',  ( -161.4692556286852607, -167.6391397928654783, 46.40781461928724383 ) ) ;
#5339=CARTESIAN_POINT ( 'NONE',  ( -142.0420953463935803, -174.5438272943107449, 52.72008163687743831 ) ) ;
#5341=CARTESIAN_POINT ( 'NONE',  ( -157.6495955161842062, -170.9391397928654328, 41.15050349809589392 ) ) ;
#5342=CARTESIAN_POINT ( 'NONE',  ( -157.6495955161842062, -158.0391397928654271, 58.16351966513671812 ) ) ;
#5346=CARTESIAN_POINT ( 'NONE',  ( -153.0531000319306827, -176.2362167067690280, 39.65701158161630957 ) ) ;
#5355=CYLINDRICAL_SURFACE ( 'NONE', #17479, 10.00000000000000888 ) ;
#5359=CARTESIAN_POINT ( 'NONE',  ( -154.3824083646099439, -155.4938272943107052, 40.69124936498395328 ) ) ;
#5361=CARTESIAN_POINT ( 'NONE',  ( -161.4692556286852607, -169.4130981290893203, 52.90620854394536821 ) ) ;
#5366=CARTESIAN_POINT ( 'NONE',  ( -141.4692556286852891, -183.9891397928654726, 49.65701158161630957 ) ) ;
#5372=CARTESIAN_POINT ( 'NONE',  ( -149.8854112254399240, -156.7362167067690280, 59.65701158161632378 ) ) ;
#5375=CYLINDRICAL_SURFACE ( 'NONE', #20645, 10.00000000000000888 ) ;
#5381=CARTESIAN_POINT ( 'NONE',  ( -143.8425227516148084, -159.3584106276440480, 44.11586579668791330 ) ) ;
#5382=CARTESIAN_POINT ( 'NONE',  ( -160.8964159109769696, -179.0438272943107449, 46.59394152635518083 ) ) ;
#5383=CARTESIAN_POINT ( 'NONE',  ( -149.8854112254399240, -177.3160212151857138, 39.65701158161629536 ) ) ;
#5392=CARTESIAN_POINT ( 'NONE',  ( -151.4692556286852607, -165.8130981290893260, 59.65701158161632378 ) ) ;
#5393=CARTESIAN_POINT ( 'NONE',  ( -148.5561028927606344, -166.2584106276440536, 58.62277379824867296 ) ) ;
#5394=DIRECTION ( 'NONE',  ( -0.000000000000000000, 1.000000000000000000, -0.000000000000000000 ) ) ;
#5398=CARTESIAN_POINT ( 'NONE',  ( -161.4692556286852891, -179.6391397928654783, 46.40781461928724383 ) ) ;
#5408=CARTESIAN_POINT ( 'NONE',  ( -154.5594255724347761, -173.1630981290893203, 40.14644641866476604 ) ) ;
#5412=CARTESIAN_POINT ( 'NONE',  ( -159.0959885057557983, -184.5938272943107279, 55.19815736654470584 ) ) ;
#5415=CARTESIAN_POINT ( 'NONE',  ( -142.0420953463936087, -186.6584106276440309, 49.65701158161630957 ) ) ;
#5423=EDGE_LOOP ( 'NONE', ( #15077, #1825, #19914, #11826 ) ) ;
#5432=CARTESIAN_POINT ( 'NONE',  ( -145.2889157411863721, -166.4391397928654612, 58.16351966513671812 ) ) ;
#5433=CARTESIAN_POINT ( 'NONE',  ( -161.4692556286853176, -181.5630981290892976, 49.65701158161630957 ) ) ;
#5440=CARTESIAN_POINT ( 'NONE',  ( -157.2955611005346270, -178.4438272943107222, 57.67623309621198047 ) ) ;
#5444=CARTESIAN_POINT ( 'NONE',  ( -151.4692556286852607, -169.7391397928654442, 59.65701158161632378 ) ) ;
#5450=ORIENTED_EDGE ( 'NONE', *, *, #15045, .F. ) ;
#5456=CARTESIAN_POINT ( 'NONE',  ( -143.3790856849358306, -192.3630981290893089, 55.53486410454105027 ) ) ;
#5461=CARTESIAN_POINT ( 'NONE',  ( -151.4692556286852891, -171.8130981290893260, 60.17163382399899518 ) ) ;
#5466=CARTESIAN_POINT ( 'NONE',  ( -143.3790856849358306, -184.2891397928654840, 55.53486410454105027 ) ) ;
#5477=CARTESIAN_POINT ( 'NONE',  ( -148.3790856849358306, -171.3891397928654499, 40.14644641866477315 ) ) ;
#5482=CARTESIAN_POINT ( 'NONE',  ( -141.4692556286852891, -195.8391397928654101, 46.40781461928724383 ) ) ;
#5483=CARTESIAN_POINT ( 'NONE',  ( -142.0420953463935803, -180.2438272943107052, 46.59394152635518083 ) ) ;
#5491=CARTESIAN_POINT ( 'NONE',  ( -151.4692556286852891, -187.7391397928655010, 59.65701158161632378 ) ) ;
#5492=CARTESIAN_POINT ( 'NONE',  ( -160.8964159109769696, -167.3084106276440366, 46.59394152635518083 ) ) ;
#5514=CARTESIAN_POINT ( 'NONE',  ( -159.0959885057557983, -179.1938272943107506, 44.11586579668791330 ) ) ;
#5515=CARTESIAN_POINT ( 'NONE',  ( -148.5561028927606344, -195.0584106276440650, 40.69124936498395328 ) ) ;
#5517=CARTESIAN_POINT ( 'NONE',  ( -148.5561028927606344, -181.2584106276440536, 58.62277379824867296 ) ) ;
#5520=ORIENTED_EDGE ( 'NONE', *, *, #11962, .T. ) ;
#5522=FACE_OUTER_BOUND ( 'NONE', #18331, .T. ) ;
#5538=CARTESIAN_POINT ( 'NONE',  ( -151.4692556286852891, -169.7391397928655010, 60.17163382399899518 ) ) ;
#5539=CARTESIAN_POINT ( 'NONE',  ( -159.5594255724347761, -181.8630981290893374, 43.77915905869157598 ) ) ;
#5541=CARTESIAN_POINT ( 'NONE',  ( -159.5594255724347761, -163.2630981290893146, 55.53486410454104316 ) ) ;
#5543=CARTESIAN_POINT ( 'NONE',  ( -159.0959885057557983, -161.1938272943107222, 44.11586579668791330 ) ) ;
#5546=DIRECTION ( 'NONE',  ( -0.000000000000000000, 1.000000000000000000, -0.000000000000000000 ) ) ;
#5557=ORIENTED_EDGE ( 'NONE', *, *, #8655, .F. ) ;
#5559=CARTESIAN_POINT ( 'NONE',  ( -149.8854112254399240, -180.3160212151857138, 39.65701158161629536 ) ) ;
#5568=CARTESIAN_POINT ( 'NONE',  ( -141.4692556286852891, -161.9130981290892919, 46.40781461928724383 ) ) ;
#5572=CARTESIAN_POINT ( 'NONE',  ( -141.4692556286852891, -184.1391397928654783, 52.90620854394536821 ) ) ;
#5578=CARTESIAN_POINT ( 'NONE',  ( -148.3790856849358306, -169.5891397928654669, 59.16757674456786020 ) ) ;
#5585=CARTESIAN_POINT ( 'NONE',  ( -143.9637021292201950, -116.9891397928655010, 62.65701158161630957 ) ) ;
#5589=CARTESIAN_POINT ( 'NONE',  ( -148.5561028927606344, -182.7938272943107449, 40.69124936498395328 ) ) ;
#5591=CARTESIAN_POINT ( 'NONE',  ( -157.6495955161842062, -188.0130981290892862, 41.15050349809590102 ) ) ;
#5593=CARTESIAN_POINT ( 'NONE',  ( -156.4692903108300186, -155.9898770414735623, 40.99677756761010272 ) ) ;
#5599=CARTESIAN_POINT ( 'NONE',  ( -154.3824083646099439, -155.4938272943107052, 40.69124936498395328 ) ) ;
#5600=CARTESIAN_POINT ( 'NONE',  ( -142.0420953463935803, -165.5084106276440252, 46.59394152635518083 ) ) ;
#5602=CARTESIAN_POINT ( 'NONE',  ( -151.4692556286852891, -196.9891397928655010, 49.65701158161630957 ) ) ;
#5627=CARTESIAN_POINT ( 'NONE',  ( -160.8964159109769696, -182.0438272943107449, 46.59394152635518793 ) ) ;
#5652=CARTESIAN_POINT ( 'NONE',  ( -143.3790856849358306, -174.6891397928654612, 43.77915905869157598 ) ) ;
#5655=LINE ( 'NONE', #9085, #6403 ) ;
#5658=CARTESIAN_POINT ( 'NONE',  ( -145.6429501568359797, -164.9438272943106938, 41.63779006702063867 ) ) ;
#5661=CARTESIAN_POINT ( 'NONE',  ( -160.8964159109769696, -194.1584106276440593, 49.65701158161630957 ) ) ;
#5663=CARTESIAN_POINT ( 'NONE',  ( -151.4692556286853176, -174.8130981290893260, 59.65701158161632378 ) ) ;
#5668=CYLINDRICAL_SURFACE ( 'NONE', #8344, 10.00000000000000888 ) ;
#5670=ORIENTED_EDGE ( 'NONE', *, *, #8655, .T. ) ;
#5678=CARTESIAN_POINT ( 'NONE',  ( -151.4692556286852891, -126.9891397928655010, 49.65701158161630957 ) ) ;
#5679=CARTESIAN_POINT ( 'NONE',  ( -145.2889157411863721, -156.5130981290892862, 58.16351966513671812 ) ) ;
#5686=CARTESIAN_POINT ( 'NONE',  ( -154.3824083646099439, -190.2938272943107449, 58.62277379824867296 ) ) ;
#5698=VERTEX_POINT ( 'NONE', #12788 ) ;
#5704=CARTESIAN_POINT ( 'NONE',  ( -159.0959885057557983, -182.1938272943107506, 44.11586579668791330 ) ) ;
#5706=CARTESIAN_POINT ( 'NONE',  ( -141.4692556286852891, -189.0630981290892976, 49.65701158161630957 ) ) ;
#5709=CARTESIAN_POINT ( 'NONE',  ( -156.1828648351502409, -155.3945647575687872, 41.49286807254280518 ) ) ;
#5714=CARTESIAN_POINT ( 'NONE',  ( -159.0959885057557983, -167.4584106276440423, 44.11586579668791330 ) ) ;
#5716=FACE_BOUND ( 'NONE', #17871, .T. ) ;
#5721=( BOUNDED_CURVE ( )  B_SPLINE_CURVE ( 2, ( #13002, #14754, #9920, #19834, #16735, #11336, #3191, #3077, #11560, #21607, #18288, #18058, #8050 ),
 .UNSPECIFIED., .F., .F. ) 
 B_SPLINE_CURVE_WITH_KNOTS ( ( 3, 2, 2, 2, 2, 2, 3 ),
 ( 0.3750000000000000000, 0.3785714285714285587, 0.3857142857142857317, 0.3928571428571428492, 0.4000000000000000222, 0.4071428571428571397, 0.4107142857142857539 ),
 .UNSPECIFIED. ) 
 CURVE ( )  GEOMETRIC_REPRESENTATION_ITEM ( )  RATIONAL_B_SPLINE_CURVE ( ( 0.9755282581475768211, 0.9755282581475768211, 1.000000000000000000, 0.9510565162951535312, 1.000000000000000000, 0.9510565162951535312, 1.000000000000000000, 0.9510565162951535312, 1.000000000000000000, 0.9510565162951535312, 1.000000000000000000, 0.9755282581475765991, 0.9755282581475768211 ) ) 
 REPRESENTATION_ITEM ( '' )  );
#5724=VERTEX_POINT ( 'NONE', #14328 ) ;
#5735=CARTESIAN_POINT ( 'NONE',  ( -161.4692556286852891, -172.4130981290892919, 52.90620854394536821 ) ) ;
#5738=CARTESIAN_POINT ( 'NONE',  ( -142.0420953463936087, -177.3938272943107393, 49.65701158161630957 ) ) ;
#5739=CARTESIAN_POINT ( 'NONE',  ( -157.2955611005345986, -194.6084106276440195, 41.63779006702063867 ) ) ;
#5742=DIRECTION ( 'NONE',  ( -0.000000000000000000, 1.000000000000000000, -0.000000000000000000 ) ) ;
#5756=CARTESIAN_POINT ( 'NONE',  ( -154.5594255724347761, -171.0891397928654669, 40.14644641866476604 ) ) ;
#5763=CARTESIAN_POINT ( 'NONE',  ( -160.8964159109769696, -163.8938272943107393, 49.65701158161630957 ) ) ;
#5766=CARTESIAN_POINT ( 'NONE',  ( -145.6429501568359797, -192.2084106276440139, 41.63779006702063867 ) ) ;
#5767=ORIENTED_EDGE ( 'NONE', *, *, #20576, .T. ) ;
#5772=ORIENTED_EDGE ( 'NONE', *, *, #19850, .T. ) ;
#5778=CARTESIAN_POINT ( 'NONE',  ( -145.2889157411863437, -192.5130981290892862, 58.16351966513671812 ) ) ;
#5783=CARTESIAN_POINT ( 'NONE',  ( -143.3790856849358306, -159.3630981290893089, 55.53486410454105027 ) ) ;
#5798=ORIENTED_EDGE ( 'NONE', *, *, #21582, .T. ) ;
#5799=ORIENTED_EDGE ( 'NONE', *, *, #11278, .F. ) ;
#5805=CARTESIAN_POINT ( 'NONE',  ( -160.8964159109769696, -166.8938272943107393, 49.65701158161630957 ) ) ;
#5807=CARTESIAN_POINT ( 'NONE',  ( -151.4692556286852891, -185.3130981290893260, 39.14238933923362396 ) ) ;
#5815=CARTESIAN_POINT ( 'NONE',  ( -145.6429501568359797, -165.2084106276440139, 41.63779006702063867 ) ) ;
#5824=LINE ( 'NONE', #7174, #20157 ) ;
#5825=ORIENTED_EDGE ( 'NONE', *, *, #18959, .T. ) ;
#5836=CARTESIAN_POINT ( 'NONE',  ( -157.6495955161842062, -188.0130981290892862, 41.15050349809589392 ) ) ;
#5837=DIRECTION ( 'NONE',  ( -0.000000000000000000, 1.000000000000000000, -0.000000000000000000 ) ) ;
#5842=CARTESIAN_POINT ( 'NONE',  ( -159.0959885057557983, -169.5938272943107279, 55.19815736654470584 ) ) ;
#5845=( BOUNDED_CURVE ( )  B_SPLINE_CURVE ( 2, ( #6042, #16068, #11324, #9480, #2521, #4182, #4384, #6146, #14420, #981, #12993, #21485, #7719 ),
 .UNSPECIFIED., .F., .F. ) 
 B_SPLINE_CURVE_WITH_KNOTS ( ( 3, 2, 2, 2, 2, 2, 3 ),
 ( 0.9107142857142856984, 0.9142857142857142572, 0.9214285714285713746, 0.9285714285714286031, 0.9357142857142857206, 0.9428571428571428381, 0.9464285714285713969 ),
 .UNSPECIFIED. ) 
 CURVE ( )  GEOMETRIC_REPRESENTATION_ITEM ( )  RATIONAL_B_SPLINE_CURVE ( ( 0.9755282581475768211, 0.9755282581475768211, 1.000000000000000000, 0.9510565162951535312, 1.000000000000000000, 0.9510565162951535312, 1.000000000000000000, 0.9510565162951535312, 1.000000000000000000, 0.9510565162951535312, 1.000000000000000000, 0.9755282581475768211, 0.9755282581475768211 ) ) 
 REPRESENTATION_ITEM ( '' )  );
#5846=CARTESIAN_POINT ( 'NONE',  ( -154.3824083646099439, -179.7584106276440536, 40.69124936498395328 ) ) ;
#5857=ORIENTED_EDGE ( 'NONE', *, *, #3006, .T. ) ;
#5866=CARTESIAN_POINT ( 'NONE',  ( -151.4692556286852891, -162.2391397928654442, 39.14238933923362396 ) ) ;
#5867=AXIS2_PLACEMENT_3D ( 'NONE', #666, #14104, #10384 ) ;
#5870=CARTESIAN_POINT ( 'NONE',  ( -157.6495955161842062, -163.1130981290893374, 58.16351966513671812 ) ) ;
#5874=CARTESIAN_POINT ( 'NONE',  ( -154.3824083646099439, -190.5584106276440650, 58.62277379824867296 ) ) ;
#5880=FACE_OUTER_BOUND ( 'NONE', #14790, .T. ) ;
#5881=VERTEX_POINT ( 'NONE', #13950 ) ;
#5888=CARTESIAN_POINT ( 'NONE',  ( -141.4692556286852891, -187.1391397928654499, 52.90620854394536821 ) ) ;
#5892=CARTESIAN_POINT ( 'NONE',  ( -159.5594255724347761, -157.8630981290893089, 43.77915905869157598 ) ) ;
#5898=CARTESIAN_POINT ( 'NONE',  ( -148.5561028927606344, -188.7938272943107449, 40.69124936498395328 ) ) ;
#5907=CARTESIAN_POINT ( 'NONE',  ( -151.4692556286852607, -168.2391397928654442, 39.65701158161629536 ) ) ;
#5913=DIRECTION ( 'NONE',  ( -0.000000000000000000, 1.000000000000000000, -0.000000000000000000 ) ) ;
#5917=EDGE_CURVE ( 'NONE', #19660, #2439, #3153, .T. ) ;
#5918=CARTESIAN_POINT ( 'NONE',  ( -142.0420953463935803, -171.5438272943106881, 52.72008163687743831 ) ) ;
#5920=CARTESIAN_POINT ( 'NONE',  ( -148.3790856849358306, -189.6630981290893203, 59.16757674456786020 ) ) ;
#5927=CARTESIAN_POINT ( 'NONE',  ( -157.2955611005345986, -158.6084106276439911, 41.63779006702063867 ) ) ;
#5928=CARTESIAN_POINT ( 'NONE',  ( -161.4692556286852891, -164.6391397928654499, 46.40781461928724383 ) ) ;
#5929=CARTESIAN_POINT ( 'NONE',  ( -151.4692556286852607, -156.2391397928654726, 39.65701158161629536 ) ) ;
#5938=DIRECTION ( 'NONE',  ( -0.000000000000000000, 1.000000000000000000, -0.000000000000000000 ) ) ;
#5944=CARTESIAN_POINT ( 'NONE',  ( -149.8854112254399240, -182.3899795514095672, 39.65701158161629536 ) ) ;
#5951=CARTESIAN_POINT ( 'NONE',  ( -143.8425227516148084, -168.0938272943107563, 44.11586579668791330 ) ) ;
#5952=CARTESIAN_POINT ( 'NONE',  ( -142.0420953463936087, -195.6584106276440593, 49.65701158161630957 ) ) ;
#5955=CARTESIAN_POINT ( 'NONE',  ( -157.2955611005346270, -178.7084106276440139, 57.67623309621198047 ) ) ;
#5973=CARTESIAN_POINT ( 'NONE',  ( -159.5594255724347761, -158.7891397928654555, 43.77915905869157598 ) ) ;
#5974=( BOUNDED_CURVE ( )  B_SPLINE_CURVE ( 2, ( #21124, #2385, #7462, #7359, #20904, #20796, #6008, #9122, #11188, #7689, #12844, #19562, #12737 ),
 .UNSPECIFIED., .F., .F. ) 
 B_SPLINE_CURVE_WITH_KNOTS ( ( 3, 2, 2, 2, 2, 2, 3 ),
 ( 0.7678571428571427937, 0.7714285714285714635, 0.7785714285714285809, 0.7857142857142856984, 0.7928571428571428159, 0.8000000000000000444, 0.8035714285714286031 ),
 .UNSPECIFIED. ) 
 CURVE ( )  GEOMETRIC_REPRESENTATION_ITEM ( )  RATIONAL_B_SPLINE_CURVE ( ( 0.9755282581475768211, 0.9755282581475763770, 1.000000000000000000, 0.9510565162951535312, 1.000000000000000000, 0.9510565162951535312, 1.000000000000000000, 0.9510565162951535312, 1.000000000000000000, 0.9510565162951535312, 1.000000000000000000, 0.9755282581475768211, 0.9755282581475768211 ) ) 
 REPRESENTATION_ITEM ( '' )  );
#5979=ORIENTED_EDGE ( 'NONE', *, *, #16206, .F. ) ;
#5981=CARTESIAN_POINT ( 'NONE',  ( -143.8425227516148084, -165.0938272943107279, 44.11586579668791330 ) ) ;
#5983=CARTESIAN_POINT ( 'NONE',  ( -159.0959885057557983, -194.4584106276440423, 44.11586579668791330 ) ) ;
#5996=CARTESIAN_POINT ( 'NONE',  ( -143.3790856849358306, -193.2891397928654555, 55.53486410454105027 ) ) ;
#5999=CARTESIAN_POINT ( 'NONE',  ( -157.6495955161842062, -158.0130981290893146, 41.15050349809590102 ) ) ;
#6008=CARTESIAN_POINT ( 'NONE',  ( -141.4692556286852891, -162.0630981290892976, 49.65701158161630957 ) ) ;
#6009=EDGE_LOOP ( 'NONE', ( #14956, #2495, #7852, #4411 ) ) ;
#6023=CARTESIAN_POINT ( 'NONE',  ( -160.8964159109769696, -176.0438272943106881, 46.59394152635518083 ) ) ;
#6025=CARTESIAN_POINT ( 'NONE',  ( -161.4692556286852607, -187.7130981290893033, 46.40781461928724383 ) ) ;
#6026=ADVANCED_FACE ( 'NONE', ( #17579 ), #767, .T. ) ;
#6035=AXIS2_PLACEMENT_3D ( 'NONE', #12713, #6092, #9638 ) ;
#6042=CARTESIAN_POINT ( 'NONE',  ( -151.4692556286852607, -157.7391397928654726, 59.65701158161632378 ) ) ;
#6047=AXIS2_PLACEMENT_3D ( 'NONE', #8300, #21748, #1793 ) ;
#6062=CARTESIAN_POINT ( 'NONE',  ( -143.8425227516148084, -171.0938272943107279, 44.11586579668791330 ) ) ;
#6063=CARTESIAN_POINT ( 'NONE',  ( -160.8964159109769696, -185.0084106276440536, 52.72008163687743121 ) ) ;
#6064=EDGE_LOOP ( 'NONE', ( #11495, #7796, #20088, #5857 ) ) ;
#6065=CARTESIAN_POINT ( 'NONE',  ( -142.0420953463935803, -168.8084106276440650, 52.72008163687743831 ) ) ;
#6067=CYLINDRICAL_SURFACE ( 'NONE', #17256, 10.00000000000000888 ) ;
#6071=ORIENTED_EDGE ( 'NONE', *, *, #13052, .F. ) ;
#6074=EDGE_CURVE ( 'NONE', #10182, #4977, #436, .T. ) ;
#6082=CARTESIAN_POINT ( 'NONE',  ( -145.2889157411863721, -160.4391397928654328, 58.16351966513671812 ) ) ;
#6087=CARTESIAN_POINT ( 'NONE',  ( -159.0959885057557983, -158.1938272943107222, 44.11586579668791330 ) ) ;
#6089=CARTESIAN_POINT ( 'NONE',  ( -145.6429501568359797, -195.2084106276440707, 41.63779006702063867 ) ) ;
#6091=CARTESIAN_POINT ( 'NONE',  ( -153.0531000319306827, -160.8160212151857138, 59.65701158161631668 ) ) ;
#6092=DIRECTION ( 'NONE',  ( -0.000000000000000000, 1.000000000000000000, -0.000000000000000000 ) ) ;
#6104=CARTESIAN_POINT ( 'NONE',  ( -148.3790856849358306, -190.5891397928654953, 59.16757674456786020 ) ) ;
#6108=CARTESIAN_POINT ( 'NONE',  ( -142.0420953463935803, -189.5438272943106881, 52.72008163687743831 ) ) ;
#6112=CARTESIAN_POINT ( 'NONE',  ( -160.8964159109769696, -193.8938272943107393, 49.65701158161630957 ) ) ;
#6115=ORIENTED_EDGE ( 'NONE', *, *, #4612, .T. ) ;
#6124=CARTESIAN_POINT ( 'NONE',  ( -157.6495955161842062, -194.0130981290893146, 41.15050349809589392 ) ) ;
#6131=CARTESIAN_POINT ( 'NONE',  ( -143.8425227516148084, -174.0938272943107279, 44.11586579668791330 ) ) ;
#6133=CARTESIAN_POINT ( 'NONE',  ( -145.2889157411863721, -180.5130981290893146, 58.16351966513671812 ) ) ;
#6146=CARTESIAN_POINT ( 'NONE',  ( -141.4692556286852891, -156.8391397928654669, 46.40781461928724383 ) ) ;
#6155=CARTESIAN_POINT ( 'NONE',  ( -145.2889157411863437, -183.5130981290892578, 58.16351966513671812 ) ) ;
#6157=CARTESIAN_POINT ( 'NONE',  ( -153.0531000319306543, -186.8899795514095672, 59.65701158161632378 ) ) ;
#6164=VECTOR ( 'NONE', #20162, 1000.000000000000000 ) ;
#6165=CARTESIAN_POINT ( 'NONE',  ( -148.5561028927606344, -167.7938272943107165, 40.69124936498395328 ) ) ;
#6166=CARTESIAN_POINT ( 'NONE',  ( -142.0420953463936087, -180.6584106276440309, 49.65701158161630957 ) ) ;
#6167=ORIENTED_EDGE ( 'NONE', *, *, #7870, .F. ) ;
#6169=CARTESIAN_POINT ( 'NONE',  ( -154.3824083646099439, -166.5584106276440366, 58.62277379824867296 ) ) ;
#6189=CARTESIAN_POINT ( 'NONE',  ( -157.6495955161842062, -161.9391397928654897, 41.15050349809590102 ) ) ;
#6196=CARTESIAN_POINT ( 'NONE',  ( -142.0420953463935803, -159.5438272943107449, 52.72008163687743831 ) ) ;
#6198=CARTESIAN_POINT ( 'NONE',  ( -154.3824083646099439, -184.5584106276440650, 58.62277379824867296 ) ) ;
#6213=VECTOR ( 'NONE', #13361, 1000.000000000000000 ) ;
#6216=CARTESIAN_POINT ( 'NONE',  ( -141.4692556286852891, -186.8391397928654385, 46.40781461928724383 ) ) ;
#6219=CARTESIAN_POINT ( 'NONE',  ( -160.8964159109769696, -187.7438272943107336, 52.72008163687743121 ) ) ;
#6224=CARTESIAN_POINT ( 'NONE',  ( -160.8964159109769696, -181.7438272943107336, 52.72008163687743121 ) ) ;
#6243=CARTESIAN_POINT ( 'NONE',  ( -154.3824083646099439, -164.4938272943107336, 40.69124936498395328 ) ) ;
#6246=CARTESIAN_POINT ( 'NONE',  ( -148.3790856849358306, -176.4630981290893033, 40.14644641866477315 ) ) ;
#6247=CARTESIAN_POINT ( 'NONE',  ( -151.4692556286852891, -196.9891397928655010, 39.65701158161630246 ) ) ;
#6252=CARTESIAN_POINT ( 'NONE',  ( -157.6495955161842062, -167.0391397928654555, 58.16351966513671812 ) ) ;
#6253=CARTESIAN_POINT ( 'NONE',  ( -148.5561028927606344, -160.2584106276440536, 58.62277379824867296 ) ) ;
#6267=DIRECTION ( 'NONE',  ( 0.000000000000000000, -1.000000000000000000, 0.000000000000000000 ) ) ;
#6269=CARTESIAN_POINT ( 'NONE',  ( -142.0420953463935803, -171.5084106276440536, 46.59394152635518793 ) ) ;
#6273=CARTESIAN_POINT ( 'NONE',  ( -148.3790856849358306, -188.4630981290893317, 40.14644641866477315 ) ) ;
#6279=CARTESIAN_POINT ( 'NONE',  ( -154.3824083646099439, -169.2938272943107165, 58.62277379824867296 ) ) ;
#6280=CARTESIAN_POINT ( 'NONE',  ( -145.6429501568359797, -187.1084106276440480, 57.67623309621197336 ) ) ;
#6282=ADVANCED_FACE ( 'NONE', ( #12072 ), #11862, .T. ) ;
#6283=ORIENTED_EDGE ( 'NONE', *, *, #16598, .F. ) ;
#6285=CARTESIAN_POINT ( 'NONE',  ( -151.4692556286852891, -164.9084106276440593, 39.74470866294723947 ) ) ;
#6290=ORIENTED_EDGE ( 'NONE', *, *, #8145, .F. ) ;
#6294=EDGE_CURVE ( 'NONE', #8663, #19941, #10437, .T. ) ;
#6304=CARTESIAN_POINT ( 'NONE',  ( -141.4692556286852891, -162.9891397928654726, 49.65701158161630957 ) ) ;
#6306=ADVANCED_FACE ( 'NONE', ( #6705 ), #3943, .T. ) ;
#6309=CARTESIAN_POINT ( 'NONE',  ( -154.5594255724347761, -186.0891397928654953, 40.14644641866476604 ) ) ;
#6312=CARTESIAN_POINT ( 'NONE',  ( -159.0959885057557983, -193.8584106276440480, 55.19815736654470584 ) ) ;
#6314=CARTESIAN_POINT ( 'NONE',  ( -160.8964159109769696, -182.3084106276440650, 46.59394152635518793 ) ) ;
#6318=CARTESIAN_POINT ( 'NONE',  ( -141.4692556286852891, -160.1391397928654499, 52.90620854394536821 ) ) ;
#6330=CARTESIAN_POINT ( 'NONE',  ( -141.4692556286852891, -190.1391397928655067, 52.90620854394536821 ) ) ;
#6333=CARTESIAN_POINT ( 'NONE',  ( -145.6429501568359797, -192.8438272943107563, 57.67623309621198047 ) ) ;
#6338=CARTESIAN_POINT ( 'NONE',  ( -151.4692556286852891, -181.1438272943107393, 59.56931450028537967 ) ) ;
#6356=CARTESIAN_POINT ( 'NONE',  ( -151.4692556286852891, -160.1438272943107393, 59.56931450028537256 ) ) ;
#6358=CARTESIAN_POINT ( 'NONE',  ( -141.4692556286852891, -174.2130981290893033, 52.90620854394536821 ) ) ;
#6371=ORIENTED_EDGE ( 'NONE', *, *, #19690, .F. ) ;
#6380=CARTESIAN_POINT ( 'NONE',  ( -142.0420953463935803, -168.8084106276440650, 52.72008163687743831 ) ) ;
#6381=CARTESIAN_POINT ( 'NONE',  ( -145.6429501568359797, -192.8438272943107279, 57.67623309621197336 ) ) ;
#6392=CARTESIAN_POINT ( 'NONE',  ( -151.4692556286852891, -160.1438272943107393, 59.56931450028537967 ) ) ;
#6393=CARTESIAN_POINT ( 'NONE',  ( -159.0959885057557983, -182.4584106276440707, 44.11586579668791330 ) ) ;
#6394=VERTEX_POINT ( 'NONE', #3498 ) ;
#6396=CARTESIAN_POINT ( 'NONE',  ( -148.5561028927606344, -172.2584106276440536, 58.62277379824867296 ) ) ;
#6403=VECTOR ( 'NONE', #10949, 1000.000000000000114 ) ;
#6416=CARTESIAN_POINT ( 'NONE',  ( -149.8854112254399240, -170.3899795514095672, 39.65701158161629536 ) ) ;
#6421=CARTESIAN_POINT ( 'NONE',  ( -154.5594255724347761, -184.8891397928654783, 59.16757674456785310 ) ) ;
#6424=CARTESIAN_POINT ( 'NONE',  ( -148.5561028927606344, -193.2584106276440252, 58.62277379824867296 ) ) ;
#6426=CARTESIAN_POINT ( 'NONE',  ( -145.6429501568359797, -189.2084106276440423, 41.63779006702063867 ) ) ;
#6428=CARTESIAN_POINT ( 'NONE',  ( -161.4692556286852891, -161.6391397928654783, 46.40781461928724383 ) ) ;
#6429=CARTESIAN_POINT ( 'NONE',  ( -151.4692556286852607, -160.7391397928654158, 59.65701158161632378 ) ) ;
#6442=CARTESIAN_POINT ( 'NONE',  ( -141.4692556286852891, -177.9891397928654442, 49.65701158161630957 ) ) ;
#6445=CARTESIAN_POINT ( 'NONE',  ( -143.8425227516148084, -186.6938272943107222, 55.19815736654470584 ) ) ;
#6450=CARTESIAN_POINT ( 'NONE',  ( -160.8964159109769696, -188.0438272943107449, 46.59394152635518793 ) ) ;
#6459=ORIENTED_EDGE ( 'NONE', *, *, #9404, .F. ) ;
#6462=EDGE_CURVE ( 'NONE', #19662, #10404, #12153, .T. ) ;
#6467=CARTESIAN_POINT ( 'NONE',  ( -148.5561028927606344, -159.9938272943107336, 58.62277379824867296 ) ) ;
#6469=CARTESIAN_POINT ( 'NONE',  ( -143.3790856849358306, -182.7630981290893146, 43.77915905869157598 ) ) ;
#6476=CARTESIAN_POINT ( 'NONE',  ( -151.4692556286852891, -181.7391397928654726, 59.65701158161631668 ) ) ;
#6482=DIRECTION ( 'NONE',  ( -0.000000000000000000, 1.000000000000000000, -0.000000000000000000 ) ) ;
#6486=CARTESIAN_POINT ( 'NONE',  ( -141.4692556286852891, -167.9130981290892919, 46.40781461928724383 ) ) ;
#6495=CARTESIAN_POINT ( 'NONE',  ( -142.0420953463935803, -165.5084106276439968, 46.59394152635518793 ) ) ;
#6496=CARTESIAN_POINT ( 'NONE',  ( -159.0959885057557983, -187.5938272943107279, 55.19815736654470584 ) ) ;
#6498=CARTESIAN_POINT ( 'NONE',  ( -158.9748091281504401, -116.9891397928655010, 36.65701158161628115 ) ) ;
#6503=CARTESIAN_POINT ( 'NONE',  ( -159.5594255724347761, -184.8630981290893089, 43.77915905869157598 ) ) ;
#6507=CARTESIAN_POINT ( 'NONE',  ( -159.0959885057557983, -157.5938272943107279, 55.19815736654470584 ) ) ;
#6508=CARTESIAN_POINT ( 'NONE',  ( -160.8964159109769696, -182.1584106276440309, 49.65701158161630957 ) ) ;
#6511=CARTESIAN_POINT ( 'NONE',  ( -154.3824083646099439, -173.7584106276440536, 40.69124936498395328 ) ) ;
#6522=CARTESIAN_POINT ( 'NONE',  ( -166.4803626276155626, -116.9891397928655010, 49.65701158161629536 ) ) ;
#6534=CARTESIAN_POINT ( 'NONE',  ( -151.4692556286852891, -196.9891397928655010, 59.65701158161632378 ) ) ;
#6537=CARTESIAN_POINT ( 'NONE',  ( -143.8425227516148084, -156.6938272943107222, 55.19815736654470584 ) ) ;
#6539=CARTESIAN_POINT ( 'NONE',  ( -148.5561028927606344, -189.0584106276440650, 40.69124936498395328 ) ) ;
#6546=EDGE_CURVE ( 'NONE', #19216, #10835, #2369, .T. ) ;
#6550=DIRECTION ( 'NONE',  ( -1.000000000000000000, 0.000000000000000000, -0.000000000000000000 ) ) ;
#6557=CARTESIAN_POINT ( 'NONE',  ( -157.6495955161842062, -182.0391397928654840, 58.16351966513671812 ) ) ;
#6559=DIRECTION ( 'NONE',  ( 0.000000000000000000, 0.000000000000000000, -1.000000000000000000 ) ) ;
#6561=CARTESIAN_POINT ( 'NONE',  ( -159.0959885057557983, -194.1938272943107222, 44.11586579668791330 ) ) ;
#6568=CARTESIAN_POINT ( 'NONE',  ( -160.8964159109769696, -187.8938272943107393, 49.65701158161630957 ) ) ;
#6583=CARTESIAN_POINT ( 'NONE',  ( -153.0531000319306543, -192.8899795514095672, 59.65701158161632378 ) ) ;
#6586=CARTESIAN_POINT ( 'NONE',  ( -155.3247660971250923, -155.7098880568450454, 40.99743995317548695 ) ) ;
#6587=CARTESIAN_POINT ( 'NONE',  ( -151.4692556286852891, -161.6438272943107393, 39.74470866294723947 ) ) ;
#6588=CARTESIAN_POINT ( 'NONE',  ( -141.4692556286852891, -165.8391397928654669, 46.40781461928724383 ) ) ;
#6589=CARTESIAN_POINT ( 'NONE',  ( -161.4692556286853176, -181.5630981290892976, 49.65701158161630957 ) ) ;
#6591=CARTESIAN_POINT ( 'NONE',  ( -159.5594255724347761, -191.7891397928654555, 43.77915905869157598 ) ) ;
#6597=CARTESIAN_POINT ( 'NONE',  ( -161.4692556286852891, -167.3391397928654101, 52.90620854394536821 ) ) ;
#6606=ORIENTED_EDGE ( 'NONE', *, *, #12774, .T. ) ;
#6615=CARTESIAN_POINT ( 'NONE',  ( -151.4692556286852891, -169.4084106276440593, 59.56931450028537967 ) ) ;
#6616=CARTESIAN_POINT ( 'NONE',  ( -142.0420953463935803, -186.2438272943107336, 46.59394152635518083 ) ) ;
#6627=CARTESIAN_POINT ( 'NONE',  ( -157.2955611005346270, -163.4438272943107506, 57.67623309621198047 ) ) ;
#6628=CARTESIAN_POINT ( 'NONE',  ( -145.6429501568359797, -172.1084106276440195, 57.67623309621197336 ) ) ;
#6632=CARTESIAN_POINT ( 'NONE',  ( -159.0959885057557983, -163.8584106276440480, 55.19815736654470584 ) ) ;
#6635=STYLED_ITEM ( 'NONE', ( #992 ), #7211 ) ;
#6636=DIRECTION ( 'NONE',  ( 0.000000000000000000, 0.000000000000000000, 1.000000000000000000 ) ) ;
#6642=CARTESIAN_POINT ( 'NONE',  ( -148.3790856849358306, -193.5891397928654669, 59.16757674456786020 ) ) ;
#6658=ORIENTED_EDGE ( 'NONE', *, *, #19850, .F. ) ;
#6660=CARTESIAN_POINT ( 'NONE',  ( -151.4692556286852891, -184.4084106276440593, 59.56931450028537967 ) ) ;
#6663=CARTESIAN_POINT ( 'NONE',  ( -160.8964159109769696, -179.3084106276440082, 46.59394152635518793 ) ) ;
#6666=CARTESIAN_POINT ( 'NONE',  ( -143.3790856849358306, -159.6891397928654897, 43.77915905869157598 ) ) ;
#6678=CARTESIAN_POINT ( 'NONE',  ( -151.4692556286852891, -196.9891397928655010, 49.65701158161630957 ) ) ;
#6679=CARTESIAN_POINT ( 'NONE',  ( -157.6495955161842062, -179.0391397928654840, 58.16351966513671812 ) ) ;
#6687=CARTESIAN_POINT ( 'NONE',  ( -159.0959885057557983, -173.1938272943107506, 44.11586579668791330 ) ) ;
#6692=CARTESIAN_POINT ( 'NONE',  ( -143.3790856849358306, -189.6891397928654612, 43.77915905869157598 ) ) ;
#6705=FACE_OUTER_BOUND ( 'NONE', #12501, .T. ) ;
#6706=CARTESIAN_POINT ( 'NONE',  ( -159.0959885057557983, -163.5938272943107279, 55.19815736654470584 ) ) ;
#6708=CARTESIAN_POINT ( 'NONE',  ( -159.5594255724347761, -169.8630981290893089, 43.77915905869157598 ) ) ;
#6714=CARTESIAN_POINT ( 'NONE',  ( -153.0531000319306827, -166.8160212151857138, 59.65701158161631668 ) ) ;
#6722=CARTESIAN_POINT ( 'NONE',  ( -141.4692556286852891, -195.9891397928654726, 49.65701158161630957 ) ) ;
#6725=LINE ( 'NONE', #11883, #16156 ) ;
#6730=CARTESIAN_POINT ( 'NONE',  ( -145.6429501568359797, -166.1084106276440480, 57.67623309621198047 ) ) ;
#6731=CARTESIAN_POINT ( 'NONE',  ( -160.8964159109769696, -190.7438272943107336, 52.72008163687743121 ) ) ;
#6732=CARTESIAN_POINT ( 'NONE',  ( -161.4692556286853176, -166.5630981290893260, 49.65701158161630957 ) ) ;
#6734=CARTESIAN_POINT ( 'NONE',  ( -151.4692556286852891, -188.3130981290893260, 39.65701158161629536 ) ) ;
#6741=CARTESIAN_POINT ( 'NONE',  ( -157.2955611005346270, -160.4438272943106654, 57.67623309621198047 ) ) ;
#6742=CARTESIAN_POINT ( 'NONE',  ( -160.8964159109769696, -176.1584106276440309, 49.65701158161630957 ) ) ;
#6745=CARTESIAN_POINT ( 'NONE',  ( -143.8425227516148084, -156.9584106276440423, 55.19815736654470584 ) ) ;
#6750=ORIENTED_EDGE ( 'NONE', *, *, #2230, .F. ) ;
#6767=CARTESIAN_POINT ( 'NONE',  ( -143.8425227516148084, -183.3584106276440480, 44.11586579668791330 ) ) ;
#6769=CARTESIAN_POINT ( 'NONE',  ( -160.8964159109769696, -179.0084106276440252, 52.72008163687743121 ) ) ;
#6774=AXIS2_PLACEMENT_3D ( 'NONE', #15663, #15358, #10290 ) ;
#6790=CARTESIAN_POINT ( 'NONE',  ( -148.3790856849358306, -180.3891397928654783, 40.14644641866477315 ) ) ;
#6791=CARTESIAN_POINT ( 'NONE',  ( -161.4692556286852891, -194.3391397928654669, 52.90620854394536821 ) ) ;
#6796=CARTESIAN_POINT ( 'NONE',  ( -159.0959885057557983, -172.5938272943107279, 55.19815736654470584 ) ) ;
#6798=CARTESIAN_POINT ( 'NONE',  ( -141.4692556286852891, -195.9891397928654726, 49.65701158161630957 ) ) ;
#6800=DIRECTION ( 'NONE',  ( -1.000000000000000000, 0.000000000000000000, -4.622506457652816058E-16 ) ) ;
#6804=VERTEX_POINT ( 'NONE', #3134 ) ;
#6810=CARTESIAN_POINT ( 'NONE',  ( -151.4692556286852891, -196.9891397928655010, 49.65701158161630957 ) ) ;
#6813=CARTESIAN_POINT ( 'NONE',  ( -141.4692556286852891, -174.2130981290893033, 52.90620854394536821 ) ) ;
#6815=CARTESIAN_POINT ( 'NONE',  ( -157.6495955161842062, -170.0130981290892862, 41.15050349809590102 ) ) ;
#6834=CARTESIAN_POINT ( 'NONE',  ( -159.0959885057557983, -160.8584106276440480, 55.19815736654470584 ) ) ;
#6835=CARTESIAN_POINT ( 'NONE',  ( -157.2955611005345986, -191.3438272943106995, 41.63779006702063867 ) ) ;
#6843=CARTESIAN_POINT ( 'NONE',  ( -148.5561028927606344, -164.7938272943107449, 40.69124936498395328 ) ) ;
#6844=CARTESIAN_POINT ( 'NONE',  ( -151.4692556286852891, -173.9084106276440593, 39.74470866294723947 ) ) ;
#6846=CARTESIAN_POINT ( 'NONE',  ( -148.5561028927606344, -159.0584106276440650, 40.69124936498395328 ) ) ;
#6869=CARTESIAN_POINT ( 'NONE',  ( -154.3824083646099439, -182.7584106276440536, 40.69124936498395328 ) ) ;
#6872=CARTESIAN_POINT ( 'NONE',  ( -157.2955611005346270, -176.6084106276440195, 41.63779006702063867 ) ) ;
#6889=CARTESIAN_POINT ( 'NONE',  ( -161.4692556286852607, -179.6391397928654783, 46.40781461928724383 ) ) ;
#6890=CYLINDRICAL_SURFACE ( 'NONE', #8371, 10.00000000000000888 ) ;
#6891=CARTESIAN_POINT ( 'NONE',  ( -153.0531000319306827, -195.1622583705451746, 39.65701158161629536 ) ) ;
#6897=CARTESIAN_POINT ( 'NONE',  ( -157.2955611005346270, -170.3438272943107563, 41.63779006702063867 ) ) ;
#6899=CARTESIAN_POINT ( 'NONE',  ( -154.5594255724347761, -169.8891397928654499, 59.16757674456785310 ) ) ;
#6903=CARTESIAN_POINT ( 'NONE',  ( -148.3790856849358306, -189.3891397928654783, 40.14644641866477315 ) ) ;
#6914=CARTESIAN_POINT ( 'NONE',  ( -155.3247640818417779, -155.4453048272798696, 40.99743929837026002 ) ) ;
#6916=CARTESIAN_POINT ( 'NONE',  ( -141.4692556286852891, -165.2130981290893033, 52.90620854394536821 ) ) ;
#6941=CARTESIAN_POINT ( 'NONE',  ( -157.2955611005346270, -157.7084106276440423, 57.67623309621198047 ) ) ;
#6942=CARTESIAN_POINT ( 'NONE',  ( -160.8964159109769696, -185.0438272943107165, 46.59394152635518083 ) ) ;
#6946=CARTESIAN_POINT ( 'NONE',  ( -159.5594255724347761, -173.7891397928654840, 43.77915905869157598 ) ) ;
#6952=CARTESIAN_POINT ( 'NONE',  ( -142.0420953463935803, -174.8084106276440082, 52.72008163687743831 ) ) ;
#6954=CARTESIAN_POINT ( 'NONE',  ( -159.0959885057557983, -158.4584106276440423, 44.11586579668791330 ) ) ;
#6960=VERTEX_POINT ( 'NONE', #20226 ) ;
#6979=CARTESIAN_POINT ( 'NONE',  ( -148.5561028927606344, -176.7938272943107165, 40.69124936498395328 ) ) ;
#6980=CARTESIAN_POINT ( 'NONE',  ( -151.4692556286852891, -196.9891397928655010, 49.65701158161630957 ) ) ;
#6982=CARTESIAN_POINT ( 'NONE',  ( -142.0420953463935803, -186.8084106276440650, 52.72008163687743831 ) ) ;
#6984=CARTESIAN_POINT ( 'NONE',  ( -142.0420953463935803, -174.8084106276440082, 52.72008163687743831 ) ) ;
#6985=ORIENTED_EDGE ( 'NONE', *, *, #868, .F. ) ;
#6990=ORIENTED_EDGE ( 'NONE', *, *, #9487, .T. ) ;
#7000=CARTESIAN_POINT ( 'NONE',  ( -161.4692556286852607, -173.3391397928654385, 52.90620854394536821 ) ) ;
#7007=CARTESIAN_POINT ( 'NONE',  ( -160.8964159109769696, -170.0438272943107449, 46.59394152635518793 ) ) ;
#7010=CARTESIAN_POINT ( 'NONE',  ( -161.4692556286853176, -158.4891397928654726, 49.65701158161630957 ) ) ;
#7023=DIRECTION ( 'NONE',  ( 0.000000000000000000, -1.000000000000000000, 0.000000000000000000 ) ) ;
#7027=CARTESIAN_POINT ( 'NONE',  ( -143.3790856849358306, -167.7630981290893146, 43.77915905869157598 ) ) ;
#7036=CARTESIAN_POINT ( 'NONE',  ( -141.4692556286852891, -156.2130981290893033, 52.90620854394536821 ) ) ;
#7046=CARTESIAN_POINT ( 'NONE',  ( -155.3247660971248933, -155.7098880568450738, 40.99743995317544432 ) ) ;
#7047=CARTESIAN_POINT ( 'NONE',  ( -151.4692556286852891, -176.6438272943107108, 39.74470866294723947 ) ) ;
#7049=CARTESIAN_POINT ( 'NONE',  ( -161.4692556286852607, -193.4130981290893203, 52.90620854394536821 ) ) ;
#7050=DIRECTION ( 'NONE',  ( 0.000000000000000000, 0.000000000000000000, 1.000000000000000000 ) ) ;
#7059=CARTESIAN_POINT ( 'NONE',  ( -154.3824083646099439, -169.5584106276440366, 58.62277379824867296 ) ) ;
#7067=AXIS2_PLACEMENT_3D ( 'NONE', #18803, #6267, #18054 ) ;
#7068=CARTESIAN_POINT ( 'NONE',  ( -153.0531000319306827, -180.1622583705451746, 39.65701158161629536 ) ) ;
#7072=EDGE_CURVE ( 'NONE', #12353, #16672, #4898, .T. ) ;
#7083=CARTESIAN_POINT ( 'NONE',  ( -154.3824083646099439, -179.4938272943107336, 40.69124936498395328 ) ) ;
#7086=CARTESIAN_POINT ( 'NONE',  ( -142.0420953463935803, -189.5084106276440536, 46.59394152635518793 ) ) ;
#7088=CARTESIAN_POINT ( 'NONE',  ( -154.3824083646099439, -175.5584106276440366, 58.62277379824867296 ) ) ;
#7091=CARTESIAN_POINT ( 'NONE',  ( -143.9637021292202235, -116.9891397928655010, 36.65701158161628825 ) ) ;
#7105=CARTESIAN_POINT ( 'NONE',  ( -143.3790856849358306, -179.7630981290893146, 43.77915905869157598 ) ) ;
#7106=CARTESIAN_POINT ( 'NONE',  ( -148.3790856849358306, -174.3891397928654783, 40.14644641866477315 ) ) ;
#7112=CARTESIAN_POINT ( 'NONE',  ( -154.3824083646099439, -176.4938272943107336, 40.69124936498395328 ) ) ;
#7114=CARTESIAN_POINT ( 'NONE',  ( -153.0531000319306827, -171.1622583705452030, 39.65701158161629536 ) ) ;
#7123=ORIENTED_EDGE ( 'NONE', *, *, #21327, .F. ) ;
#7135=CARTESIAN_POINT ( 'NONE',  ( -157.6495955161842062, -173.0130981290893146, 41.15050349809590102 ) ) ;
#7147=DIRECTION ( 'NONE',  ( 0.000000000000000000, 0.000000000000000000, 1.000000000000000000 ) ) ;
#7152=CARTESIAN_POINT ( 'NONE',  ( -143.3790856849358306, -172.2891397928654840, 55.53486410454105027 ) ) ;
#7156=CARTESIAN_POINT ( 'NONE',  ( -151.4692556286852891, -157.4084106276440593, 59.56931450028537967 ) ) ;
#7157=CARTESIAN_POINT ( 'NONE',  ( -154.3824083646099439, -178.2938272943107165, 58.62277379824867296 ) ) ;
#7161=CARTESIAN_POINT ( 'NONE',  ( -151.4692556286852891, -196.9891397928655010, 39.65701158161630246 ) ) ;
#7168=CARTESIAN_POINT ( 'NONE',  ( -148.5561028927606344, -169.2584106276440536, 58.62277379824867296 ) ) ;
#7174=CARTESIAN_POINT ( 'NONE',  ( -158.9748091281504401, -116.9891397928655010, 36.65701158161628115 ) ) ;
#7189=CARTESIAN_POINT ( 'NONE',  ( -160.8964159109769696, -184.7438272943107052, 52.72008163687743121 ) ) ;
#7190=CARTESIAN_POINT ( 'NONE',  ( -142.0420953463935803, -192.8084106276440366, 52.72008163687743831 ) ) ;
#7193=CARTESIAN_POINT ( 'NONE',  ( -151.4692556286852891, -181.4084106276440025, 59.56931450028537967 ) ) ;
#7201=VERTEX_POINT ( 'NONE', #19186 ) ;
#7203=ORIENTED_EDGE ( 'NONE', *, *, #3264, .T. ) ;
#7211=MANIFOLD_SOLID_BREP ( 'Thread2', #4950 ) ;
#7215=CARTESIAN_POINT ( 'NONE',  ( -143.3790856849358306, -165.6891397928654897, 43.77915905869157598 ) ) ;
#7221=CARTESIAN_POINT ( 'NONE',  ( -154.3824083646099439, -166.2938272943107165, 58.62277379824867296 ) ) ;
#7236=CARTESIAN_POINT ( 'NONE',  ( -145.2889157411863437, -180.5391397928654555, 41.15050349809589392 ) ) ;
#7238=CARTESIAN_POINT ( 'NONE',  ( -153.0531000319306827, -168.8899795514095672, 59.65701158161631668 ) ) ;
#7239=CARTESIAN_POINT ( 'NONE',  ( -143.3790856849358306, -191.7630981290893146, 43.77915905869157598 ) ) ;
#7241=CARTESIAN_POINT ( 'NONE',  ( -142.0420953463935803, -156.2438272943106767, 46.59394152635518083 ) ) ;
#7243=CARTESIAN_POINT ( 'NONE',  ( -143.3790856849358306, -158.7630981290893146, 43.77915905869157598 ) ) ;
#7250=CARTESIAN_POINT ( 'NONE',  ( -141.4692556286852891, -183.8391397928654669, 46.40781461928724383 ) ) ;
#7266=CARTESIAN_POINT ( 'NONE',  ( -160.8964159109769696, -184.7438272943107052, 52.72008163687743121 ) ) ;
#7277=CARTESIAN_POINT ( 'NONE',  ( -157.2955611005345986, -161.6084106276440480, 41.63779006702063867 ) ) ;
#7278=CARTESIAN_POINT ( 'NONE',  ( -161.4692556286852891, -164.3391397928654385, 52.90620854394536821 ) ) ;
#7281=EDGE_CURVE ( 'NONE', #21028, #12248, #64, .T. ) ;
#7288=CARTESIAN_POINT ( 'NONE',  ( -159.5594255724347761, -160.8630981290893089, 43.77915905869157598 ) ) ;
#7303=CARTESIAN_POINT ( 'NONE',  ( -148.5561028927606344, -180.9938272943107336, 58.62277379824867296 ) ) ;
#7304=CARTESIAN_POINT ( 'NONE',  ( -160.8964159109769696, -191.0084106276440536, 52.72008163687743121 ) ) ;
#7307=CARTESIAN_POINT ( 'NONE',  ( -160.8964159109769696, -176.1584106276440309, 49.65701158161630957 ) ) ;
#7324=CARTESIAN_POINT ( 'NONE',  ( -151.4692556286852891, -196.9891397928655010, 49.65701158161630957 ) ) ;
#7325=CARTESIAN_POINT ( 'NONE',  ( -154.5594255724347761, -174.0891397928654669, 40.14644641866476604 ) ) ;
#7332=CARTESIAN_POINT ( 'NONE',  ( -154.3824083646099439, -167.4938272943107336, 40.69124936498395328 ) ) ;
#7344=ORIENTED_EDGE ( 'NONE', *, *, #16894, .T. ) ;
#7347=CARTESIAN_POINT ( 'NONE',  ( -148.3790856849358306, -194.4630981290893317, 40.14644641866477315 ) ) ;
#7351=CARTESIAN_POINT ( 'NONE',  ( -159.5594255724347761, -163.2630981290893146, 55.53486410454104316 ) ) ;
#7353=LINE ( 'NONE', #12405, #1923 ) ;
#7357=CARTESIAN_POINT ( 'NONE',  ( -160.8964159109769696, -190.8938272943107393, 49.65701158161630957 ) ) ;
#7359=CARTESIAN_POINT ( 'NONE',  ( -145.2889157411863437, -162.5130981290893430, 58.16351966513671812 ) ) ;
#7367=EDGE_LOOP ( 'NONE', ( #546, #20132, #4048, #6071, #17857, #3320, #12825, #9669, #6290, #1145, #17255, #14311, #897, #16422, #7903, #18191, #16039, #19712, #14097, #5799, #794, #7503, #11549, #17880, #6985, #242, #2906, #11708, #17859, #8389, #13474 ) ) ;
#7371=CARTESIAN_POINT ( 'NONE',  ( -149.8854112254399240, -171.3160212151857138, 39.65701158161629536 ) ) ;
#7375=CARTESIAN_POINT ( 'NONE',  ( -142.0420953463936087, -180.3938272943107108, 49.65701158161630957 ) ) ;
#7377=CARTESIAN_POINT ( 'NONE',  ( -154.5594255724347761, -191.1630981290893203, 40.14644641866476604 ) ) ;
#7380=CARTESIAN_POINT ( 'NONE',  ( -149.8854112254399240, -162.3160212151857138, 39.65701158161629536 ) ) ;
#7386=CARTESIAN_POINT ( 'NONE',  ( -143.8425227516148084, -156.6938272943107222, 55.19815736654470584 ) ) ;
#7387=CARTESIAN_POINT ( 'NONE',  ( -154.3824083646099439, -163.5584106276440366, 58.62277379824867296 ) ) ;
#7390=PLANE ( 'NONE',  #20158 ) ;
#7395=CARTESIAN_POINT ( 'NONE',  ( -157.6495955161842062, -179.0391397928654840, 58.16351966513671812 ) ) ;
#7404=CARTESIAN_POINT ( 'NONE',  ( -159.5594255724347761, -157.2630981290893146, 55.53486410454104316 ) ) ;
#7409=CARTESIAN_POINT ( 'NONE',  ( -157.2955611005346270, -179.3438272943107279, 41.63779006702063867 ) ) ;
#7410=CARTESIAN_POINT ( 'NONE',  ( -143.8425227516148084, -189.9584106276440423, 55.19815736654470584 ) ) ;
#7413=CARTESIAN_POINT ( 'NONE',  ( -145.6429501568359797, -175.1084106276440480, 57.67623309621198047 ) ) ;
#7417=( GEOMETRIC_REPRESENTATION_CONTEXT ( 3 ) GLOBAL_UNCERTAINTY_ASSIGNED_CONTEXT ( ( #3112 ) ) GLOBAL_UNIT_ASSIGNED_CONTEXT ( ( #15176, #3388, #11536 ) ) REPRESENTATION_CONTEXT ( 'NONE', 'WORKASPACE' ) );
#7429=CARTESIAN_POINT ( 'NONE',  ( -157.6495955161842062, -170.0391397928654840, 58.16351966513671812 ) ) ;
#7430=CARTESIAN_POINT ( 'NONE',  ( -141.4692556286852891, -158.9130981290892919, 46.40781461928724383 ) ) ;
#7432=DIRECTION ( 'NONE',  ( -0.5000000000000003331, 0.000000000000000000, 0.8660254037844384856 ) ) ;
#7435=CARTESIAN_POINT ( 'NONE',  ( -145.6429501568359797, -167.9438272943107506, 41.63779006702063867 ) ) ;
#7438=CARTESIAN_POINT ( 'NONE',  ( -142.0420953463936087, -192.6584106276440593, 49.65701158161630957 ) ) ;
#7456=CARTESIAN_POINT ( 'NONE',  ( -157.6495955161842062, -161.0130981290893146, 41.15050349809590102 ) ) ;
#7460=CARTESIAN_POINT ( 'NONE',  ( -142.0420953463935803, -189.5438272943106881, 52.72008163687743831 ) ) ;
#7462=CARTESIAN_POINT ( 'NONE',  ( -148.3790856849358306, -162.6630981290892919, 59.16757674456786020 ) ) ;
#7482=CARTESIAN_POINT ( 'NONE',  ( -157.2955611005345986, -167.3438272943107279, 41.63779006702063867 ) ) ;
#7484=CARTESIAN_POINT ( 'NONE',  ( -161.4692556286852607, -187.4130981290893203, 52.90620854394536821 ) ) ;
#7487=CARTESIAN_POINT ( 'NONE',  ( -141.4692556286852891, -162.8391397928654101, 46.40781461928724383 ) ) ;
#7493=CARTESIAN_POINT ( 'NONE',  ( -148.5561028927606344, -163.2584106276440536, 58.62277379824867296 ) ) ;
#7495=DIRECTION ( 'NONE',  ( 0.000000000000000000, 0.000000000000000000, -1.000000000000000000 ) ) ;
#7503=ORIENTED_EDGE ( 'NONE', *, *, #12229, .F. ) ;
#7509=ADVANCED_FACE ( 'NONE', ( #3524 ), #2306, .T. ) ;
#7512=CARTESIAN_POINT ( 'NONE',  ( -141.4692556286852891, -183.0630981290892976, 49.65701158161630957 ) ) ;
#7513=CARTESIAN_POINT ( 'NONE',  ( -151.4692556286852891, -192.8130981290892692, 59.65701158161632378 ) ) ;
#7514=CARTESIAN_POINT ( 'NONE',  ( -151.4692556286852891, -196.9891397928655010, 59.65701158161632378 ) ) ;
#7517=CARTESIAN_POINT ( 'NONE',  ( -159.0959885057557983, -170.1938272943107222, 44.11586579668791330 ) ) ;
#7518=CARTESIAN_POINT ( 'NONE',  ( -160.8964159109769696, -194.1584106276440593, 49.65701158161630957 ) ) ;
#7520=CARTESIAN_POINT ( 'NONE',  ( -159.0959885057557983, -178.8584106276440480, 55.19815736654470584 ) ) ;
#7522=DIRECTION ( 'NONE',  ( 0.000000000000000000, 0.000000000000000000, 1.000000000000000000 ) ) ;
#7535=DIRECTION ( 'NONE',  ( 0.000000000000000000, -1.000000000000000000, 0.000000000000000000 ) ) ;
#7536=CARTESIAN_POINT ( 'NONE',  ( -157.6495955161842062, -164.0391397928654555, 58.16351966513671812 ) ) ;
#7542=CARTESIAN_POINT ( 'NONE',  ( -151.4692556286853176, -164.3130981290893260, 39.65701158161629536 ) ) ;
#7545=CARTESIAN_POINT ( 'NONE',  ( -143.8425227516148084, -162.0938272943107279, 44.11586579668791330 ) ) ;
#7547=CARTESIAN_POINT ( 'NONE',  ( -159.0959885057557983, -190.8584106276440480, 55.19815736654470584 ) ) ;
#7549=CARTESIAN_POINT ( 'NONE',  ( -157.6495955161842062, -175.1130981290893089, 58.16351966513671812 ) ) ;
#7562=CARTESIAN_POINT ( 'NONE',  ( -148.5561028927606344, -159.0584106276440650, 40.69124936498395328 ) ) ;
#7566=CARTESIAN_POINT ( 'NONE',  ( -145.2889157411863721, -161.6130981290892805, 41.15050349809590102 ) ) ;
#7571=CARTESIAN_POINT ( 'NONE',  ( -142.0420953463936087, -189.3938272943107393, 49.65701158161630957 ) ) ;
#7574=VERTEX_POINT ( 'NONE', #5392 ) ;
#7576=EDGE_CURVE ( 'NONE', #19802, #393, #18076, .T. ) ;
#7584=CARTESIAN_POINT ( 'NONE',  ( -141.4692556286852891, -164.9130981290892919, 46.40781461928724383 ) ) ;
#7591=CARTESIAN_POINT ( 'NONE',  ( -154.3824083646099439, -169.2938272943107165, 58.62277379824867296 ) ) ;
#7593=CARTESIAN_POINT ( 'NONE',  ( -148.3790856849358306, -183.6630981290893203, 59.16757674456786020 ) ) ;
#7600=CARTESIAN_POINT ( 'NONE',  ( -155.3247660971250923, -155.7098880568450454, 40.99743995317548695 ) ) ;
#7619=CARTESIAN_POINT ( 'NONE',  ( -143.3790856849358306, -182.7630981290893146, 43.77915905869157598 ) ) ;
#7627=CARTESIAN_POINT ( 'NONE',  ( -142.0420953463936087, -174.3938272943107393, 49.65701158161630957 ) ) ;
#7628=FACE_OUTER_BOUND ( 'NONE', #10986, .T. ) ;
#7635=VECTOR ( 'NONE', #11021, 1000.000000000000000 ) ;
#7636=ORIENTED_EDGE ( 'NONE', *, *, #1349, .F. ) ;
#7641=VERTEX_POINT ( 'NONE', #1187 ) ;
#7652=CARTESIAN_POINT ( 'NONE',  ( -154.5594255724347761, -165.0891397928654669, 40.14644641866476604 ) ) ;
#7660=CARTESIAN_POINT ( 'NONE',  ( -142.0420953463935803, -165.5438272943107165, 52.72008163687743831 ) ) ;
#7662=CARTESIAN_POINT ( 'NONE',  ( -160.8964159109769696, -194.3084106276440366, 46.59394152635518793 ) ) ;
#7663=ORIENTED_EDGE ( 'NONE', *, *, #21455, .T. ) ;
#7664=DIRECTION ( 'NONE',  ( 0.000000000000000000, 0.000000000000000000, 1.000000000000000000 ) ) ;
#7669=LINE ( 'NONE', #17347, #3423 ) ;
#7677=CARTESIAN_POINT ( 'NONE',  ( -154.5594255724347761, -193.8891397928654783, 59.16757674456785310 ) ) ;
#7681=CARTESIAN_POINT ( 'NONE',  ( -161.4692556286852607, -160.4130981290893203, 52.90620854394536821 ) ) ;
#7686=CARTESIAN_POINT ( 'NONE',  ( -157.2955611005346270, -193.4438272943106938, 57.67623309621198047 ) ) ;
#7689=CARTESIAN_POINT ( 'NONE',  ( -145.2889157411863437, -161.6130981290892805, 41.15050349809589392 ) ) ;
#7691=CARTESIAN_POINT ( 'NONE',  ( -151.4692556286853176, -165.2391397928654442, 39.65701158161629536 ) ) ;
#7703=CARTESIAN_POINT ( 'NONE',  ( -159.0959885057557983, -167.1938272943107222, 44.11586579668791330 ) ) ;
#7705=CARTESIAN_POINT ( 'NONE',  ( -161.4692556286853176, -187.5630981290892976, 49.65701158161630957 ) ) ;
#7707=CARTESIAN_POINT ( 'NONE',  ( -143.3790856849358306, -163.2891397928654555, 55.53486410454105027 ) ) ;
#7719=CARTESIAN_POINT ( 'NONE',  ( -151.4692556286852607, -156.2391397928654726, 39.65701158161629536 ) ) ;
#7728=CARTESIAN_POINT ( 'NONE',  ( -157.6495955161842062, -157.1130981290892805, 58.16351966513671812 ) ) ;
#7730=CARTESIAN_POINT ( 'NONE',  ( -159.5594255724347761, -187.2630981290893146, 55.53486410454104316 ) ) ;
#7731=CARTESIAN_POINT ( 'NONE',  ( -151.4692556286852891, -196.9891397928655010, 58.65701158161631668 ) ) ;
#7736=CARTESIAN_POINT ( 'NONE',  ( -160.8964159109769696, -167.0438272943106881, 46.59394152635518793 ) ) ;
#7737=CARTESIAN_POINT ( 'NONE',  ( -148.5561028927606344, -187.2584106276440536, 58.62277379824867296 ) ) ;
#7739=CARTESIAN_POINT ( 'NONE',  ( -148.5561028927606344, -171.0584106276440366, 40.69124936498395328 ) ) ;
#7741=FACE_OUTER_BOUND ( 'NONE', #15729, .T. ) ;
#7746=VERTEX_POINT ( 'NONE', #16059 ) ;
#7747=VECTOR ( 'NONE', #17136, 1000.000000000000000 ) ;
#7752=DIRECTION ( 'NONE',  ( 0.000000000000000000, 0.000000000000000000, -1.000000000000000000 ) ) ;
#7757=CARTESIAN_POINT ( 'NONE',  ( -151.4692556286852891, -156.2391397928654442, 39.14238933923362396 ) ) ;
#7762=ORIENTED_EDGE ( 'NONE', *, *, #6462, .T. ) ;
#7764=CARTESIAN_POINT ( 'NONE',  ( -154.3824083646099439, -194.7584106276440536, 40.69124936498395328 ) ) ;
#7780=CARTESIAN_POINT ( 'NONE',  ( -157.6495955161842062, -185.9391397928654897, 41.15050349809590102 ) ) ;
#7783=CARTESIAN_POINT ( 'NONE',  ( -151.4692556286852891, -191.6438272943107108, 39.74470866294723947 ) ) ;
#7787=CARTESIAN_POINT ( 'NONE',  ( -151.4692556286852891, -194.6438272943107393, 39.74470866294723947 ) ) ;
#7796=ORIENTED_EDGE ( 'NONE', *, *, #12774, .F. ) ;
#7797=ORIENTED_EDGE ( 'NONE', *, *, #21316, .T. ) ;
#7799=CARTESIAN_POINT ( 'NONE',  ( -151.4692556286852891, -194.3130981290893260, 39.65701158161630246 ) ) ;
#7804=CARTESIAN_POINT ( 'NONE',  ( -159.0959885057557983, -176.1938272943107506, 44.11586579668791330 ) ) ;
#7806=CARTESIAN_POINT ( 'NONE',  ( -143.3790856849358306, -191.7630981290893146, 43.77915905869157598 ) ) ;
#7819=CARTESIAN_POINT ( 'NONE',  ( -151.4692556286852891, -186.2391397928655010, 39.65701158161630246 ) ) ;
#7828=VECTOR ( 'NONE', #5394, 1000.000000000000000 ) ;
#7834=CARTESIAN_POINT ( 'NONE',  ( -148.3790856849358306, -182.4630981290893033, 40.14644641866477315 ) ) ;
#7837=CARTESIAN_POINT ( 'NONE',  ( -161.4692556286852891, -190.4130981290892919, 52.90620854394536821 ) ) ;
#7842=CARTESIAN_POINT ( 'NONE',  ( -145.6429501568359797, -168.8438272943107563, 57.67623309621198047 ) ) ;
#7843=CARTESIAN_POINT ( 'NONE',  ( -160.8964159109769696, -182.3084106276440650, 46.59394152635518083 ) ) ;
#7844=ORIENTED_EDGE ( 'NONE', *, *, #10163, .F. ) ;
#7846=CARTESIAN_POINT ( 'NONE',  ( -148.5561028927606344, -169.2584106276440536, 58.62277379824867296 ) ) ;
#7848=DIRECTION ( 'NONE',  ( -0.8660254037844383745, 0.000000000000000000, 0.5000000000000004441 ) ) ;
#7851=ORIENTED_EDGE ( 'NONE', *, *, #15967, .T. ) ;
#7852=ORIENTED_EDGE ( 'NONE', *, *, #905, .T. ) ;
#7854=ORIENTED_EDGE ( 'NONE', *, *, #12229, .T. ) ;
#7859=( BOUNDED_CURVE ( )  B_SPLINE_CURVE ( 2, ( #3945, #12423, #15517, #420, #7152, #10672, #17375, #13855, #15731, #635, #5477, #7371, #12203 ),
 .UNSPECIFIED., .F., .F. ) 
 B_SPLINE_CURVE_WITH_KNOTS ( ( 3, 2, 2, 2, 2, 2, 3 ),
 ( 0.5535714285714286031, 0.5571428571428571619, 0.5642857142857142794, 0.5714285714285713969, 0.5785714285714286254, 0.5857142857142857428, 0.5892857142857143016 ),
 .UNSPECIFIED. ) 
 CURVE ( )  GEOMETRIC_REPRESENTATION_ITEM ( )  RATIONAL_B_SPLINE_CURVE ( ( 0.9755282581475768211, 0.9755282581475768211, 1.000000000000000000, 0.9510565162951535312, 1.000000000000000000, 0.9510565162951535312, 1.000000000000000000, 0.9510565162951535312, 1.000000000000000000, 0.9510565162951535312, 1.000000000000000000, 0.9755282581475768211, 0.9755282581475768211 ) ) 
 REPRESENTATION_ITEM ( '' )  );
#7864=CARTESIAN_POINT ( 'NONE',  ( -143.3790856849358306, -162.6891397928654897, 43.77915905869157598 ) ) ;
#7866=CARTESIAN_POINT ( 'NONE',  ( -161.4692556286853176, -185.4891397928654726, 49.65701158161630957 ) ) ;
#7867=ORIENTED_EDGE ( 'NONE', *, *, #10504, .T. ) ;
#7869=CARTESIAN_POINT ( 'NONE',  ( -154.3824083646099439, -193.5584106276440650, 58.62277379824867296 ) ) ;
#7870=EDGE_CURVE ( 'NONE', #14442, #14572, #13089, .T. ) ;
#7872=CARTESIAN_POINT ( 'NONE',  ( -142.0420953463935803, -186.8084106276440650, 52.72008163687743831 ) ) ;
#7874=CARTESIAN_POINT ( 'NONE',  ( -157.6495955161842062, -161.9391397928654897, 41.15050349809589392 ) ) ;
#7878=ORIENTED_EDGE ( 'NONE', *, *, #16764, .F. ) ;
#7886=CARTESIAN_POINT ( 'NONE',  ( -151.4692556286852891, -177.2391397928654442, 39.65701158161629536 ) ) ;
#7887=CARTESIAN_POINT ( 'NONE',  ( -145.2889157411863721, -193.4391397928654328, 58.16351966513671812 ) ) ;
#7890=CARTESIAN_POINT ( 'NONE',  ( -154.3824083646099439, -187.2938272943107449, 58.62277379824867296 ) ) ;
#7895=CARTESIAN_POINT ( 'NONE',  ( -160.8964159109769696, -181.8938272943107108, 49.65701158161630957 ) ) ;
#7903=ORIENTED_EDGE ( 'NONE', *, *, #18515, .F. ) ;
#7908=EDGE_CURVE ( 'NONE', #16205, #2985, #16528, .T. ) ;
#7909=EDGE_CURVE ( 'NONE', #13720, #2548, #21474, .T. ) ;
#7913=CARTESIAN_POINT ( 'NONE',  ( -148.5561028927606344, -167.7938272943107165, 40.69124936498395328 ) ) ;
#7915=CARTESIAN_POINT ( 'NONE',  ( -143.3790856849358306, -179.7630981290893146, 43.77915905869157598 ) ) ;
#7921=CARTESIAN_POINT ( 'NONE',  ( -160.8964159109769696, -158.3084106276440650, 46.59394152635518083 ) ) ;
#7925=EDGE_CURVE ( 'NONE', #2439, #17969, #18798, .T. ) ;
#7936=CARTESIAN_POINT ( 'NONE',  ( -157.2955611005346270, -163.7084106276440139, 57.67623309621198047 ) ) ;
#7940=CARTESIAN_POINT ( 'NONE',  ( -154.5594255724347761, -188.1630981290893203, 40.14644641866476604 ) ) ;
#7941=LINE ( 'NONE', #9600, #10806 ) ;
#7948=CARTESIAN_POINT ( 'NONE',  ( -145.6429501568359797, -171.8438272943107279, 57.67623309621198047 ) ) ;
#7949=CARTESIAN_POINT ( 'NONE',  ( -157.2955611005345986, -187.7084106276440139, 57.67623309621197336 ) ) ;
#7952=CARTESIAN_POINT ( 'NONE',  ( -143.8425227516148084, -165.3584106276440480, 44.11586579668791330 ) ) ;
#7969=CARTESIAN_POINT ( 'NONE',  ( -141.4692556286852891, -159.8391397928654385, 46.40781461928724383 ) ) ;
#7976=CARTESIAN_POINT ( 'NONE',  ( -145.6429501568359797, -192.2084106276440139, 41.63779006702063867 ) ) ;
#7978=CARTESIAN_POINT ( 'NONE',  ( -148.5561028927606344, -184.2584106276440536, 58.62277379824867296 ) ) ;
#7997=CARTESIAN_POINT ( 'NONE',  ( -143.3790856849358306, -189.6891397928654612, 43.77915905869157598 ) ) ;
#8000=CARTESIAN_POINT ( 'NONE',  ( -159.0959885057557983, -187.5938272943107279, 55.19815736654470584 ) ) ;
#8005=CARTESIAN_POINT ( 'NONE',  ( -143.8425227516148084, -183.0938272943107279, 44.11586579668791330 ) ) ;
#8023=CARTESIAN_POINT ( 'NONE',  ( -160.8964159109769696, -160.7438272943107336, 52.72008163687743121 ) ) ;
#8026=CARTESIAN_POINT ( 'NONE',  ( -151.4692556286852891, -174.8130981290892976, 60.17163382399899518 ) ) ;
#8031=CARTESIAN_POINT ( 'NONE',  ( -154.5594255724347761, -168.0891397928654669, 40.14644641866476604 ) ) ;
#8032=CARTESIAN_POINT ( 'NONE',  ( -154.3824083646099439, -160.5584106276440366, 58.62277379824867296 ) ) ;
#8048=CARTESIAN_POINT ( 'NONE',  ( -157.2955611005346270, -167.6084106276440480, 41.63779006702063867 ) ) ;
#8049=CARTESIAN_POINT ( 'NONE',  ( -145.6429501568359797, -194.9438272943107222, 41.63779006702063867 ) ) ;
#8050=CARTESIAN_POINT ( 'NONE',  ( -151.4692556286852891, -177.8130981290892976, 59.65701158161631668 ) ) ;
#8052=CARTESIAN_POINT ( 'NONE',  ( -141.4692556286852891, -176.9130981290892635, 46.40781461928724383 ) ) ;
#8054=CARTESIAN_POINT ( 'NONE',  ( -151.4692556286852607, -159.8130981290892692, 59.65701158161632378 ) ) ;
#8056=CARTESIAN_POINT ( 'NONE',  ( -142.0420953463935803, -162.2438272943107336, 46.59394152635518793 ) ) ;
#8057=CARTESIAN_POINT ( 'NONE',  ( -145.6429501568359797, -189.2084106276440423, 41.63779006702063867 ) ) ;
#8058=ORIENTED_EDGE ( 'NONE', *, *, #11482, .F. ) ;
#8060=CARTESIAN_POINT ( 'NONE',  ( -159.0959885057557983, -170.4584106276440423, 44.11586579668791330 ) ) ;
#8063=PLANE ( 'NONE',  #20780 ) ;
#8082=DIRECTION ( 'NONE',  ( -0.000000000000000000, 1.000000000000000000, -0.000000000000000000 ) ) ;
#8085=CARTESIAN_POINT ( 'NONE',  ( -159.0959885057557983, -194.4584106276440423, 44.11586579668791330 ) ) ;
#8087=CARTESIAN_POINT ( 'NONE',  ( -148.5561028927606344, -181.2584106276440536, 58.62277379824867296 ) ) ;
#8096=CARTESIAN_POINT ( 'NONE',  ( -151.4692556286852607, -155.3130981290892976, 39.65701158161629536 ) ) ;
#8102=CARTESIAN_POINT ( 'NONE',  ( -161.4692556286853176, -182.4891397928654726, 49.65701158161630957 ) ) ;
#8104=CARTESIAN_POINT ( 'NONE',  ( -151.4692556286852607, -172.7391397928654726, 59.65701158161632378 ) ) ;
#8105=CARTESIAN_POINT ( 'NONE',  ( -157.2955611005346270, -190.4438272943107506, 57.67623309621198047 ) ) ;
#8109=CARTESIAN_POINT ( 'NONE',  ( -159.0959885057557983, -179.1938272943107506, 44.11586579668791330 ) ) ;
#8115=( BOUNDED_CURVE ( )  B_SPLINE_CURVE ( 2, ( #11893, #3527, #10252, #208, #6946, #20386, #5283, #20498, #11997, #18730, #17061, #1973, #10470 ),
 .UNSPECIFIED., .F., .T. ) 
 B_SPLINE_CURVE_WITH_KNOTS ( ( 3, 2, 2, 2, 2, 2, 3 ),
 ( 0.5178571428571429047, 0.5214285714285714635, 0.5285714285714285809, 0.5357142857142856984, 0.5428571428571428159, 0.5500000000000000444, 0.5535714285714286031 ),
 .UNSPECIFIED. ) 
 CURVE ( )  GEOMETRIC_REPRESENTATION_ITEM ( )  RATIONAL_B_SPLINE_CURVE ( ( 0.9755282581475768211, 0.9755282581475771542, 1.000000000000000000, 0.9510565162951535312, 1.000000000000000000, 0.9510565162951535312, 1.000000000000000000, 0.9510565162951535312, 1.000000000000000000, 0.9510565162951535312, 1.000000000000000000, 0.9755282581475768211, 0.9755282581475768211 ) ) 
 REPRESENTATION_ITEM ( '' )  );
#8127=CARTESIAN_POINT ( 'NONE',  ( -148.5561028927606344, -156.0584106276440650, 40.69124936498395328 ) ) ;
#8128=CARTESIAN_POINT ( 'NONE',  ( -151.4692556286852891, -158.6438272943107108, 39.74470866294723947 ) ) ;
#8129=CARTESIAN_POINT ( 'NONE',  ( -154.5594255724347761, -182.1630981290893203, 40.14644641866476604 ) ) ;
#8136=CARTESIAN_POINT ( 'NONE',  ( -157.6495955161842062, -182.0391397928654840, 58.16351966513671812 ) ) ;
#8142=CARTESIAN_POINT ( 'NONE',  ( -148.3790856849358306, -187.5891397928654953, 59.16757674456786020 ) ) ;
#8145=EDGE_CURVE ( 'NONE', #18280, #12353, #5974, .T. ) ;
#8153=CARTESIAN_POINT ( 'NONE',  ( -157.2955611005346270, -172.7084106276440423, 57.67623309621198047 ) ) ;
#8154=CARTESIAN_POINT ( 'NONE',  ( -160.8964159109769696, -188.0438272943107449, 46.59394152635518083 ) ) ;
#8155=CARTESIAN_POINT ( 'NONE',  ( -157.6495955161842062, -166.1130981290892805, 58.16351966513671812 ) ) ;
#8159=CARTESIAN_POINT ( 'NONE',  ( -151.4692556286852891, -177.8130981290892976, 59.65701158161631668 ) ) ;
#8162=CARTESIAN_POINT ( 'NONE',  ( -157.6495955161842062, -184.1130981290892521, 58.16351966513671812 ) ) ;
#8165=CARTESIAN_POINT ( 'NONE',  ( -160.8964159109769696, -157.7438272943107336, 52.72008163687743121 ) ) ;
#8166=CARTESIAN_POINT ( 'NONE',  ( -159.0959885057557983, -184.8584106276440480, 55.19815736654470584 ) ) ;
#8168=EDGE_LOOP ( 'NONE', ( #7878, #3342, #6283, #7123 ) ) ;
#8170=CARTESIAN_POINT ( 'NONE',  ( -148.5561028927606344, -174.0584106276440366, 40.69124936498395328 ) ) ;
#8191=CARTESIAN_POINT ( 'NONE',  ( -151.4692556286852891, -196.9891397928655010, 39.65701158161630246 ) ) ;
#8197=CARTESIAN_POINT ( 'NONE',  ( -160.8964159109769696, -158.0438272943107165, 46.59394152635518793 ) ) ;
#8199=CARTESIAN_POINT ( 'NONE',  ( -145.6429501568359797, -183.2084106276440423, 41.63779006702063867 ) ) ;
#8202=CARTESIAN_POINT ( 'NONE',  ( -141.4692556286852891, -159.8391397928654669, 46.40781461928724383 ) ) ;
#8214=DIRECTION ( 'NONE',  ( 1.000000000000000000, 0.000000000000000000, 0.000000000000000000 ) ) ;
#8217=CARTESIAN_POINT ( 'NONE',  ( -151.4692556286852891, -180.2391397928654442, 39.14238933923362396 ) ) ;
#8219=CARTESIAN_POINT ( 'NONE',  ( -151.4692556286852891, -193.1438272943107393, 59.56931450028537967 ) ) ;
#8223=CARTESIAN_POINT ( 'NONE',  ( -160.8964159109769696, -179.0438272943107449, 46.59394152635518793 ) ) ;
#8233=VERTEX_POINT ( 'NONE', #1382 ) ;
#8240=CARTESIAN_POINT ( 'NONE',  ( -157.2955611005345986, -157.4438272943107222, 57.67623309621197336 ) ) ;
#8242=CARTESIAN_POINT ( 'NONE',  ( -151.4692556286852891, -180.8130981290892976, 60.17163382399899518 ) ) ;
#8253=CARTESIAN_POINT ( 'NONE',  ( -141.4692556286852891, -155.9130981290893203, 46.40781461928724383 ) ) ;
#8266=CARTESIAN_POINT ( 'NONE',  ( -160.8964159109769696, -164.0084106276440536, 52.72008163687743121 ) ) ;
#8267=CARTESIAN_POINT ( 'NONE',  ( -142.0420953463935803, -186.5438272943107449, 52.72008163687743831 ) ) ;
#8268=CARTESIAN_POINT ( 'NONE',  ( -154.5594255724347761, -165.9630981290893033, 59.16757674456785310 ) ) ;
#8271=CARTESIAN_POINT ( 'NONE',  ( -148.3790856849358306, -176.4630981290893033, 40.14644641866477315 ) ) ;
#8277=CARTESIAN_POINT ( 'NONE',  ( -151.4692556286852891, -157.1438272943107393, 59.56931450028537967 ) ) ;
#8278=CARTESIAN_POINT ( 'NONE',  ( -143.8425227516148084, -171.3584106276440764, 44.11586579668791330 ) ) ;
#8279=VERTEX_POINT ( 'NONE', #19680 ) ;
#8281=CARTESIAN_POINT ( 'NONE',  ( -142.0420953463936087, -162.6584106276440593, 49.65701158161630957 ) ) ;
#8296=CARTESIAN_POINT ( 'NONE',  ( -148.3790856849358306, -170.4630981290893033, 40.14644641866477315 ) ) ;
#8300=CARTESIAN_POINT ( 'NONE',  ( -151.4692556286852891, -196.9891397928655010, 49.65701158161630957 ) ) ;
#8303=CARTESIAN_POINT ( 'NONE',  ( -160.8964159109769696, -185.0084106276440821, 52.72008163687743121 ) ) ;
#8305=CARTESIAN_POINT ( 'NONE',  ( -151.4692556286852891, -188.9084106276440593, 39.74470866294723947 ) ) ;
#8313=AXIS2_PLACEMENT_3D ( 'NONE', #10086, #15374, #3686 ) ;
#8324=CARTESIAN_POINT ( 'NONE',  ( -159.5594255724347761, -176.1891397928654612, 55.53486410454104316 ) ) ;
#8331=CARTESIAN_POINT ( 'NONE',  ( -160.8964159109769696, -187.7438272943107336, 52.72008163687743121 ) ) ;
#8340=VERTEX_POINT ( 'NONE', #18015 ) ;
#8344=AXIS2_PLACEMENT_3D ( 'NONE', #10960, #496, #9208 ) ;
#8345=CARTESIAN_POINT ( 'NONE',  ( -159.5594255724347761, -193.2630981290893146, 55.53486410454104316 ) ) ;
#8349=CARTESIAN_POINT ( 'NONE',  ( -160.8964159109769696, -163.8938272943107393, 49.65701158161630957 ) ) ;
#8351=CARTESIAN_POINT ( 'NONE',  ( -145.2889157411863721, -177.5130981290893430, 58.16351966513671812 ) ) ;
#8359=CARTESIAN_POINT ( 'NONE',  ( -151.4692556286852607, -166.7391397928654158, 59.65701158161632378 ) ) ;
#8371=AXIS2_PLACEMENT_3D ( 'NONE', #13916, #13812, #20550 ) ;
#8376=CARTESIAN_POINT ( 'NONE',  ( -142.0420953463935803, -168.5084106276440536, 46.59394152635518793 ) ) ;
#8377=CARTESIAN_POINT ( 'NONE',  ( -157.2955611005345986, -190.4438272943107222, 57.67623309621197336 ) ) ;
#8387=CARTESIAN_POINT ( 'NONE',  ( -143.8425227516148084, -162.0938272943107279, 44.11586579668791330 ) ) ;
#8388=CARTESIAN_POINT ( 'NONE',  ( -143.8425227516148084, -174.3584106276440480, 44.11586579668791330 ) ) ;
#8389=ORIENTED_EDGE ( 'NONE', *, *, #21084, .F. ) ;
#8391=CARTESIAN_POINT ( 'NONE',  ( -160.8964159109769696, -158.0084106276440536, 52.72008163687743121 ) ) ;
#8407=DIRECTION ( 'NONE',  ( -0.000000000000000000, 1.000000000000000000, -0.000000000000000000 ) ) ;
#8411=PRODUCT_DEFINITION_CONTEXT ( 'detailed design', #12800, 'design' ) ;
#8414=ORIENTED_EDGE ( 'NONE', *, *, #21322, .F. ) ;
#8416=CARTESIAN_POINT ( 'NONE',  ( -145.6429501568359797, -186.2084106276440707, 41.63779006702063867 ) ) ;
#8418=CARTESIAN_POINT ( 'NONE',  ( -151.4692556286852891, -179.9084106276440593, 39.74470866294723947 ) ) ;
#8426=ORIENTED_EDGE ( 'NONE', *, *, #7072, .F. ) ;
#8436=CARTESIAN_POINT ( 'NONE',  ( -145.2889157411863721, -178.4391397928654044, 58.16351966513671812 ) ) ;
#8448=CARTESIAN_POINT ( 'NONE',  ( -159.0959885057557983, -170.1938272943107222, 44.11586579668791330 ) ) ;
#8464=CARTESIAN_POINT ( 'NONE',  ( -154.5594255724347761, -170.1630981290893203, 40.14644641866476604 ) ) ;
#8465=CARTESIAN_POINT ( 'NONE',  ( -154.3824083646099439, -163.2938272943107449, 58.62277379824867296 ) ) ;
#8467=CARTESIAN_POINT ( 'NONE',  ( -151.4692556286852891, -167.3130981290893260, 39.14238933923362396 ) ) ;
#8472=CARTESIAN_POINT ( 'NONE',  ( -151.4692556286852607, -184.7391397928654726, 59.65701158161632378 ) ) ;
#8486=VECTOR ( 'NONE', #15328, 1000.000000000000000 ) ;
#8490=CARTESIAN_POINT ( 'NONE',  ( -154.3824083646099439, -161.7584106276440252, 40.69124936498395328 ) ) ;
#8491=CARTESIAN_POINT ( 'NONE',  ( -145.6429501568359797, -188.9438272943106938, 41.63779006702063867 ) ) ;
#8499=CARTESIAN_POINT ( 'NONE',  ( -160.8964159109769696, -163.7438272943107336, 52.72008163687743121 ) ) ;
#8500=CARTESIAN_POINT ( 'NONE',  ( -157.2955611005345986, -170.6084106276440480, 41.63779006702063867 ) ) ;
#8503=CARTESIAN_POINT ( 'NONE',  ( -154.3824083646099439, -161.7584106276440252, 40.69124936498395328 ) ) ;
#8508=EDGE_CURVE ( 'NONE', #18977, #14601, #15269, .T. ) ;
#8519=DIRECTION ( 'NONE',  ( 0.000000000000000000, 0.000000000000000000, 1.000000000000000000 ) ) ;
#8520=CARTESIAN_POINT ( 'NONE',  ( -149.8854112254399240, -171.7362167067689995, 59.65701158161632378 ) ) ;
#8528=CARTESIAN_POINT ( 'NONE',  ( -142.0420953463935803, -183.8084106276440366, 52.72008163687743831 ) ) ;
#8530=CARTESIAN_POINT ( 'NONE',  ( -142.0420953463935803, -174.5084106276440252, 46.59394152635518793 ) ) ;
#8547=CARTESIAN_POINT ( 'NONE',  ( -148.3790856849358306, -181.5891397928654669, 59.16757674456786020 ) ) ;
#8550=CARTESIAN_POINT ( 'NONE',  ( -151.4692556286852891, -196.9891397928655010, 39.65701158161630246 ) ) ;
#8555=CARTESIAN_POINT ( 'NONE',  ( -157.2955611005346270, -176.3438272943106710, 41.63779006702063867 ) ) ;
#8563=EDGE_LOOP ( 'NONE', ( #16614, #2, #8414, #952 ) ) ;
#8568=DIRECTION ( 'NONE',  ( 0.000000000000000000, 0.000000000000000000, 1.000000000000000000 ) ) ;
#8573=CARTESIAN_POINT ( 'NONE',  ( -148.3790856849358306, -165.6630981290892919, 59.16757674456786020 ) ) ;
#8591=CARTESIAN_POINT ( 'NONE',  ( -161.4692556286853176, -194.4891397928654726, 49.65701158161630957 ) ) ;
#8592=CARTESIAN_POINT ( 'NONE',  ( -145.6429501568359797, -180.8438272943106995, 57.67623309621197336 ) ) ;
#8594=CARTESIAN_POINT ( 'NONE',  ( -148.3790856849358306, -194.4630981290893317, 40.14644641866477315 ) ) ;
#8598=CARTESIAN_POINT ( 'NONE',  ( -153.0531000319306827, -183.8899795514095672, 59.65701158161631668 ) ) ;
#8601=CARTESIAN_POINT ( 'NONE',  ( -156.1828648351502125, -155.3945647575688156, 41.49286807254280518 ) ) ;
#8602=CARTESIAN_POINT ( 'NONE',  ( -160.8964159109769696, -173.3084106276440366, 46.59394152635518083 ) ) ;
#8604=CARTESIAN_POINT ( 'NONE',  ( -159.0959885057557983, -164.4584106276440423, 44.11586579668791330 ) ) ;
#8607=CARTESIAN_POINT ( 'NONE',  ( -151.4692556286852891, -196.9891397928655010, 59.65701158161632378 ) ) ;
#8609=SHAPE_REPRESENTATION ( 'bolt', ( #12657 ), #7417 ) ;
#8631=CARTESIAN_POINT ( 'NONE',  ( -145.6429501568359797, -184.1084106276440480, 57.67623309621198047 ) ) ;
#8633=CARTESIAN_POINT ( 'NONE',  ( -142.0420953463935803, -180.5084106276440536, 46.59394152635518793 ) ) ;
#8636=FACE_OUTER_BOUND ( 'NONE', #5423, .T. ) ;
#8650=CARTESIAN_POINT ( 'NONE',  ( -143.3790856849358306, -168.6891397928654897, 43.77915905869157598 ) ) ;
#8651=CARTESIAN_POINT ( 'NONE',  ( -153.0531000319306827, -180.8899795514095956, 59.65701158161632378 ) ) ;
#8655=EDGE_CURVE ( 'NONE', #10182, #12281, #10941, .T. ) ;
#8658=CARTESIAN_POINT ( 'NONE',  ( -154.3824083646099439, -170.4938272943107336, 40.69124936498395328 ) ) ;
#8661=CARTESIAN_POINT ( 'NONE',  ( -154.5594255724347761, -159.0891397928654953, 40.14644641866476604 ) ) ;
#8662=AXIS2_PLACEMENT_3D ( 'NONE', #18116, #9763, #16460 ) ;
#8663=VERTEX_POINT ( 'NONE', #1824 ) ;
#8671=CARTESIAN_POINT ( 'NONE',  ( -151.4692556286852891, -180.8130981290893260, 59.65701158161631668 ) ) ;
#8677=CARTESIAN_POINT ( 'NONE',  ( -161.4692556286853176, -172.5630981290893260, 49.65701158161630957 ) ) ;
#8689=CARTESIAN_POINT ( 'NONE',  ( -148.3790856849358306, -185.4630981290893033, 40.14644641866477315 ) ) ;
#8693=EDGE_CURVE ( 'NONE', #16672, #6394, #1930, .T. ) ;
#8702=CARTESIAN_POINT ( 'NONE',  ( -154.3824083646099439, -155.7584106276440536, 40.69124936498395328 ) ) ;
#8703=CARTESIAN_POINT ( 'NONE',  ( -142.0420953463935803, -183.2438272943107336, 46.59394152635518083 ) ) ;
#8704=CARTESIAN_POINT ( 'NONE',  ( -141.4692556286852891, -178.1391397928654499, 52.90620854394536821 ) ) ;
#8714=CARTESIAN_POINT ( 'NONE',  ( -142.0420953463935803, -177.8084106276440366, 52.72008163687743831 ) ) ;
#8737=CARTESIAN_POINT ( 'NONE',  ( -145.6429501568359797, -180.8438272943106995, 57.67623309621198047 ) ) ;
#8741=CARTESIAN_POINT ( 'NONE',  ( -157.2955611005346270, -185.6084106276440195, 41.63779006702063867 ) ) ;
#8743=CARTESIAN_POINT ( 'NONE',  ( -142.0420953463936087, -180.6584106276440309, 49.65701158161630957 ) ) ;
#8744=ORIENTED_EDGE ( 'NONE', *, *, #12977, .T. ) ;
#8758=CARTESIAN_POINT ( 'NONE',  ( -141.4692556286852891, -180.0630981290892976, 49.65701158161630957 ) ) ;
#8759=CARTESIAN_POINT ( 'NONE',  ( -141.4692556286852891, -169.1391397928654214, 52.90620854394536821 ) ) ;
#8761=CARTESIAN_POINT ( 'NONE',  ( -151.4692556286852891, -195.2391397928655010, 39.65701158161629536 ) ) ;
#8767=CARTESIAN_POINT ( 'NONE',  ( -160.8964159109769696, -178.7438272943107052, 52.72008163687743121 ) ) ;
#8770=CARTESIAN_POINT ( 'NONE',  ( -149.8854112254399524, -195.3160212151857422, 39.65701158161630246 ) ) ;
#8781=CARTESIAN_POINT ( 'NONE',  ( -148.3790856849358306, -181.5891397928654669, 59.16757674456786020 ) ) ;
#8783=AXIS2_PLACEMENT_3D ( 'NONE', #4949, #18395, #11658 ) ;
#8788=CARTESIAN_POINT ( 'NONE',  ( -161.4692556286852607, -172.4130981290892635, 52.90620854394536821 ) ) ;
#8800=CARTESIAN_POINT ( 'NONE',  ( -149.8854112254399240, -169.6622583705451746, 59.65701158161632378 ) ) ;
#8802=ORIENTED_EDGE ( 'NONE', *, *, #14390, .T. ) ;
#8807=ADVANCED_FACE ( 'NONE', ( #595 ), #21206, .T. ) ;
#8810=CARTESIAN_POINT ( 'NONE',  ( -145.6429501568359797, -156.2084106276440423, 41.63779006702063867 ) ) ;
#8811=CARTESIAN_POINT ( 'NONE',  ( -159.0959885057557983, -178.5938272943107279, 55.19815736654470584 ) ) ;
#8816=DIRECTION ( 'NONE',  ( 0.000000000000000000, 1.000000000000000000, 0.000000000000000000 ) ) ;
#8823=CARTESIAN_POINT ( 'NONE',  ( -160.8964159109769696, -170.3084106276440082, 46.59394152635518083 ) ) ;
#8829=( BOUNDED_CURVE ( )  B_SPLINE_CURVE ( 2, ( #2084, #14081, #19586, #15948, #7707, #20818, #19374, #7487, #19479, #2508, #21143, #7380, #12433 ),
 .UNSPECIFIED., .F., .T. ) 
 B_SPLINE_CURVE_WITH_KNOTS ( ( 3, 2, 2, 2, 2, 2, 3 ),
 ( 0.7678571428571427937, 0.7714285714285714635, 0.7785714285714285809, 0.7857142857142856984, 0.7928571428571428159, 0.8000000000000000444, 0.8035714285714286031 ),
 .UNSPECIFIED. ) 
 CURVE ( )  GEOMETRIC_REPRESENTATION_ITEM ( )  RATIONAL_B_SPLINE_CURVE ( ( 0.9755282581475768211, 0.9755282581475763770, 1.000000000000000000, 0.9510565162951535312, 1.000000000000000000, 0.9510565162951535312, 1.000000000000000000, 0.9510565162951535312, 1.000000000000000000, 0.9510565162951535312, 1.000000000000000000, 0.9755282581475768211, 0.9755282581475768211 ) ) 
 REPRESENTATION_ITEM ( '' )  );
#8832=CARTESIAN_POINT ( 'NONE',  ( -153.0531000319306827, -159.8899795514095672, 59.65701158161631668 ) ) ;
#8836=ADVANCED_FACE ( 'NONE', ( #16005 ), #14021, .T. ) ;
#8844=CARTESIAN_POINT ( 'NONE',  ( -161.4692556286853176, -172.5630981290893260, 49.65701158161630957 ) ) ;
#8848=CARTESIAN_POINT ( 'NONE',  ( -151.4692556286852891, -176.6438272943107393, 39.74470866294723947 ) ) ;
#8849=CARTESIAN_POINT ( 'NONE',  ( -142.0420953463935803, -195.5084106276440536, 46.59394152635518083 ) ) ;
#8850=VERTEX_POINT ( 'NONE', #1346 ) ;
#8851=CARTESIAN_POINT ( 'NONE',  ( -145.6429501568359797, -178.1084106276440480, 57.67623309621198047 ) ) ;
#8867=CARTESIAN_POINT ( 'NONE',  ( -141.4692556286852891, -166.1391397928655067, 52.90620854394536821 ) ) ;
#8874=CARTESIAN_POINT ( 'NONE',  ( -151.4692556286852891, -173.6438272943107108, 39.74470866294723947 ) ) ;
#8876=CARTESIAN_POINT ( 'NONE',  ( -154.5594255724347761, -171.0891397928654669, 40.14644641866476604 ) ) ;
#8889=AXIS2_PLACEMENT_3D ( 'NONE', #6678, #20333, #10197 ) ;
#8890=CARTESIAN_POINT ( 'NONE',  ( -143.3790856849358306, -180.6891397928654612, 43.77915905869157598 ) ) ;
#8899=CARTESIAN_POINT ( 'NONE',  ( -161.4692556286852607, -163.7130981290892464, 46.40781461928724383 ) ) ;
#8917=CARTESIAN_POINT ( 'NONE',  ( -157.2955611005346270, -160.7084106276440423, 57.67623309621198047 ) ) ;
#8918=CARTESIAN_POINT ( 'NONE',  ( -154.3824083646099439, -185.4938272943107336, 40.69124936498395328 ) ) ;
#8926=CARTESIAN_POINT ( 'NONE',  ( -145.6429501568359797, -155.9438272943106938, 41.63779006702063867 ) ) ;
#8927=CARTESIAN_POINT ( 'NONE',  ( -148.5561028927606344, -162.0584106276440366, 40.69124936498395328 ) ) ;
#8943=CARTESIAN_POINT ( 'NONE',  ( -158.9748091281504401, -126.9891397928655010, 62.65701158161630957 ) ) ;
#8949=CARTESIAN_POINT ( 'NONE',  ( -160.8964159109769696, -181.7438272943107336, 52.72008163687743121 ) ) ;
#8950=CARTESIAN_POINT ( 'NONE',  ( -148.5561028927606344, -192.0584106276440650, 40.69124936498395328 ) ) ;
#8951=ORIENTED_EDGE ( 'NONE', *, *, #661, .F. ) ;
#8952=( BOUNDED_CURVE ( )  B_SPLINE_CURVE ( 2, ( #5170, #3632, #10355, #17058, #1970, #8704, #529, #15424, #319, #13754, #20494, #5383, #12099 ),
 .UNSPECIFIED., .F., .F. ) 
 B_SPLINE_CURVE_WITH_KNOTS ( ( 3, 2, 2, 2, 2, 2, 3 ),
 ( 0.4107142857142857539, 0.4142857142857143127, 0.4214285714285714302, 0.4285714285714285476, 0.4357142857142857206, 0.4428571428571428381, 0.4464285714285714524 ),
 .UNSPECIFIED. ) 
 CURVE ( )  GEOMETRIC_REPRESENTATION_ITEM ( )  RATIONAL_B_SPLINE_CURVE ( ( 0.9755282581475768211, 0.9755282581475769321, 1.000000000000000000, 0.9510565162951535312, 1.000000000000000000, 0.9510565162951535312, 1.000000000000000000, 0.9510565162951535312, 1.000000000000000000, 0.9510565162951535312, 1.000000000000000000, 0.9755282581475765991, 0.9755282581475768211 ) ) 
 REPRESENTATION_ITEM ( '' )  );
#8953=CARTESIAN_POINT ( 'NONE',  ( -159.0959885057557983, -176.4584106276440707, 44.11586579668791330 ) ) ;
#8964=AXIS2_PLACEMENT_3D ( 'NONE', #7324, #7535, #19211 ) ;
#8973=CARTESIAN_POINT ( 'NONE',  ( -145.2889157411863721, -171.5391397928654555, 41.15050349809590102 ) ) ;
#8974=CARTESIAN_POINT ( 'NONE',  ( -149.8854112254399240, -159.7362167067690280, 59.65701158161632378 ) ) ;
#8976=CARTESIAN_POINT ( 'NONE',  ( -143.9637021292201950, -116.9891397928655010, 62.65701158161630957 ) ) ;
#8979=CARTESIAN_POINT ( 'NONE',  ( -142.0420953463935803, -165.2438272943107052, 46.59394152635518793 ) ) ;
#8984=EDGE_CURVE ( 'NONE', #12361, #13462, #3221, .T. ) ;
#8986=CARTESIAN_POINT ( 'NONE',  ( -143.9637021292202235, -126.9891397928655010, 36.65701158161628825 ) ) ;
#8997=CARTESIAN_POINT ( 'NONE',  ( -141.4692556286852891, -194.9130981290892635, 46.40781461928724383 ) ) ;
#8999=CARTESIAN_POINT ( 'NONE',  ( -145.2889157411863437, -174.5130981290893146, 58.16351966513671812 ) ) ;
#9000=CARTESIAN_POINT ( 'NONE',  ( -148.3790856849358306, -161.4630981290893317, 40.14644641866477315 ) ) ;
#9002=VECTOR ( 'NONE', #4155, 1000.000000000000000 ) ;
#9007=CARTESIAN_POINT ( 'NONE',  ( -142.0420953463936087, -192.3938272943107393, 49.65701158161630957 ) ) ;
#9024=CARTESIAN_POINT ( 'NONE',  ( -151.4692556286852891, -178.1438272943106824, 59.56931450028537256 ) ) ;
#9026=CARTESIAN_POINT ( 'NONE',  ( -148.3790856849358306, -192.6630981290892919, 59.16757674456786020 ) ) ;
#9035=CARTESIAN_POINT ( 'NONE',  ( -159.5594255724347761, -188.1891397928654612, 55.53486410454104316 ) ) ;
#9036=CARTESIAN_POINT ( 'NONE',  ( -159.0959885057557983, -169.8584106276440764, 55.19815736654470584 ) ) ;
#9043=EDGE_LOOP ( 'NONE', ( #14773, #9421, #21626, #16616 ) ) ;
#9044=CARTESIAN_POINT ( 'NONE',  ( -154.5594255724347761, -180.0891397928654669, 40.14644641866476604 ) ) ;
#9054=SURFACE_STYLE_USAGE ( .BOTH. , #2534 ) ;
#9059=CARTESIAN_POINT ( 'NONE',  ( -154.3824083646099439, -181.2938272943107449, 58.62277379824867296 ) ) ;
#9060=CARTESIAN_POINT ( 'NONE',  ( -145.6429501568359797, -190.1084106276440195, 57.67623309621197336 ) ) ;
#9062=CARTESIAN_POINT ( 'NONE',  ( -148.5561028927606344, -175.2584106276440536, 58.62277379824867296 ) ) ;
#9081=CARTESIAN_POINT ( 'NONE',  ( -159.5594255724347761, -167.1891397928654897, 55.53486410454104316 ) ) ;
#9084=CARTESIAN_POINT ( 'NONE',  ( -151.4692556286852891, -196.9891397928655010, 39.65701158161630246 ) ) ;
#9085=CARTESIAN_POINT ( 'NONE',  ( -166.4803626276155626, -126.9891397928655010, 49.65701158161629536 ) ) ;
#9089=CARTESIAN_POINT ( 'NONE',  ( -160.8964159109769696, -167.0438272943106881, 46.59394152635518793 ) ) ;
#9093=VECTOR ( 'NONE', #9799, 1000.000000000000000 ) ;
#9094=CARTESIAN_POINT ( 'NONE',  ( -151.4692556286852891, -194.9084106276440025, 39.74470866294723947 ) ) ;
#9100=EDGE_CURVE ( 'NONE', #19943, #19802, #21527, .T. ) ;
#9113=CARTESIAN_POINT ( 'NONE',  ( -148.3790856849358306, -155.4630981290893033, 40.14644641866477315 ) ) ;
#9115=FACE_OUTER_BOUND ( 'NONE', #17452, .T. ) ;
#9120=CARTESIAN_POINT ( 'NONE',  ( -151.4692556286852891, -190.1438272943107393, 59.56931450028537967 ) ) ;
#9122=CARTESIAN_POINT ( 'NONE',  ( -141.4692556286852891, -161.9130981290893487, 46.40781461928724383 ) ) ;
#9130=( GEOMETRIC_REPRESENTATION_CONTEXT ( 3 ) GLOBAL_UNCERTAINTY_ASSIGNED_CONTEXT ( ( #11045 ) ) GLOBAL_UNIT_ASSIGNED_CONTEXT ( ( #21064, #19395, #21386 ) ) REPRESENTATION_CONTEXT ( 'NONE', 'WORKASPACE' ) );
#9132=CARTESIAN_POINT ( 'NONE',  ( -151.4692556286853176, -164.3130981290893260, 39.65701158161629536 ) ) ;
#9136=CARTESIAN_POINT ( 'NONE',  ( -143.8425227516148084, -168.6938272943107222, 55.19815736654470584 ) ) ;
#9138=CARTESIAN_POINT ( 'NONE',  ( -161.4692556286852607, -184.7130981290893317, 46.40781461928724383 ) ) ;
#9146=CARTESIAN_POINT ( 'NONE',  ( -160.8964159109769696, -164.3084106276440650, 46.59394152635518083 ) ) ;
#9150=( BOUNDED_CURVE ( )  B_SPLINE_CURVE ( 2, ( #7886, #19894, #17890, #16020, #2803, #14701, #16243, #4783, #14374, #1151, #14587, #21330, #12946 ),
 .UNSPECIFIED., .F., .F. ) 
 B_SPLINE_CURVE_WITH_KNOTS ( ( 3, 2, 2, 2, 2, 2, 3 ),
 ( 0.4464285714285714524, 0.4500000000000000111, 0.4571428571428571286, 0.4642857142857143016, 0.4714285714285714191, 0.4785714285714285920, 0.4821428571428571508 ),
 .UNSPECIFIED. ) 
 CURVE ( )  GEOMETRIC_REPRESENTATION_ITEM ( )  RATIONAL_B_SPLINE_CURVE ( ( 0.9755282581475768211, 0.9755282581475769321, 1.000000000000000000, 0.9510565162951535312, 1.000000000000000000, 0.9510565162951535312, 1.000000000000000000, 0.9510565162951535312, 1.000000000000000000, 0.9510565162951535312, 1.000000000000000000, 0.9755282581475768211, 0.9755282581475768211 ) ) 
 REPRESENTATION_ITEM ( '' )  );
#9155=CARTESIAN_POINT ( 'NONE',  ( -151.4692556286853176, -180.2391397928654726, 39.65701158161629536 ) ) ;
#9165=CARTESIAN_POINT ( 'NONE',  ( -148.3790856849358306, -183.6630981290893203, 59.16757674456786020 ) ) ;
#9166=FILL_AREA_STYLE_COLOUR ( '', #16112 ) ;
#9171=CARTESIAN_POINT ( 'NONE',  ( -154.3824083646099439, -172.2938272943107165, 58.62277379824867296 ) ) ;
#9172=CARTESIAN_POINT ( 'NONE',  ( -151.4692556286852891, -194.9084106276440025, 39.74470866294723947 ) ) ;
#9190=CARTESIAN_POINT ( 'NONE',  ( -148.3790856849358306, -180.6630981290893203, 59.16757674456786020 ) ) ;
#9192=CARTESIAN_POINT ( 'NONE',  ( -143.3790856849358306, -160.2891397928654555, 55.53486410454105027 ) ) ;
#9198=CARTESIAN_POINT ( 'NONE',  ( -148.5561028927606344, -165.9938272943107336, 58.62277379824867296 ) ) ;
#9200=CARTESIAN_POINT ( 'NONE',  ( -154.3824083646099439, -191.7584106276440536, 40.69124936498395328 ) ) ;
#9202=CARTESIAN_POINT ( 'NONE',  ( -159.5594255724347761, -175.2630981290893146, 55.53486410454104316 ) ) ;
#9208=DIRECTION ( 'NONE',  ( 0.000000000000000000, 0.000000000000000000, 1.000000000000000000 ) ) ;
#9210=ORIENTED_EDGE ( 'NONE', *, *, #19040, .T. ) ;
#9214=EDGE_CURVE ( 'NONE', #19943, #21028, #16980, .T. ) ;
#9217=CARTESIAN_POINT ( 'NONE',  ( -141.4692556286852891, -192.2130981290893033, 52.90620854394536821 ) ) ;
#9221=CARTESIAN_POINT ( 'NONE',  ( -148.3790856849358306, -159.6630981290892919, 59.16757674456786020 ) ) ;
#9227=CARTESIAN_POINT ( 'NONE',  ( -154.3824083646099439, -191.4938272943107336, 40.69124936498395328 ) ) ;
#9231=CARTESIAN_POINT ( 'NONE',  ( -151.4692556286852607, -169.7391397928654442, 59.65701158161632378 ) ) ;
#9234=CARTESIAN_POINT ( 'NONE',  ( -143.3790856849358306, -168.6891397928654897, 43.77915905869157598 ) ) ;
#9237=ORIENTED_EDGE ( 'NONE', *, *, #15967, .F. ) ;
#9245=CARTESIAN_POINT ( 'NONE',  ( -160.8964159109769696, -169.8938272943107393, 49.65701158161630957 ) ) ;
#9246=CARTESIAN_POINT ( 'NONE',  ( -148.3790856849358306, -186.6630981290893203, 59.16757674456786020 ) ) ;
#9253=CARTESIAN_POINT ( 'NONE',  ( -142.0420953463935803, -162.8084106276440650, 52.72008163687743831 ) ) ;
#9261=LINE ( 'NONE', #21156, #18023 ) ;
#9269=CARTESIAN_POINT ( 'NONE',  ( -157.6495955161842062, -158.0130981290893146, 41.15050349809589392 ) ) ;
#9276=CARTESIAN_POINT ( 'NONE',  ( -142.0420953463935803, -168.2438272943107336, 46.59394152635518793 ) ) ;
#9277=CARTESIAN_POINT ( 'NONE',  ( -159.0959885057557983, -190.8584106276440480, 55.19815736654470584 ) ) ;
#9279=CARTESIAN_POINT ( 'NONE',  ( -143.8425227516148084, -177.3584106276440480, 44.11586579668791330 ) ) ;
#9296=CARTESIAN_POINT ( 'NONE',  ( -141.4692556286852891, -156.8391397928654669, 46.40781461928724383 ) ) ;
#9301=ORIENTED_EDGE ( 'NONE', *, *, #15069, .T. ) ;
#9303=CARTESIAN_POINT ( 'NONE',  ( -159.0959885057557983, -164.1938272943107222, 44.11586579668791330 ) ) ;
#9306=EDGE_LOOP ( 'NONE', ( #15852, #7851, #15044, #8058 ) ) ;
#9319=CARTESIAN_POINT ( 'NONE',  ( -151.4692556286852891, -189.2391397928654158, 39.14238933923362396 ) ) ;
#9324=CARTESIAN_POINT ( 'NONE',  ( -159.5594255724347761, -160.8630981290893089, 43.77915905869157598 ) ) ;
#9329=CARTESIAN_POINT ( 'NONE',  ( -151.4692556286852891, -193.1438272943107393, 59.56931450028537967 ) ) ;
#9339=ORIENTED_EDGE ( 'NONE', *, *, #17326, .F. ) ;
#9346=CARTESIAN_POINT ( 'NONE',  ( -142.0420953463935803, -174.2438272943107052, 46.59394152635518083 ) ) ;
#9348=CARTESIAN_POINT ( 'NONE',  ( -145.2889157411863721, -191.6130981290893089, 41.15050349809590102 ) ) ;
#9355=CARTESIAN_POINT ( 'NONE',  ( -142.0420953463935803, -159.5084106276440252, 46.59394152635518083 ) ) ;
#9359=EDGE_CURVE ( 'NONE', #7746, #1989, #4509, .T. ) ;
#9367=DIRECTION ( 'NONE',  ( 0.000000000000000000, 0.000000000000000000, 1.000000000000000000 ) ) ;
#9384=CARTESIAN_POINT ( 'NONE',  ( -160.8964159109769696, -175.7438272943107052, 52.72008163687743121 ) ) ;
#9385=CARTESIAN_POINT ( 'NONE',  ( -154.3824083646099439, -181.5584106276440650, 58.62277379824867296 ) ) ;
#9387=CARTESIAN_POINT ( 'NONE',  ( -159.0959885057557983, -172.8584106276440764, 55.19815736654470584 ) ) ;
#9404=EDGE_CURVE ( 'NONE', #21213, #8340, #7941, .T. ) ;
#9406=CARTESIAN_POINT ( 'NONE',  ( -151.4692556286852891, -163.7391397928655010, 60.17163382399899518 ) ) ;
#9408=DIRECTION ( 'NONE',  ( -0.000000000000000000, 1.000000000000000000, -0.000000000000000000 ) ) ;
#9410=LINE ( 'NONE', #3905, #1118 ) ;
#9413=CARTESIAN_POINT ( 'NONE',  ( -151.4692556286852891, -161.6438272943107393, 39.74470866294723947 ) ) ;
#9421=ORIENTED_EDGE ( 'NONE', *, *, #15285, .T. ) ;
#9434=CARTESIAN_POINT ( 'NONE',  ( -154.5594255724347761, -189.0891397928654953, 40.14644641866476604 ) ) ;
#9438=CARTESIAN_POINT ( 'NONE',  ( -157.2955611005346270, -188.3438272943107279, 41.63779006702063867 ) ) ;
#9444=CARTESIAN_POINT ( 'NONE',  ( -157.2955611005346270, -191.3438272943106995, 41.63779006702063867 ) ) ;
#9462=CARTESIAN_POINT ( 'NONE',  ( -154.3824083646099439, -172.2938272943107165, 58.62277379824867296 ) ) ;
#9464=CARTESIAN_POINT ( 'NONE',  ( -143.3790856849358306, -189.3630981290893089, 55.53486410454105027 ) ) ;
#9480=CARTESIAN_POINT ( 'NONE',  ( -145.2889157411863437, -157.4391397928654612, 58.16351966513671812 ) ) ;
#9487=EDGE_CURVE ( 'NONE', #12850, #9846, #12568, .T. ) ;
#9490=CARTESIAN_POINT ( 'NONE',  ( -145.2889157411863437, -182.6130981290893374, 41.15050349809589392 ) ) ;
#9498=CARTESIAN_POINT ( 'NONE',  ( -142.0420953463935803, -174.5438272943107449, 52.72008163687743831 ) ) ;
#9499=CARTESIAN_POINT ( 'NONE',  ( -142.0420953463935803, -189.5084106276440536, 46.59394152635518083 ) ) ;
#9502=CARTESIAN_POINT ( 'NONE',  ( -157.2955611005346270, -173.6084106276440480, 41.63779006702063867 ) ) ;
#9520=CARTESIAN_POINT ( 'NONE',  ( -151.4692556286852891, -160.7391397928654726, 60.17163382399899518 ) ) ;
#9527=CARTESIAN_POINT ( 'NONE',  ( -160.8964159109769696, -194.0084106276440252, 52.72008163687743121 ) ) ;
#9529=CARTESIAN_POINT ( 'NONE',  ( -154.3824083646099439, -188.7584106276440536, 40.69124936498395328 ) ) ;
#9531=CYLINDRICAL_SURFACE ( 'NONE', #12892, 10.00000000000000888 ) ;
#9534=ORIENTED_EDGE ( 'NONE', *, *, #21084, .T. ) ;
#9542=CARTESIAN_POINT ( 'NONE',  ( -157.6495955161842062, -185.0391397928653987, 58.16351966513671812 ) ) ;
#9543=DIRECTION ( 'NONE',  ( 0.000000000000000000, 1.000000000000000000, 0.000000000000000000 ) ) ;
#9545=CARTESIAN_POINT ( 'NONE',  ( -142.0420953463935803, -192.2438272943107336, 46.59394152635518793 ) ) ;
#9550=CARTESIAN_POINT ( 'NONE',  ( -159.0959885057557983, -187.5938272943107279, 55.19815736654470584 ) ) ;
#9554=CARTESIAN_POINT ( 'NONE',  ( -151.4692556286852891, -177.2391397928654442, 39.65701158161629536 ) ) ;
#9558=ORIENTED_EDGE ( 'NONE', *, *, #2230, .T. ) ;
#9561=CARTESIAN_POINT ( 'NONE',  ( -161.4692556286852891, -193.4130981290892919, 52.90620854394536821 ) ) ;
#9567=CARTESIAN_POINT ( 'NONE',  ( -143.8425227516148084, -171.0938272943107279, 44.11586579668791330 ) ) ;
#9569=CARTESIAN_POINT ( 'NONE',  ( -143.3790856849358306, -177.3630981290893089, 55.53486410454105027 ) ) ;
#9577=CARTESIAN_POINT ( 'NONE',  ( -143.8425227516148084, -156.3584106276440480, 44.11586579668791330 ) ) ;
#9584=ORIENTED_EDGE ( 'NONE', *, *, #1011, .T. ) ;
#9594=CARTESIAN_POINT ( 'NONE',  ( -159.0959885057557983, -170.4584106276440423, 44.11586579668791330 ) ) ;
#9598=CARTESIAN_POINT ( 'NONE',  ( -149.8854112254399240, -188.3899795514095956, 39.65701158161630957 ) ) ;
#9600=CARTESIAN_POINT ( 'NONE',  ( -151.4692556286852891, -196.9891397928655010, 59.65701158161632378 ) ) ;
#9605=CARTESIAN_POINT ( 'NONE',  ( -160.8964159109769696, -173.0438272943107449, 46.59394152635518793 ) ) ;
#9606=CARTESIAN_POINT ( 'NONE',  ( -145.6429501568359797, -180.2084106276440707, 41.63779006702063867 ) ) ;
#9610=CARTESIAN_POINT ( 'NONE',  ( -157.2955611005346270, -166.7084106276440423, 57.67623309621198047 ) ) ;
#9612=FACE_OUTER_BOUND ( 'NONE', #10750, .T. ) ;
#9626=CARTESIAN_POINT ( 'NONE',  ( -154.5594255724347761, -160.8891397928654499, 59.16757674456785310 ) ) ;
#9629=DIRECTION ( 'NONE',  ( -0.000000000000000000, 1.000000000000000000, -0.000000000000000000 ) ) ;
#9633=CARTESIAN_POINT ( 'NONE',  ( -142.0420953463935803, -192.8084106276440650, 52.72008163687743831 ) ) ;
#9635=CARTESIAN_POINT ( 'NONE',  ( -148.5561028927606344, -183.0584106276440650, 40.69124936498395328 ) ) ;
#9638=DIRECTION ( 'NONE',  ( 0.000000000000000000, 0.000000000000000000, 1.000000000000000000 ) ) ;
#9650=CARTESIAN_POINT ( 'NONE',  ( -148.3790856849358306, -192.3891397928654783, 40.14644641866477315 ) ) ;
#9653=CARTESIAN_POINT ( 'NONE',  ( -143.8425227516148084, -189.0938272943107279, 44.11586579668791330 ) ) ;
#9659=CARTESIAN_POINT ( 'NONE',  ( -148.5561028927606344, -180.9938272943107336, 58.62277379824867296 ) ) ;
#9669=ORIENTED_EDGE ( 'NONE', *, *, #14698, .F. ) ;
#9675=CARTESIAN_POINT ( 'NONE',  ( -151.4692556286852891, -155.9084106276440593, 39.74470866294723947 ) ) ;
#9677=CARTESIAN_POINT ( 'NONE',  ( -151.4692556286852891, -163.1438272943106824, 59.56931450028537256 ) ) ;
#9678=CARTESIAN_POINT ( 'NONE',  ( -151.4692556286853176, -165.2391397928654442, 39.65701158161629536 ) ) ;
#9679=CARTESIAN_POINT ( 'NONE',  ( -161.4692556286852607, -175.4130981290893203, 52.90620854394536821 ) ) ;
#9682=CARTESIAN_POINT ( 'NONE',  ( -151.4692556286852607, -184.7391397928654726, 59.65701158161632378 ) ) ;
#9688=CARTESIAN_POINT ( 'NONE',  ( -148.5561028927606344, -157.2584106276440536, 58.62277379824867296 ) ) ;
#9702=CARTESIAN_POINT ( 'NONE',  ( -160.8964159109769696, -167.1584106276440593, 49.65701158161630957 ) ) ;
#9703=CARTESIAN_POINT ( 'NONE',  ( -157.2955611005345986, -188.3438272943107279, 41.63779006702063867 ) ) ;
#9707=CARTESIAN_POINT ( 'NONE',  ( -145.2889157411863437, -174.5391397928654840, 41.15050349809589392 ) ) ;
#9712=CARTESIAN_POINT ( 'NONE',  ( -154.3824083646099439, -160.2938272943107449, 58.62277379824867296 ) ) ;
#9713=CARTESIAN_POINT ( 'NONE',  ( -160.8964159109769696, -185.1584106276440309, 49.65701158161630957 ) ) ;
#9716=CARTESIAN_POINT ( 'NONE',  ( -143.8425227516148084, -168.9584106276440423, 55.19815736654470584 ) ) ;
#9718=DIRECTION ( 'NONE',  ( -0.4999999999999993894, 0.000000000000000000, 0.8660254037844389297 ) ) ;
#9739=DIRECTION ( 'NONE',  ( -0.000000000000000000, 1.000000000000000000, -0.000000000000000000 ) ) ;
#9741=ORIENTED_EDGE ( 'NONE', *, *, #19082, .F. ) ;
#9743=CARTESIAN_POINT ( 'NONE',  ( -157.2955611005346270, -157.4438272943107506, 57.67623309621198047 ) ) ;
#9745=CARTESIAN_POINT ( 'NONE',  ( -159.0959885057557983, -184.8584106276440480, 55.19815736654470584 ) ) ;
#9747=CARTESIAN_POINT ( 'NONE',  ( -154.5594255724347761, -162.0891397928654669, 40.14644641866476604 ) ) ;
#9748=VECTOR ( 'NONE', #12615, 1000.000000000000227 ) ;
#9752=CARTESIAN_POINT ( 'NONE',  ( -151.4692556286852891, -196.9891397928655010, 39.65701158161630246 ) ) ;
#9760=CARTESIAN_POINT ( 'NONE',  ( -159.5594255724347761, -191.7891397928654555, 43.77915905869157598 ) ) ;
#9763=DIRECTION ( 'NONE',  ( -0.000000000000000000, 1.000000000000000000, -0.000000000000000000 ) ) ;
#9764=CARTESIAN_POINT ( 'NONE',  ( -157.2955611005346270, -193.4438272943106938, 57.67623309621198047 ) ) ;
#9769=CARTESIAN_POINT ( 'NONE',  ( -143.8425227516148084, -183.6938272943107506, 55.19815736654470584 ) ) ;
#9780=ORIENTED_EDGE ( 'NONE', *, *, #17590, .F. ) ;
#9787=CARTESIAN_POINT ( 'NONE',  ( -143.8425227516148084, -159.0938272943107279, 44.11586579668791330 ) ) ;
#9790=CARTESIAN_POINT ( 'NONE',  ( -157.6495955161842062, -181.1130981290893089, 58.16351966513671812 ) ) ;
#9797=CARTESIAN_POINT ( 'NONE',  ( -154.5594255724347761, -183.0891397928654669, 40.14644641866476604 ) ) ;
#9798=CARTESIAN_POINT ( 'NONE',  ( -159.0959885057557983, -158.4584106276440423, 44.11586579668791330 ) ) ;
#9799=DIRECTION ( 'NONE',  ( -0.000000000000000000, -1.000000000000000000, -0.000000000000000000 ) ) ;
#9806=CARTESIAN_POINT ( 'NONE',  ( -148.3790856849358306, -167.4630981290893033, 40.14644641866477315 ) ) ;
#9812=CARTESIAN_POINT ( 'NONE',  ( -157.2955611005346270, -164.6084106276440764, 41.63779006702063867 ) ) ;
#9813=CARTESIAN_POINT ( 'NONE',  ( -142.0420953463935803, -189.5438272943107165, 52.72008163687743831 ) ) ;
#9818=CARTESIAN_POINT ( 'NONE',  ( -151.4692556286852891, -185.3130981290893260, 39.65701158161630246 ) ) ;
#9821=CARTESIAN_POINT ( 'NONE',  ( -145.6429501568359797, -162.8438272943107279, 57.67623309621198047 ) ) ;
#9822=CARTESIAN_POINT ( 'NONE',  ( -151.4692556286852891, -184.4084106276440309, 59.56931450028537256 ) ) ;
#9823=ORIENTED_EDGE ( 'NONE', *, *, #12708, .F. ) ;
#9825=CARTESIAN_POINT ( 'NONE',  ( -143.8425227516148084, -171.3584106276440764, 44.11586579668791330 ) ) ;
#9830=VERTEX_POINT ( 'NONE', #5593 ) ;
#9832=CARTESIAN_POINT ( 'NONE',  ( -141.4692556286852891, -192.8391397928654669, 46.40781461928724383 ) ) ;
#9833=ORIENTED_EDGE ( 'NONE', *, *, #6546, .T. ) ;
#9845=CARTESIAN_POINT ( 'NONE',  ( -157.6495955161842062, -185.0391397928654271, 58.16351966513671812 ) ) ;
#9846=VERTEX_POINT ( 'NONE', #3848 ) ;
#9848=CARTESIAN_POINT ( 'NONE',  ( -154.3824083646099439, -157.2938272943107449, 58.62277379824867296 ) ) ;
#9850=CARTESIAN_POINT ( 'NONE',  ( -142.0420953463935803, -189.5084106276440536, 46.59394152635518793 ) ) ;
#9867=CARTESIAN_POINT ( 'NONE',  ( -145.2889157411863721, -183.5391397928655124, 41.15050349809590102 ) ) ;
#9870=CARTESIAN_POINT ( 'NONE',  ( -142.0420953463935803, -189.2438272943107336, 46.59394152635518793 ) ) ;
#9874=CARTESIAN_POINT ( 'NONE',  ( -148.5561028927606344, -183.9938272943107336, 58.62277379824867296 ) ) ;
#9879=ADVANCED_FACE ( 'NONE', ( #12320 ), #3635, .T. ) ;
#9886=EDGE_CURVE ( 'NONE', #18762, #1989, #8115, .T. ) ;
#9893=CARTESIAN_POINT ( 'NONE',  ( -160.8964159109769696, -157.8938272943107393, 49.65701158161630957 ) ) ;
#9895=CARTESIAN_POINT ( 'NONE',  ( -143.3790856849358306, -176.7630981290893146, 43.77915905869157598 ) ) ;
#9906=CARTESIAN_POINT ( 'NONE',  ( -151.4692556286852891, -196.9891397928655010, 49.65701158161630957 ) ) ;
#9917=EDGE_CURVE ( 'NONE', #19197, #2548, #8829, .T. ) ;
#9918=CARTESIAN_POINT ( 'NONE',  ( -160.8964159109769696, -170.3084106276440082, 46.59394152635518793 ) ) ;
#9919=CARTESIAN_POINT ( 'NONE',  ( -145.6429501568359797, -186.8438272943106995, 57.67623309621197336 ) ) ;
#9920=CARTESIAN_POINT ( 'NONE',  ( -154.5594255724347761, -179.1630981290893203, 40.14644641866476604 ) ) ;
#9924=CARTESIAN_POINT ( 'NONE',  ( -149.8854112254399809, -174.3160212151857422, 39.65701158161628825 ) ) ;
#9930=CARTESIAN_POINT ( 'NONE',  ( -143.8425227516148084, -159.6938272943107222, 55.19815736654470584 ) ) ;
#9931=CARTESIAN_POINT ( 'NONE',  ( -142.0420953463935803, -171.5084106276440536, 46.59394152635518083 ) ) ;
#9935=CARTESIAN_POINT ( 'NONE',  ( -154.3824083646099439, -157.5584106276440650, 58.62277379824867296 ) ) ;
#9941=AXIS2_PLACEMENT_3D ( 'NONE', #12573, #21071, #459 ) ;
#9957=CYLINDRICAL_SURFACE ( 'NONE', #16605, 10.00000000000000888 ) ;
#9959=VERTEX_POINT ( 'NONE', #5709 ) ;
#9961=CARTESIAN_POINT ( 'NONE',  ( -151.4692556286852891, -185.9084106276440025, 39.74470866294723947 ) ) ;
#9963=CARTESIAN_POINT ( 'NONE',  ( -159.0959885057557983, -185.4584106276440707, 44.11586579668791330 ) ) ;
#9973=DIRECTION ( 'NONE',  ( 0.000000000000000000, 0.000000000000000000, 1.000000000000000000 ) ) ;
#9979=CARTESIAN_POINT ( 'NONE',  ( -159.5594255724347761, -176.7891397928654840, 43.77915905869157598 ) ) ;
#9980=LINE ( 'NONE', #1262, #18584 ) ;
#9987=CARTESIAN_POINT ( 'NONE',  ( -154.3824083646099439, -184.2938272943107449, 58.62277379824867296 ) ) ;
#10000=CARTESIAN_POINT ( 'NONE',  ( -151.4692556286852891, -196.9891397928655010, 49.65701158161630957 ) ) ;
#10003=DIRECTION ( 'NONE',  ( 0.000000000000000000, 0.000000000000000000, 1.000000000000000000 ) ) ;
#10004=CARTESIAN_POINT ( 'NONE',  ( -142.0420953463936087, -165.3938272943107393, 49.65701158161630957 ) ) ;
#10006=CARTESIAN_POINT ( 'NONE',  ( -151.4692556286852891, -182.3130981290893260, 39.14238933923362396 ) ) ;
#10016=CARTESIAN_POINT ( 'NONE',  ( -151.4692556286852891, -186.8130981290893260, 59.65701158161632378 ) ) ;
#10020=LINE ( 'NONE', #1417, #4147 ) ;
#10027=CARTESIAN_POINT ( 'NONE',  ( -145.6429501568359797, -168.2084106276440139, 41.63779006702063867 ) ) ;
#10028=CARTESIAN_POINT ( 'NONE',  ( -160.8964159109769696, -193.7438272943107052, 52.72008163687743121 ) ) ;
#10041=CARTESIAN_POINT ( 'NONE',  ( -142.0420953463935803, -165.2438272943107052, 46.59394152635518793 ) ) ;
#10042=CARTESIAN_POINT ( 'NONE',  ( -160.8964159109769696, -176.3084106276440082, 46.59394152635518083 ) ) ;
#10045=CARTESIAN_POINT ( 'NONE',  ( -142.0420953463935803, -159.5084106276440536, 46.59394152635518793 ) ) ;
#10058=CYLINDRICAL_SURFACE ( 'NONE', #10076, 10.00000000000000888 ) ;
#10067=CARTESIAN_POINT ( 'NONE',  ( -151.4692556286852891, -190.4084106276440309, 59.56931450028537967 ) ) ;
#10069=CARTESIAN_POINT ( 'NONE',  ( -160.8964159109769696, -176.3084106276440082, 46.59394152635518793 ) ) ;
#10076=AXIS2_PLACEMENT_3D ( 'NONE', #2993, #8407, #16431 ) ;
#10083=DIRECTION ( 'NONE',  ( -0.000000000000000000, 1.000000000000000000, -0.000000000000000000 ) ) ;
#10084=CARTESIAN_POINT ( 'NONE',  ( -145.2889157411863721, -175.4391397928654328, 58.16351966513671812 ) ) ;
#10086=CARTESIAN_POINT ( 'NONE',  ( -151.4692556286852891, -196.9891397928655010, 49.65701158161630957 ) ) ;
#10093=CARTESIAN_POINT ( 'NONE',  ( -143.8425227516148084, -171.0938272943107279, 44.11586579668791330 ) ) ;
#10110=( BOUNDED_CURVE ( )  B_SPLINE_CURVE ( 2, ( #7799, #14505, #21247, #6124, #12853, #19576, #4468, #9561, #8345, #18698, #15055, #6583, #3158 ),
 .UNSPECIFIED., .F., .F. ) 
 B_SPLINE_CURVE_WITH_KNOTS ( ( 3, 2, 2, 2, 2, 2, 3 ),
 ( 0.01785714285714287350, 0.02142857142857142877, 0.02857142857142857054, 0.03571428571428571230, 0.04285714285714285754, 0.05000000000000000278, 0.05357142857142858927 ),
 .UNSPECIFIED. ) 
 CURVE ( )  GEOMETRIC_REPRESENTATION_ITEM ( )  RATIONAL_B_SPLINE_CURVE ( ( 0.9755282581475767101, 0.9755282581475768211, 1.000000000000000000, 0.9510565162951535312, 1.000000000000000000, 0.9510565162951535312, 1.000000000000000000, 0.9510565162951535312, 1.000000000000000000, 0.9510565162951535312, 1.000000000000000000, 0.9755282581475765991, 0.9755282581475767101 ) ) 
 REPRESENTATION_ITEM ( '' )  );
#10111=CARTESIAN_POINT ( 'NONE',  ( -148.5561028927606344, -165.9938272943107336, 58.62277379824867296 ) ) ;
#10113=CARTESIAN_POINT ( 'NONE',  ( -154.5594255724347761, -170.1630981290893203, 40.14644641866476604 ) ) ;
#10123=DIRECTION ( 'NONE',  ( -0.000000000000000000, -1.000000000000000000, -0.000000000000000000 ) ) ;
#10126=CARTESIAN_POINT ( 'NONE',  ( -145.2889157411863437, -155.6130981290893089, 41.15050349809589392 ) ) ;
#10130=CARTESIAN_POINT ( 'NONE',  ( -166.4803626276155626, -116.9891397928655010, 49.65701158161629536 ) ) ;
#10138=ADVANCED_FACE ( 'NONE', ( #11969 ), #5355, .T. ) ;
#10139=CARTESIAN_POINT ( 'NONE',  ( -145.6429501568359797, -163.1084106276440195, 57.67623309621198047 ) ) ;
#10140=CARTESIAN_POINT ( 'NONE',  ( -142.0420953463935803, -192.5438272943107449, 52.72008163687743831 ) ) ;
#10149=CARTESIAN_POINT ( 'NONE',  ( -145.6429501568359797, -159.8438272943107563, 57.67623309621198047 ) ) ;
#10150=CARTESIAN_POINT ( 'NONE',  ( -143.8425227516148084, -177.9584106276440707, 55.19815736654470584 ) ) ;
#10154=CARTESIAN_POINT ( 'NONE',  ( -157.2955611005346270, -161.6084106276440480, 41.63779006702063867 ) ) ;
#10161=CARTESIAN_POINT ( 'NONE',  ( -145.2889157411863437, -192.5391397928654555, 41.15050349809589392 ) ) ;
#10163=EDGE_CURVE ( 'NONE', #20510, #4977, #18699, .T. ) ;
#10173=CARTESIAN_POINT ( 'NONE',  ( -156.4692903108300186, -155.9898770414735623, 40.99677756761010272 ) ) ;
#10179=CARTESIAN_POINT ( 'NONE',  ( -159.0959885057557983, -182.4584106276440707, 44.11586579668791330 ) ) ;
#10181=CARTESIAN_POINT ( 'NONE',  ( -142.0420953463936087, -174.6584106276440593, 49.65701158161630957 ) ) ;
#10182=VERTEX_POINT ( 'NONE', #3815 ) ;
#10185=DIRECTION ( 'NONE',  ( -4.622506457652817044E-16, 0.000000000000000000, 1.000000000000000000 ) ) ;
#10197=DIRECTION ( 'NONE',  ( 0.000000000000000000, 0.000000000000000000, 1.000000000000000000 ) ) ;
#10198=CARTESIAN_POINT ( 'NONE',  ( -141.4692556286852891, -183.9891397928654726, 49.65701158161630957 ) ) ;
#10206=CARTESIAN_POINT ( 'NONE',  ( -151.4692556286852891, -175.1438272943107393, 59.56931450028537967 ) ) ;
#10208=CARTESIAN_POINT ( 'NONE',  ( -148.3790856849358306, -195.3891397928654783, 40.14644641866477315 ) ) ;
#10222=DIRECTION ( 'NONE',  ( 0.000000000000000000, 0.000000000000000000, 1.000000000000000000 ) ) ;
#10225=CARTESIAN_POINT ( 'NONE',  ( -145.2889157411863721, -167.6130981290893089, 41.15050349809590102 ) ) ;
#10235=DIRECTION ( 'NONE',  ( -0.000000000000000000, 1.000000000000000000, -0.000000000000000000 ) ) ;
#10247=CARTESIAN_POINT ( 'NONE',  ( -145.6429501568359797, -162.2084106276440707, 41.63779006702063867 ) ) ;
#10248=CARTESIAN_POINT ( 'NONE',  ( -151.4692556286852891, -181.1438272943107108, 59.56931450028537256 ) ) ;
#10250=CARTESIAN_POINT ( 'NONE',  ( -141.4692556286852891, -194.9130981290892635, 46.40781461928724383 ) ) ;
#10252=CARTESIAN_POINT ( 'NONE',  ( -154.5594255724347761, -174.0891397928654669, 40.14644641866476604 ) ) ;
#10254=CARTESIAN_POINT ( 'NONE',  ( -161.4692556286852891, -184.4130981290893203, 52.90620854394536821 ) ) ;
#10257=CARTESIAN_POINT ( 'NONE',  ( -159.5594255724347761, -188.7891397928654555, 43.77915905869157598 ) ) ;
#10258=CARTESIAN_POINT ( 'NONE',  ( -148.5561028927606344, -178.2584106276440536, 58.62277379824867296 ) ) ;
#10260=CARTESIAN_POINT ( 'NONE',  ( -151.4692556286852891, -160.4084106276440593, 59.56931450028537967 ) ) ;
#10264=ORIENTED_EDGE ( 'NONE', *, *, #12606, .F. ) ;
#10267=EDGE_LOOP ( 'NONE', ( #15690, #2323, #5100, #9833 ) ) ;
#10283=CARTESIAN_POINT ( 'NONE',  ( -159.0959885057557983, -188.4584106276440423, 44.11586579668791330 ) ) ;
#10285=CARTESIAN_POINT ( 'NONE',  ( -142.0420953463936087, -177.6584106276440309, 49.65701158161630957 ) ) ;
#10290=DIRECTION ( 'NONE',  ( 0.000000000000000000, 0.000000000000000000, -1.000000000000000000 ) ) ;
#10298=CARTESIAN_POINT ( 'NONE',  ( -151.4692556286852891, -196.9891397928655010, 59.65701158161632378 ) ) ;
#10305=CARTESIAN_POINT ( 'NONE',  ( -143.3790856849358306, -181.2891397928654840, 55.53486410454105027 ) ) ;
#10313=CARTESIAN_POINT ( 'NONE',  ( -157.2955611005346270, -175.4438272943107506, 57.67623309621198047 ) ) ;
#10317=ORIENTED_EDGE ( 'NONE', *, *, #349, .F. ) ;
#10321=ORIENTED_EDGE ( 'NONE', *, *, #9359, .F. ) ;
#10330=CARTESIAN_POINT ( 'NONE',  ( -151.4692556286853176, -173.3130981290892976, 39.65701158161629536 ) ) ;
#10332=CARTESIAN_POINT ( 'NONE',  ( -145.2889157411863721, -164.6130981290893089, 41.15050349809590102 ) ) ;
#10342=CARTESIAN_POINT ( 'NONE',  ( -141.4692556286852891, -186.2130981290892748, 52.90620854394536821 ) ) ;
#10345=LINE ( 'NONE', #3728, #9748 ) ;
#10353=CARTESIAN_POINT ( 'NONE',  ( -154.3824083646099439, -158.7584106276440536, 40.69124936498395328 ) ) ;
#10354=CARTESIAN_POINT ( 'NONE',  ( -154.3824083646099439, -181.2938272943107449, 58.62277379824867296 ) ) ;
#10355=CARTESIAN_POINT ( 'NONE',  ( -148.3790856849358306, -178.5891397928654669, 59.16757674456786020 ) ) ;
#10356=CARTESIAN_POINT ( 'NONE',  ( -141.4692556286852891, -195.0630981290893260, 49.65701158161630957 ) ) ;
#10365=CARTESIAN_POINT ( 'NONE',  ( -142.0420953463935803, -156.5438272943107165, 52.72008163687743831 ) ) ;
#10366=CARTESIAN_POINT ( 'NONE',  ( -154.3824083646099439, -178.5584106276440366, 58.62277379824867296 ) ) ;
#10384=DIRECTION ( 'NONE',  ( 0.000000000000000000, 0.000000000000000000, 1.000000000000000000 ) ) ;
#10391=CARTESIAN_POINT ( 'NONE',  ( -159.0959885057557983, -182.1938272943107506, 44.11586579668791330 ) ) ;
#10394=CARTESIAN_POINT ( 'NONE',  ( -157.2955611005346270, -187.7084106276440139, 57.67623309621198047 ) ) ;
#10396=CARTESIAN_POINT ( 'NONE',  ( -151.4692556286852891, -178.4084106276440878, 59.56931450028537967 ) ) ;
#10404=VERTEX_POINT ( 'NONE', #14156 ) ;
#10411=CARTESIAN_POINT ( 'NONE',  ( -157.6495955161842062, -173.0391397928654555, 58.16351966513671812 ) ) ;
#10413=CARTESIAN_POINT ( 'NONE',  ( -159.5594255724347761, -194.1891397928654897, 55.53486410454104316 ) ) ;
#10418=CARTESIAN_POINT ( 'NONE',  ( -148.5561028927606344, -170.7938272943107165, 40.69124936498395328 ) ) ;
#10422=CARTESIAN_POINT ( 'NONE',  ( -159.5594255724347761, -158.1891397928654612, 55.53486410454104316 ) ) ;
#10429=ORIENTED_EDGE ( 'NONE', *, *, #15279, .T. ) ;
#10437=LINE ( 'NONE', #17138, #18366 ) ;
#10441=CARTESIAN_POINT ( 'NONE',  ( -156.1828648351502409, -155.3945647575688156, 41.49286807254280518 ) ) ;
#10443=CARTESIAN_POINT ( 'NONE',  ( -161.4692556286853176, -166.5630981290893260, 49.65701158161630957 ) ) ;
#10447=CARTESIAN_POINT ( 'NONE',  ( -148.3790856849358306, -184.5891397928654669, 59.16757674456786020 ) ) ;
#10453=CARTESIAN_POINT ( 'NONE',  ( -145.2889157411863437, -185.6130981290893089, 41.15050349809589392 ) ) ;
#10460=CARTESIAN_POINT ( 'NONE',  ( -148.3790856849358306, -164.4630981290893317, 40.14644641866477315 ) ) ;
#10465=CARTESIAN_POINT ( 'NONE',  ( -160.8964159109769696, -161.0084106276440252, 52.72008163687743121 ) ) ;
#10466=CARTESIAN_POINT ( 'NONE',  ( -151.4692556286852891, -185.6438272943107393, 39.74470866294723947 ) ) ;
#10468=CARTESIAN_POINT ( 'NONE',  ( -159.5594255724347761, -193.2630981290893146, 55.53486410454104316 ) ) ;
#10470=CARTESIAN_POINT ( 'NONE',  ( -151.4692556286852607, -172.7391397928654726, 59.65701158161632378 ) ) ;
#10476=CARTESIAN_POINT ( 'NONE',  ( -153.0531000319306543, -187.8160212151857422, 59.65701158161632378 ) ) ;
#10477=CARTESIAN_POINT ( 'NONE',  ( -145.6429501568359797, -168.2084106276440139, 41.63779006702063867 ) ) ;
#10478=DIRECTION ( 'NONE',  ( 0.000000000000000000, -0.000000000000000000, 1.000000000000000000 ) ) ;
#10483=CARTESIAN_POINT ( 'NONE',  ( -161.4692556286853176, -179.4891397928654726, 49.65701158161630957 ) ) ;
#10484=ORIENTED_EDGE ( 'NONE', *, *, #13823, .F. ) ;
#10493=CARTESIAN_POINT ( 'NONE',  ( -151.4692556286853176, -173.3130981290892976, 39.65701158161629536 ) ) ;
#10498=CARTESIAN_POINT ( 'NONE',  ( -160.8964159109769696, -185.0438272943107165, 46.59394152635518793 ) ) ;
#10501=( BOUNDED_CURVE ( )  B_SPLINE_CURVE ( 2, ( #13716, #5346, #12061, #20880, #491, #14037, #2462, #20772, #9202, #7549, #812, #15901, #5663 ),
 .UNSPECIFIED., .F., .F. ) 
 B_SPLINE_CURVE_WITH_KNOTS ( ( 3, 2, 2, 2, 2, 2, 3 ),
 ( 0.4464285714285714524, 0.4500000000000000111, 0.4571428571428571286, 0.4642857142857143016, 0.4714285714285714191, 0.4785714285714285920, 0.4821428571428571508 ),
 .UNSPECIFIED. ) 
 CURVE ( )  GEOMETRIC_REPRESENTATION_ITEM ( )  RATIONAL_B_SPLINE_CURVE ( ( 0.9755282581475768211, 0.9755282581475769321, 1.000000000000000000, 0.9510565162951535312, 1.000000000000000000, 0.9510565162951535312, 1.000000000000000000, 0.9510565162951535312, 1.000000000000000000, 0.9510565162951535312, 1.000000000000000000, 0.9755282581475768211, 0.9755282581475768211 ) ) 
 REPRESENTATION_ITEM ( '' )  );
#10502=CARTESIAN_POINT ( 'NONE',  ( -148.5561028927606344, -180.0584106276440366, 40.69124936498395328 ) ) ;
#10504=EDGE_CURVE ( 'NONE', #8850, #9830, #3376, .T. ) ;
#10510=ORIENTED_EDGE ( 'NONE', *, *, #17917, .T. ) ;
#10522=CARTESIAN_POINT ( 'NONE',  ( -154.5594255724347761, -169.8891397928654499, 59.16757674456785310 ) ) ;
#10523=CARTESIAN_POINT ( 'NONE',  ( -151.4692556286852891, -180.8130981290893260, 59.65701158161631668 ) ) ;
#10527=CARTESIAN_POINT ( 'NONE',  ( -160.8964159109769696, -176.0438272943107165, 46.59394152635518793 ) ) ;
#10540=CARTESIAN_POINT ( 'NONE',  ( -141.4692556286852891, -181.1391397928654783, 52.90620854394536821 ) ) ;
#10543=CARTESIAN_POINT ( 'NONE',  ( -151.4692556286852607, -168.8130981290893260, 59.65701158161632378 ) ) ;
#10544=CARTESIAN_POINT ( 'NONE',  ( -149.8854112254399524, -191.3899795514095956, 39.65701158161630957 ) ) ;
#10547=CARTESIAN_POINT ( 'NONE',  ( -159.5594255724347761, -172.2630981290892862, 55.53486410454104316 ) ) ;
#10552=CARTESIAN_POINT ( 'NONE',  ( -148.3790856849358306, -183.3891397928654783, 40.14644641866477315 ) ) ;
#10559=CARTESIAN_POINT ( 'NONE',  ( -151.4692556286852607, -169.7391397928654442, 59.65701158161632378 ) ) ;
#10569=CARTESIAN_POINT ( 'NONE',  ( -148.5561028927606344, -160.2584106276440536, 58.62277379824867296 ) ) ;
#10570=CARTESIAN_POINT ( 'NONE',  ( -151.4692556286852891, -182.6438272943106824, 39.74470866294723947 ) ) ;
#10578=CARTESIAN_POINT ( 'NONE',  ( -161.4692556286853176, -188.4891397928654726, 49.65701158161630957 ) ) ;
#10579=CARTESIAN_POINT ( 'NONE',  ( -145.6429501568359797, -163.1084106276440195, 57.67623309621197336 ) ) ;
#10587=CARTESIAN_POINT ( 'NONE',  ( -161.4692556286852891, -160.4130981290893203, 52.90620854394536821 ) ) ;
#10588=ORIENTED_EDGE ( 'NONE', *, *, #9100, .T. ) ;
#10597=EDGE_CURVE ( 'NONE', #10835, #6960, #21328, .T. ) ;
#10598=EDGE_CURVE ( 'NONE', #11010, #8663, #12299, .T. ) ;
#10599=LINE ( 'NONE', #2535, #19864 ) ;
#10603=CARTESIAN_POINT ( 'NONE',  ( -143.8425227516148084, -183.0938272943107279, 44.11586579668791330 ) ) ;
#10604=CARTESIAN_POINT ( 'NONE',  ( -160.8964159109769696, -194.0084106276440252, 52.72008163687743121 ) ) ;
#10606=CARTESIAN_POINT ( 'NONE',  ( -157.2955611005346270, -176.6084106276440195, 41.63779006702063867 ) ) ;
#10610=DIRECTION ( 'NONE',  ( -0.4999999999999996114, 0.000000000000000000, -0.8660254037844388186 ) ) ;
#10625=CARTESIAN_POINT ( 'NONE',  ( -159.5594255724347761, -167.7891397928654840, 43.77915905869157598 ) ) ;
#10632=VECTOR ( 'NONE', #14038, 1000.000000000000000 ) ;
#10637=CARTESIAN_POINT ( 'NONE',  ( -143.8425227516148084, -195.3584106276440480, 44.11586579668791330 ) ) ;
#10653=CARTESIAN_POINT ( 'NONE',  ( -151.4692556286852891, -192.8130981290892692, 59.65701158161632378 ) ) ;
#10657=CARTESIAN_POINT ( 'NONE',  ( -151.4692556286852891, -158.3130981290892976, 39.14238933923362396 ) ) ;
#10662=CARTESIAN_POINT ( 'NONE',  ( -148.5561028927606344, -192.9938272943107336, 58.62277379824867296 ) ) ;
#10668=FACE_OUTER_BOUND ( 'NONE', #1496, .T. ) ;
#10672=CARTESIAN_POINT ( 'NONE',  ( -141.4692556286852891, -172.1391397928654783, 52.90620854394536821 ) ) ;
#10676=CARTESIAN_POINT ( 'NONE',  ( -160.8964159109769696, -182.0438272943107449, 46.59394152635518083 ) ) ;
#10678=CARTESIAN_POINT ( 'NONE',  ( -159.5594255724347761, -190.2630981290893146, 55.53486410454104316 ) ) ;
#10686=CARTESIAN_POINT ( 'NONE',  ( -157.2955611005345986, -164.6084106276440480, 41.63779006702063867 ) ) ;
#10689=( BOUNDED_CURVE ( )  B_SPLINE_CURVE ( 2, ( #500, #18908, #8781, #15496, #3814, #10540, #17241, #2155, #8890, #7236, #13937, #5559, #19021 ),
 .UNSPECIFIED., .F., .F. ) 
 B_SPLINE_CURVE_WITH_KNOTS ( ( 3, 2, 2, 2, 2, 2, 3 ),
 ( 0.3392857142857142461, 0.3428571428571428603, 0.3499999999999999778, 0.3571428571428571508, 0.3642857142857142683, 0.3714285714285714413, 0.3750000000000000000 ),
 .UNSPECIFIED. ) 
 CURVE ( )  GEOMETRIC_REPRESENTATION_ITEM ( )  RATIONAL_B_SPLINE_CURVE ( ( 0.9755282581475768211, 0.9755282581475765991, 1.000000000000000000, 0.9510565162951535312, 1.000000000000000000, 0.9510565162951535312, 1.000000000000000000, 0.9510565162951535312, 1.000000000000000000, 0.9510565162951535312, 1.000000000000000000, 0.9755282581475768211, 0.9755282581475768211 ) ) 
 REPRESENTATION_ITEM ( '' )  );
#10712=CARTESIAN_POINT ( 'NONE',  ( -148.5561028927606344, -182.7938272943107449, 40.69124936498395328 ) ) ;
#10713=CARTESIAN_POINT ( 'NONE',  ( -142.0420953463936087, -192.6584106276440593, 49.65701158161630957 ) ) ;
#10715=CARTESIAN_POINT ( 'NONE',  ( -151.4692556286852891, -175.4084106276440878, 59.56931450028537967 ) ) ;
#10733=FACE_OUTER_BOUND ( 'NONE', #18497, .T. ) ;
#10734=CARTESIAN_POINT ( 'NONE',  ( -141.4692556286852891, -174.9891397928654726, 49.65701158161630957 ) ) ;
#10736=CARTESIAN_POINT ( 'NONE',  ( -159.5594255724347761, -163.8630981290893089, 43.77915905869157598 ) ) ;
#10739=CARTESIAN_POINT ( 'NONE',  ( -160.8964159109769696, -160.7438272943107052, 52.72008163687743121 ) ) ;
#10749=DIRECTION ( 'NONE',  ( -0.000000000000000000, 1.000000000000000000, -0.000000000000000000 ) ) ;
#10750=EDGE_LOOP ( 'NONE', ( #21683, #21075, #4887, #17366 ) ) ;
#10754=CARTESIAN_POINT ( 'NONE',  ( -158.9748091281504401, -116.9891397928655010, 62.65701158161630957 ) ) ;
#10759=CARTESIAN_POINT ( 'NONE',  ( -141.4692556286852891, -155.9130981290893203, 46.40781461928724383 ) ) ;
#10766=CARTESIAN_POINT ( 'NONE',  ( -160.8964159109769696, -193.7438272943106767, 52.72008163687743121 ) ) ;
#10779=CARTESIAN_POINT ( 'NONE',  ( -151.4692556286852607, -165.8130981290893260, 59.65701158161632378 ) ) ;
#10783=CARTESIAN_POINT ( 'NONE',  ( -157.2955611005345986, -173.3438272943107279, 41.63779006702063867 ) ) ;
#10785=CARTESIAN_POINT ( 'NONE',  ( -151.4692556286852891, -191.3130981290893260, 39.14238933923362396 ) ) ;
#10794=CARTESIAN_POINT ( 'NONE',  ( -157.2955611005345986, -167.6084106276440195, 41.63779006702063867 ) ) ;
#10802=CARTESIAN_POINT ( 'NONE',  ( -157.6495955161842062, -160.1130981290893089, 58.16351966513671812 ) ) ;
#10806=VECTOR ( 'NONE', #5837, 1000.000000000000000 ) ;
#10817=( BOUNDED_CURVE ( )  B_SPLINE_CURVE ( 2, ( #5952, #8849, #12680, #783, #5515, #9172, #3879, #5739, #4090, #3771, #7518, #10604, #17308, #2112, #19088, #2220, #17632, #15770, #15556, #7190, #10713, #13895, #14219, #15870, #8950, #17416, #15978, #14005, #2540, #20633, #20959, #7304, #9277, #20739, #3988, #12462, #2321, #9060, #7410, #674, #10821, #9499, #1215, #8057, #12900, #4515, #19843, #4734, #19733, #2758, #11453, #4626, #21506, #7949, #13012, #16520, #7737, #6280, #19402, #16414, #11345, #18182, #16196, #21172, #2975, #14438, #11133, #11025, #1108, #2643, #9713, #6063, #8166, #18068, #1436, #9822, #1324, #19509, #16305, #14872, #17737, #21287, #14763, #4402, #19621, #11238, #3089, #21617, #6393, #7843, #6508, #13121, #4298, #14654, #9385, #16090, #12790, #1000, #17848, #14545, #6166, #17958, #2863, #9606, #21394, #1547, #4966, #4850, #18412, #18299, #18628, #14979, #1981, #13550, #10366, #3640, #10258, #13342, #10150, #8714, #11570, #15097, #16960, #20079, #5075, #329, #16746, #1, #3533, #10042, #6742, #1872, #20392, #13450, #17067, #5289, #216, #1656, #112, #6952, #1766, #20287, #8388, #15213, #3429, #6844, #3201, #11678, #5181, #8602, #15322, #15433, #11900, #13228, #16636, #21724, #3312, #6628, #20184, #11789, #13659, #9931, #8278, #12003, #18520, #19965, #16851, #8500, #18737, #8823, #20823, #438, #9036, #651, #7059, #4065, #7168, #13871, #4175, #15632, #20609, #19165, #10903, #10477, #2409, #17607, #18841, #10794, #5714, #5492, #20716, #19274, #17282, #14194, #17177, #12439, #5393, #20934, #2090, #12219, #17392, #5600, #12326, #5815, #2513, #15846, #18953, #10686, #17498, #9146, #15532, #757, #3854, #15746, #7387, #13763, #7493, #10579, #2197, #9253, #537, #12546, #15953, #20505, #8927, #12109, #3747, #7277, #13978, #19061, #3964, #2295, #14087, #11106, #8032, #4273, #6253, #21044, #14739, #17712, #971, #9355, #4598, #4484, #19591, #11212, #21149, #5927, #9798, #7921, #12656, #17820, #19707, #21363, #19378, #16282, #9688, #18151, #11002, #12763, #11317, #2617, #9577, #864, #18041, #1188, #12872, #7600, #19484 ),
 .UNSPECIFIED., .F., .F. ) 
 B_SPLINE_CURVE_WITH_KNOTS ( ( 3, 2, 2, 2, 2, 2, 2, 2, 2, 2, 2, 2, 2, 2, 2, 2, 2, 2, 2, 2, 2, 2, 2, 2, 2, 2, 2, 2, 2, 2, 2, 2, 2, 2, 2, 2, 2, 2, 2, 2, 2, 2, 2, 2, 2, 2, 2, 2, 2, 2, 2, 2, 2, 2, 2, 2, 2, 2, 2, 2, 2, 2, 2, 2, 2, 2, 2, 2, 2, 2, 2, 2, 2, 2, 2, 2, 2, 2, 2, 2, 2, 2, 2, 2, 2, 2, 2, 2, 2, 2, 2, 2, 2, 2, 2, 2, 2, 2, 2, 2, 2, 2, 2, 2, 2, 2, 2, 2, 2, 2, 2, 2, 2, 2, 2, 2, 2, 2, 2, 2, 2, 2, 2, 2, 2, 2, 2, 2, 2, 2, 2, 2, 2, 2, 3 ),
 ( 0.000000000000000000, 0.007142857142857142634, 0.01428571428571428527, 0.02142857142857142877, 0.02857142857142857054, 0.03571428571428571230, 0.04285714285714285754, 0.05000000000000000278, 0.05714285714285714107, 0.06428571428571427937, 0.07142857142857142461, 0.07857142857142856984, 0.08571428571428571508, 0.09285714285714286031, 0.1000000000000000056, 0.1071428571428571369, 0.1142857142857142821, 0.1214285714285714274, 0.1285714285714285587, 0.1357142857142857040, 0.1428571428571428492, 0.1499999999999999944, 0.1571428571428571397, 0.1642857142857142849, 0.1714285714285714302, 0.1785714285714285754, 0.1857142857142857206, 0.1928571428571428659, 0.2000000000000000111, 0.2071428571428571563, 0.2142857142857142738, 0.2214285714285714191, 0.2285714285714285643, 0.2357142857142857095, 0.2428571428571428548, 0.2500000000000000000, 0.2571428571428571175, 0.2642857142857142905, 0.2714285714285714080, 0.2785714285714285809, 0.2857142857142856984, 0.2928571428571428714, 0.2999999999999999889, 0.3071428571428571619, 0.3142857142857142794, 0.3214285714285713969, 0.3285714285714285698, 0.3357142857142856873, 0.3428571428571428603, 0.3499999999999999778, 0.3571428571428571508, 0.3642857142857142683, 0.3714285714285714413, 0.3785714285714285587, 0.3857142857142857317, 0.3928571428571429047, 0.4000000000000000222, 0.4071428571428571397, 0.4142857142857143127, 0.4214285714285714302, 0.4285714285714285476, 0.4357142857142857206, 0.4428571428571428381, 0.4500000000000000111, 0.4571428571428571286, 0.4642857142857142461, 0.4714285714285714191, 0.4785714285714285920, 0.4857142857142857095, 0.4928571428571428825, 0.5000000000000000000, 0.5071428571428571175, 0.5142857142857142350, 0.5214285714285714635, 0.5285714285714285809, 0.5357142857142856984, 0.5428571428571428159, 0.5500000000000000444, 0.5571428571428571619, 0.5642857142857142794, 0.5714285714285713969, 0.5785714285714286254, 0.5857142857142857428, 0.5928571428571428603, 0.5999999999999999778, 0.6071428571428570953, 0.6142857142857143238, 0.6214285714285714413, 0.6285714285714285587, 0.6357142857142856762, 0.6428571428571427937, 0.6500000000000000222, 0.6571428571428571397, 0.6642857142857142572, 0.6714285714285713746, 0.6785714285714286031, 0.6857142857142857206, 0.6928571428571428381, 0.6999999999999999556, 0.7071428571428571841, 0.7142857142857143016, 0.7214285714285714191, 0.7285714285714285365, 0.7357142857142857650, 0.7428571428571428825, 0.7500000000000000000, 0.7571428571428571175, 0.7642857142857142350, 0.7714285714285714635, 0.7785714285714285809, 0.7857142857142858094, 0.7928571428571428159, 0.8000000000000000444, 0.8071428571428571619, 0.8142857142857142794, 0.8214285714285713969, 0.8285714285714286254, 0.8357142857142857428, 0.8428571428571428603, 0.8499999999999999778, 0.8571428571428570953, 0.8642857142857143238, 0.8714285714285714413, 0.8785714285714285587, 0.8857142857142856762, 0.8928571428571429047, 0.9000000000000000222, 0.9071428571428571397, 0.9142857142857142572, 0.9214285714285713746, 0.9285714285714284921, 0.9357142857142857206, 0.9428571428571428381, 0.9499999999999999556, 0.9523897249335834259 ),
 .UNSPECIFIED. ) 
 CURVE ( )  GEOMETRIC_REPRESENTATION_ITEM ( )  RATIONAL_B_SPLINE_CURVE ( ( 1.000000000000000000, 0.9510565162951535312, 1.000000000000000000, 0.9510565162951535312, 1.000000000000000000, 0.9510565162951535312, 1.000000000000000000, 0.9510565162951535312, 1.000000000000000000, 0.9510565162951535312, 1.000000000000000000, 0.9510565162951535312, 1.000000000000000000, 0.9510565162951535312, 1.000000000000000000, 0.9510565162951535312, 1.000000000000000000, 0.9510565162951535312, 1.000000000000000000, 0.9510565162951535312, 1.000000000000000000, 0.9510565162951535312, 1.000000000000000000, 0.9510565162951535312, 1.000000000000000000, 0.9510565162951535312, 1.000000000000000000, 0.9510565162951535312, 1.000000000000000000, 0.9510565162951535312, 1.000000000000000000, 0.9510565162951535312, 1.000000000000000000, 0.9510565162951535312, 1.000000000000000000, 0.9510565162951535312, 1.000000000000000000, 0.9510565162951535312, 1.000000000000000000, 0.9510565162951535312, 1.000000000000000000, 0.9510565162951535312, 1.000000000000000000, 0.9510565162951535312, 1.000000000000000000, 0.9510565162951535312, 1.000000000000000000, 0.9510565162951535312, 1.000000000000000000, 0.9510565162951535312, 1.000000000000000000, 0.9510565162951535312, 1.000000000000000000, 0.9510565162951535312, 1.000000000000000000, 0.9510565162951535312, 1.000000000000000000, 0.9510565162951535312, 1.000000000000000000, 0.9510565162951535312, 1.000000000000000000, 0.9510565162951535312, 1.000000000000000000, 0.9510565162951535312, 1.000000000000000000, 0.9510565162951535312, 1.000000000000000000, 0.9510565162951535312, 1.000000000000000000, 0.9510565162951535312, 1.000000000000000000, 0.9510565162951535312, 1.000000000000000000, 0.9510565162951535312, 1.000000000000000000, 0.9510565162951535312, 1.000000000000000000, 0.9510565162951535312, 1.000000000000000000, 0.9510565162951535312, 1.000000000000000000, 0.9510565162951535312, 1.000000000000000000, 0.9510565162951535312, 1.000000000000000000, 0.9510565162951535312, 1.000000000000000000, 0.9510565162951535312, 1.000000000000000000, 0.9510565162951535312, 1.000000000000000000, 0.9510565162951535312, 1.000000000000000000, 0.9510565162951535312, 1.000000000000000000, 0.9510565162951535312, 1.000000000000000000, 0.9510565162951535312, 1.000000000000000000, 0.9510565162951535312, 1.000000000000000000, 0.9510565162951535312, 1.000000000000000000, 0.9510565162951535312, 1.000000000000000000, 0.9510565162951535312, 1.000000000000000000, 0.9510565162951535312, 1.000000000000000000, 0.9510565162951535312, 1.000000000000000000, 0.9510565162951535312, 1.000000000000000000, 0.9510565162951535312, 1.000000000000000000, 0.9510565162951535312, 1.000000000000000000, 0.9510565162951535312, 1.000000000000000000, 0.9510565162951535312, 1.000000000000000000, 0.9510565162951535312, 1.000000000000000000, 0.9510565162951535312, 1.000000000000000000, 0.9510565162951535312, 1.000000000000000000, 0.9510565162951535312, 1.000000000000000000, 0.9510565162951535312, 1.000000000000000000, 0.9510565162951535312, 1.000000000000000000, 0.9510565162951535312, 1.000000000000000000, 0.9510565162951535312, 1.000000000000000000, 0.9510565162951535312, 1.000000000000000000, 0.9510565162951535312, 1.000000000000000000, 0.9510565162951535312, 1.000000000000000000, 0.9510565162951535312, 1.000000000000000000, 0.9510565162951535312, 1.000000000000000000, 0.9510565162951535312, 1.000000000000000000, 0.9510565162951535312, 1.000000000000000000, 0.9510565162951535312, 1.000000000000000000, 0.9510565162951535312, 1.000000000000000000, 0.9510565162951535312, 1.000000000000000000, 0.9510565162951535312, 1.000000000000000000, 0.9510565162951535312, 1.000000000000000000, 0.9510565162951535312, 1.000000000000000000, 0.9510565162951535312, 1.000000000000000000, 0.9510565162951535312, 1.000000000000000000, 0.9510565162951535312, 1.000000000000000000, 0.9510565162951535312, 1.000000000000000000, 0.9510565162951535312, 1.000000000000000000, 0.9510565162951535312, 1.000000000000000000, 0.9510565162951535312, 1.000000000000000000, 0.9510565162951535312, 1.000000000000000000, 0.9510565162951535312, 1.000000000000000000, 0.9510565162951535312, 1.000000000000000000, 0.9510565162951535312, 1.000000000000000000, 0.9510565162951535312, 1.000000000000000000, 0.9510565162951535312, 1.000000000000000000, 0.9510565162951535312, 1.000000000000000000, 0.9510565162951535312, 1.000000000000000000, 0.9510565162951535312, 1.000000000000000000, 0.9510565162951535312, 1.000000000000000000, 0.9510565162951535312, 1.000000000000000000, 0.9510565162951535312, 1.000000000000000000, 0.9510565162951535312, 1.000000000000000000, 0.9510565162951535312, 1.000000000000000000, 0.9510565162951535312, 1.000000000000000000, 0.9510565162951535312, 1.000000000000000000, 0.9510565162951535312, 1.000000000000000000, 0.9510565162951535312, 1.000000000000000000, 0.9510565162951535312, 1.000000000000000000, 0.9510565162951535312, 1.000000000000000000, 0.9510565162951535312, 1.000000000000000000, 0.9510565162951535312, 1.000000000000000000, 0.9510565162951535312, 1.000000000000000000, 0.9510565162951535312, 1.000000000000000000, 0.9510565162951535312, 1.000000000000000000, 0.9510565162951535312, 1.000000000000000000, 0.9510565162951535312, 1.000000000000000000, 0.9510565162951535312, 1.000000000000000000, 0.9510565162951535312, 1.000000000000000000, 0.9510565162951535312, 1.000000000000000000, 0.9510565162951535312, 1.000000000000000000, 0.9510565162951535312, 1.000000000000000000, 0.9510565162951535312, 1.000000000000000000, 0.9510565162951535312, 1.000000000000000000, 0.9510565162951535312, 1.000000000000000000, 0.9510565162951535312, 1.000000000000000000, 0.9510565162951535312, 1.000000000000000000, 0.9510565162951535312, 1.000000000000000000, 0.9510565162951535312, 1.000000000000000000, 0.9510565162951535312, 1.000000000000000000, 0.9510565162951535312, 1.000000000000000000, 0.9510565162951535312, 1.000000000000000000, 0.9510565162951535312, 1.000000000000000000, 0.9510565162951535312, 1.000000000000000000, 0.9510565162951535312, 1.000000000000000000, 0.9836253951315730992, 0.9782074146920101132 ) ) 
 REPRESENTATION_ITEM ( '' )  );
#10820=CARTESIAN_POINT ( 'NONE',  ( -143.8425227516148084, -183.6938272943107506, 55.19815736654470584 ) ) ;
#10821=CARTESIAN_POINT ( 'NONE',  ( -142.0420953463936087, -189.6584106276440593, 49.65701158161630957 ) ) ;
#10824=CARTESIAN_POINT ( 'NONE',  ( -142.0420953463936087, -174.6584106276440593, 49.65701158161630957 ) ) ;
#10835=VERTEX_POINT ( 'NONE', #8943 ) ;
#10841=AXIS2_PLACEMENT_3D ( 'NONE', #14352, #9408, #15998 ) ;
#10844=CARTESIAN_POINT ( 'NONE',  ( -151.4692556286853176, -179.3130981290892976, 39.65701158161629536 ) ) ;
#10845=CARTESIAN_POINT ( 'NONE',  ( -151.4692556286852891, -171.2391397928654442, 39.14238933923362396 ) ) ;
#10846=CARTESIAN_POINT ( 'NONE',  ( -141.4692556286852891, -159.2130981290893033, 52.90620854394536821 ) ) ;
#10849=PLANE ( 'NONE',  #4998 ) ;
#10850=ORIENTED_EDGE ( 'NONE', *, *, #868, .T. ) ;
#10852=CARTESIAN_POINT ( 'NONE',  ( -160.8964159109769696, -161.0438272943107449, 46.59394152635518793 ) ) ;
#10856=VERTEX_POINT ( 'NONE', #18856 ) ;
#10866=CARTESIAN_POINT ( 'NONE',  ( -151.4692556286852891, -196.9891397928655010, 59.65701158161632378 ) ) ;
#10871=CARTESIAN_POINT ( 'NONE',  ( -156.4692864601532847, -155.0638355923473739, 40.99677534440144910 ) ) ;
#10873=ADVANCED_FACE ( 'NONE', ( #13780 ), #3056, .T. ) ;
#10874=CARTESIAN_POINT ( 'NONE',  ( -151.4692556286852891, -196.9891397928655010, 49.65701158161630957 ) ) ;
#10878=CARTESIAN_POINT ( 'NONE',  ( -154.3824083646099439, -194.4938272943107336, 40.69124936498395328 ) ) ;
#10885=CARTESIAN_POINT ( 'NONE',  ( -151.4692556286852891, -196.9891397928655010, 49.65701158161630957 ) ) ;
#10887=EDGE_LOOP ( 'NONE', ( #6750, #18654, #17968, #18311 ) ) ;
#10894=CARTESIAN_POINT ( 'NONE',  ( -142.0420953463935803, -168.5438272943107165, 52.72008163687743831 ) ) ;
#10896=CARTESIAN_POINT ( 'NONE',  ( -154.5594255724347761, -183.9630981290893033, 59.16757674456785310 ) ) ;
#10903=CARTESIAN_POINT ( 'NONE',  ( -143.8425227516148084, -168.3584106276440480, 44.11586579668791330 ) ) ;
#10904=AXIS2_PLACEMENT_3D ( 'NONE', #10000, #13617, #16922 ) ;
#10920=CARTESIAN_POINT ( 'NONE',  ( -154.5594255724347761, -186.9630981290893033, 59.16757674456785310 ) ) ;
#10925=CARTESIAN_POINT ( 'NONE',  ( -157.2955611005346270, -172.4438272943107506, 57.67623309621198047 ) ) ;
#10926=ORIENTED_EDGE ( 'NONE', *, *, #20650, .T. ) ;
#10927=CARTESIAN_POINT ( 'NONE',  ( -145.6429501568359797, -181.1084106276440195, 57.67623309621198047 ) ) ;
#10941=( BOUNDED_CURVE ( )  B_SPLINE_CURVE ( 2, ( #6798, #5130, #11849, #18578, #10208, #8770, #16911 ),
 .UNSPECIFIED., .F., .F. ) 
 B_SPLINE_CURVE_WITH_KNOTS ( ( 3, 2, 2, 3 ),
 ( 0.000000000000000000, 0.007142857142857142634, 0.01428571428571428527, 0.01785714285714286656 ),
 .UNSPECIFIED. ) 
 CURVE ( )  GEOMETRIC_REPRESENTATION_ITEM ( )  RATIONAL_B_SPLINE_CURVE ( ( 1.000000000000000000, 0.9510565162951535312, 1.000000000000000000, 0.9510565162951535312, 1.000000000000000000, 0.9755282581475767101, 0.9755282581475768211 ) ) 
 REPRESENTATION_ITEM ( '' )  );
#10946=CARTESIAN_POINT ( 'NONE',  ( -141.4692556286852891, -160.1391397928654499, 52.90620854394536821 ) ) ;
#10949=DIRECTION ( 'NONE',  ( 0.4999999999999996114, 0.000000000000000000, 0.8660254037844388186 ) ) ;
#10952=CARTESIAN_POINT ( 'NONE',  ( -142.0420953463935803, -162.5438272943106881, 52.72008163687743831 ) ) ;
#10954=DIRECTION ( 'NONE',  ( 0.8660400450101282122, -5.766140419743141397E-05, -0.4999746364707088886 ) ) ;
#10960=CARTESIAN_POINT ( 'NONE',  ( -151.4692556286852891, -196.9891397928655010, 49.65701158161630957 ) ) ;
#10964=CIRCLE ( 'NONE', #6774, 9.000000000000007105 ) ;
#10966=CARTESIAN_POINT ( 'NONE',  ( -159.5594255724347761, -191.1891397928654897, 55.53486410454104316 ) ) ;
#10968=DIRECTION ( 'NONE',  ( 0.000000000000000000, 0.000000000000000000, 1.000000000000000000 ) ) ;
#10969=CARTESIAN_POINT ( 'NONE',  ( -151.4692556286852891, -162.8130981290893260, 60.17163382399899518 ) ) ;
#10974=CARTESIAN_POINT ( 'NONE',  ( -154.3824083646099439, -188.4938272943107336, 40.69124936498395328 ) ) ;
#10982=CARTESIAN_POINT ( 'NONE',  ( -145.2889157411863437, -169.4391397928654328, 58.16351966513671812 ) ) ;
#10986=EDGE_LOOP ( 'NONE', ( #1689, #1010, #874, #18746 ) ) ;
#10993=CARTESIAN_POINT ( 'NONE',  ( -143.8425227516148084, -168.0938272943107563, 44.11586579668791330 ) ) ;
#10995=CARTESIAN_POINT ( 'NONE',  ( -157.6495955161842062, -191.0130981290893146, 41.15050349809590102 ) ) ;
#11002=CARTESIAN_POINT ( 'NONE',  ( -143.8425227516148084, -156.9584106276440423, 55.19815736654470584 ) ) ;
#11007=ORIENTED_EDGE ( 'NONE', *, *, #4516, .F. ) ;
#11010=VERTEX_POINT ( 'NONE', #20625 ) ;
#11020=CARTESIAN_POINT ( 'NONE',  ( -153.0531000319306543, -188.2362167067690848, 39.65701158161630246 ) ) ;
#11021=DIRECTION ( 'NONE',  ( -0.000000000000000000, 1.000000000000000000, -0.000000000000000000 ) ) ;
#11024=CARTESIAN_POINT ( 'NONE',  ( -160.8964159109769696, -169.7438272943106767, 52.72008163687743121 ) ) ;
#11025=CARTESIAN_POINT ( 'NONE',  ( -157.2955611005345986, -185.6084106276440195, 41.63779006702063867 ) ) ;
#11027=CARTESIAN_POINT ( 'NONE',  ( -151.4692556286852891, -169.4084106276440593, 59.56931450028537967 ) ) ;
#11033=ORIENTED_EDGE ( 'NONE', *, *, #882, .F. ) ;
#11043=CARTESIAN_POINT ( 'NONE',  ( -159.5594255724347761, -161.7891397928654555, 43.77915905869157598 ) ) ;
#11044=CARTESIAN_POINT ( 'NONE',  ( -143.3790856849358306, -158.7630981290893146, 43.77915905869157598 ) ) ;
#11045=UNCERTAINTY_MEASURE_WITH_UNIT (LENGTH_MEASURE( 1.000000000000000082E-05 ), #21064, 'distance_accuracy_value', 'NONE');
#11047=FACE_OUTER_BOUND ( 'NONE', #15907, .T. ) ;
#11048=ORIENTED_EDGE ( 'NONE', *, *, #1822, .F. ) ;
#11050=CARTESIAN_POINT ( 'NONE',  ( -160.8964159109769696, -163.7438272943107336, 52.72008163687743121 ) ) ;
#11053=ORIENTED_EDGE ( 'NONE', *, *, #14612, .T. ) ;
#11060=ORIENTED_EDGE ( 'NONE', *, *, #18850, .F. ) ;
#11068=CARTESIAN_POINT ( 'NONE',  ( -145.2889157411863721, -186.5391397928654271, 41.15050349809590102 ) ) ;
#11072=CARTESIAN_POINT ( 'NONE',  ( -141.4692556286852891, -162.0630981290892976, 49.65701158161630957 ) ) ;
#11076=CARTESIAN_POINT ( 'NONE',  ( -145.6429501568359797, -194.9438272943107222, 41.63779006702063867 ) ) ;
#11097=CARTESIAN_POINT ( 'NONE',  ( -160.8964159109769696, -170.0438272943107165, 46.59394152635518083 ) ) ;
#11099=CARTESIAN_POINT ( 'NONE',  ( -154.5594255724347761, -186.9630981290893033, 59.16757674456785310 ) ) ;
#11106=CARTESIAN_POINT ( 'NONE',  ( -157.2955611005345986, -160.7084106276440423, 57.67623309621197336 ) ) ;
#11108=DIRECTION ( 'NONE',  ( 0.000000000000000000, -1.000000000000000000, 0.000000000000000000 ) ) ;
#11125=CARTESIAN_POINT ( 'NONE',  ( -161.4692556286853176, -157.5630981290892976, 49.65701158161630957 ) ) ;
#11132=CARTESIAN_POINT ( 'NONE',  ( -159.0959885057557983, -166.5938272943107563, 55.19815736654470584 ) ) ;
#11133=CARTESIAN_POINT ( 'NONE',  ( -154.3824083646099439, -185.7584106276440536, 40.69124936498395328 ) ) ;
#11136=CARTESIAN_POINT ( 'NONE',  ( -154.3824083646099439, -169.5584106276440366, 58.62277379824867296 ) ) ;
#11153=CARTESIAN_POINT ( 'NONE',  ( -161.4692556286853176, -161.4891397928654726, 49.65701158161630957 ) ) ;
#11157=CARTESIAN_POINT ( 'NONE',  ( -153.0531000319306827, -186.1622583705452030, 39.65701158161629536 ) ) ;
#11158=ORIENTED_EDGE ( 'NONE', *, *, #19749, .T. ) ;
#11160=CARTESIAN_POINT ( 'NONE',  ( -160.8964159109769696, -194.1584106276440593, 49.65701158161630957 ) ) ;
#11162=CARTESIAN_POINT ( 'NONE',  ( -151.4692556286852891, -190.4084106276440309, 59.56931450028537967 ) ) ;
#11178=CARTESIAN_POINT ( 'NONE',  ( -161.4692556286852607, -185.3391397928654953, 52.90620854394536821 ) ) ;
#11181=CARTESIAN_POINT ( 'NONE',  ( -148.5561028927606344, -186.9938272943107336, 58.62277379824867296 ) ) ;
#11186=CARTESIAN_POINT ( 'NONE',  ( -142.0420953463936087, -183.3938272943107108, 49.65701158161630957 ) ) ;
#11188=CARTESIAN_POINT ( 'NONE',  ( -143.3790856849358306, -161.7630981290893146, 43.77915905869157598 ) ) ;
#11203=CARTESIAN_POINT ( 'NONE',  ( -142.0420953463935803, -168.2438272943107336, 46.59394152635518083 ) ) ;
#11205=CARTESIAN_POINT ( 'NONE',  ( -159.5594255724347761, -178.8630981290893089, 43.77915905869157598 ) ) ;
#11212=CARTESIAN_POINT ( 'NONE',  ( -151.4692556286852891, -158.9084106276440309, 39.74470866294723947 ) ) ;
#11219=ORIENTED_EDGE ( 'NONE', *, *, #3557, .F. ) ;
#11225=CARTESIAN_POINT ( 'NONE',  ( -145.6429501568359797, -169.1084106276440480, 57.67623309621198047 ) ) ;
#11231=CARTESIAN_POINT ( 'NONE',  ( -153.0531000319306543, -189.8899795514095672, 59.65701158161630957 ) ) ;
#11237=CARTESIAN_POINT ( 'NONE',  ( -148.5561028927606344, -173.7938272943107165, 40.69124936498395328 ) ) ;
#11238=CARTESIAN_POINT ( 'NONE',  ( -151.4692556286852891, -182.9084106276440025, 39.74470866294723947 ) ) ;
#11241=CARTESIAN_POINT ( 'NONE',  ( -143.8425227516148084, -165.9584106276440423, 55.19815736654470584 ) ) ;
#11249=EDGE_CURVE ( 'NONE', #1447, #7574, #13325, .T. ) ;
#11256=CARTESIAN_POINT ( 'NONE',  ( -157.6495955161842062, -164.9391397928654612, 41.15050349809590102 ) ) ;
#11259=DIRECTION ( 'NONE',  ( 0.000000000000000000, 0.000000000000000000, 1.000000000000000000 ) ) ;
#11265=CARTESIAN_POINT ( 'NONE',  ( -160.8964159109769696, -194.3084106276440366, 46.59394152635518793 ) ) ;
#11267=CARTESIAN_POINT ( 'NONE',  ( -142.0420953463936087, -183.6584106276440309, 49.65701158161630957 ) ) ;
#11276=CARTESIAN_POINT ( 'NONE',  ( -156.4692864601533131, -155.0638355923473455, 40.99677534440144200 ) ) ;
#11278=EDGE_CURVE ( 'NONE', #5881, #20985, #5721, .T. ) ;
#11284=CARTESIAN_POINT ( 'NONE',  ( -148.3790856849358306, -193.5891397928654669, 59.16757674456786020 ) ) ;
#11287=CARTESIAN_POINT ( 'NONE',  ( -148.5561028927606344, -192.9938272943107336, 58.62277379824867296 ) ) ;
#11306=CARTESIAN_POINT ( 'NONE',  ( -157.2955611005345986, -166.4438272943107222, 57.67623309621197336 ) ) ;
#11307=CARTESIAN_POINT ( 'NONE',  ( -145.2889157411863437, -165.5391397928654555, 41.15050349809589392 ) ) ;
#11308=CARTESIAN_POINT ( 'NONE',  ( -141.4692556286852891, -180.0630981290892976, 49.65701158161630957 ) ) ;
#11317=CARTESIAN_POINT ( 'NONE',  ( -142.0420953463936087, -156.6584106276440593, 49.65701158161630957 ) ) ;
#11321=CARTESIAN_POINT ( 'NONE',  ( -141.4692556286852891, -187.1391397928654499, 52.90620854394536821 ) ) ;
#11322=VECTOR ( 'NONE', #2259, 1000.000000000000000 ) ;
#11324=CARTESIAN_POINT ( 'NONE',  ( -148.3790856849358306, -157.5891397928654953, 59.16757674456786020 ) ) ;
#11334=CARTESIAN_POINT ( 'NONE',  ( -143.8425227516148084, -165.3584106276440480, 44.11586579668791330 ) ) ;
#11336=CARTESIAN_POINT ( 'NONE',  ( -161.4692556286852891, -178.7130981290893033, 46.40781461928724383 ) ) ;
#11344=CARTESIAN_POINT ( 'NONE',  ( -142.0420953463935803, -174.2438272943107052, 46.59394152635518793 ) ) ;
#11345=CARTESIAN_POINT ( 'NONE',  ( -142.0420953463936087, -186.6584106276440309, 49.65701158161630957 ) ) ;
#11348=CARTESIAN_POINT ( 'NONE',  ( -160.8964159109769696, -167.3084106276440366, 46.59394152635518793 ) ) ;
#11361=CARTESIAN_POINT ( 'NONE',  ( -151.4692556286853176, -164.3130981290893260, 39.65701158161629536 ) ) ;
#11372=CYLINDRICAL_SURFACE ( 'NONE', #3939, 10.00000000000000888 ) ;
#11375=CARTESIAN_POINT ( 'NONE',  ( -154.3824083646099439, -191.7584106276440536, 40.69124936498395328 ) ) ;
#11377=CARTESIAN_POINT ( 'NONE',  ( -157.2955611005346270, -181.7084106276440423, 57.67623309621198047 ) ) ;
#11379=CARTESIAN_POINT ( 'NONE',  ( -161.4692556286853176, -161.4891397928654726, 49.65701158161630957 ) ) ;
#11381=( BOUNDED_CURVE ( )  B_SPLINE_CURVE ( 2, ( #6429, #18446, #5001, #13373, #14903, #6318, #18556, #8202, #6666, #13044, #15132, #20110, #13151 ),
 .UNSPECIFIED., .F., .F. ) 
 B_SPLINE_CURVE_WITH_KNOTS ( ( 3, 2, 2, 2, 2, 2, 3 ),
 ( 0.8392857142857143016, 0.8428571428571428603, 0.8499999999999999778, 0.8571428571428570953, 0.8642857142857143238, 0.8714285714285714413, 0.8750000000000000000 ),
 .UNSPECIFIED. ) 
 CURVE ( )  GEOMETRIC_REPRESENTATION_ITEM ( )  RATIONAL_B_SPLINE_CURVE ( ( 0.9755282581475768211, 0.9755282581475768211, 1.000000000000000000, 0.9510565162951535312, 1.000000000000000000, 0.9510565162951535312, 1.000000000000000000, 0.9510565162951535312, 1.000000000000000000, 0.9510565162951535312, 1.000000000000000000, 0.9755282581475768211, 0.9755282581475768211 ) ) 
 REPRESENTATION_ITEM ( '' )  );
#11391=CARTESIAN_POINT ( 'NONE',  ( -143.3790856849358306, -187.2891397928654555, 55.53486410454105027 ) ) ;
#11393=CYLINDRICAL_SURFACE ( 'NONE', #8662, 10.00000000000000888 ) ;
#11394=CARTESIAN_POINT ( 'NONE',  ( -160.8964159109769696, -190.8938272943107393, 49.65701158161630957 ) ) ;
#11398=CARTESIAN_POINT ( 'NONE',  ( -148.5561028927606344, -179.7938272943107449, 40.69124936498395328 ) ) ;
#11399=VECTOR ( 'NONE', #530, 1000.000000000000000 ) ;
#11416=CARTESIAN_POINT ( 'NONE',  ( -143.8425227516148084, -159.6938272943107222, 55.19815736654470584 ) ) ;
#11418=CARTESIAN_POINT ( 'NONE',  ( -157.6495955161842062, -175.1130981290892521, 58.16351966513671812 ) ) ;
#11425=CARTESIAN_POINT ( 'NONE',  ( -161.4692556286853176, -182.4891397928654726, 49.65701158161630957 ) ) ;
#11430=CARTESIAN_POINT ( 'NONE',  ( -149.8854112254399524, -186.3160212151857422, 39.65701158161630246 ) ) ;
#11442=CARTESIAN_POINT ( 'NONE',  ( -142.0420953463936087, -168.6584106276440593, 49.65701158161630957 ) ) ;
#11443=CARTESIAN_POINT ( 'NONE',  ( -159.0959885057557983, -190.5938272943107279, 55.19815736654470584 ) ) ;
#11447=CARTESIAN_POINT ( 'NONE',  ( -145.2889157411863437, -177.5130981290893430, 58.16351966513671812 ) ) ;
#11452=CARTESIAN_POINT ( 'NONE',  ( -159.0959885057557983, -158.1938272943107222, 44.11586579668791330 ) ) ;
#11453=CARTESIAN_POINT ( 'NONE',  ( -160.8964159109769696, -188.1584106276440593, 49.65701158161630957 ) ) ;
#11456=CARTESIAN_POINT ( 'NONE',  ( -154.3824083646099439, -172.5584106276440366, 58.62277379824867296 ) ) ;
#11472=DIRECTION ( 'NONE',  ( 0.4999999999999993894, 0.000000000000000000, -0.8660254037844389297 ) ) ;
#11478=CARTESIAN_POINT ( 'NONE',  ( -161.4692556286852891, -185.3391397928654953, 52.90620854394536821 ) ) ;
#11481=CARTESIAN_POINT ( 'NONE',  ( -148.5561028927606344, -155.7938272943107449, 40.69124936498395328 ) ) ;
#11482=EDGE_CURVE ( 'NONE', #8663, #9959, #19968, .T. ) ;
#11485=CARTESIAN_POINT ( 'NONE',  ( -160.8964159109769696, -188.0084106276440252, 52.72008163687743121 ) ) ;
#11495=ORIENTED_EDGE ( 'NONE', *, *, #72, .T. ) ;
#11504=CARTESIAN_POINT ( 'NONE',  ( -141.4692556286852891, -181.1391397928654783, 52.90620854394536821 ) ) ;
#11507=CARTESIAN_POINT ( 'NONE',  ( -143.8425227516148084, -192.6938272943107222, 55.19815736654470584 ) ) ;
#11511=( BOUNDED_CURVE ( )  B_SPLINE_CURVE ( 2, ( #19872, #11157, #6309, #3224, #19991, #4876, #7866, #11478, #3114, #9845, #6421, #16118, #19531 ),
 .UNSPECIFIED., .F., .F. ) 
 B_SPLINE_CURVE_WITH_KNOTS ( ( 3, 2, 2, 2, 2, 2, 3 ),
 ( 0.2321428571428571508, 0.2357142857142857095, 0.2428571428571428548, 0.2500000000000000000, 0.2571428571428571175, 0.2642857142857142905, 0.2678571428571429047 ),
 .UNSPECIFIED. ) 
 CURVE ( )  GEOMETRIC_REPRESENTATION_ITEM ( )  RATIONAL_B_SPLINE_CURVE ( ( 0.9755282581475767101, 0.9755282581475768211, 1.000000000000000000, 0.9510565162951535312, 1.000000000000000000, 0.9510565162951535312, 1.000000000000000000, 0.9510565162951535312, 1.000000000000000000, 0.9510565162951535312, 1.000000000000000000, 0.9755282581475763770, 0.9755282581475768211 ) ) 
 REPRESENTATION_ITEM ( '' )  );
#11513=CARTESIAN_POINT ( 'NONE',  ( -145.6429501568359797, -186.8438272943106995, 57.67623309621198047 ) ) ;
#11532=CARTESIAN_POINT ( 'NONE',  ( -154.3824083646099439, -160.2938272943107449, 58.62277379824867296 ) ) ;
#11535=CARTESIAN_POINT ( 'NONE',  ( -148.3790856849358306, -177.6630981290893203, 59.16757674456786020 ) ) ;
#11536=( NAMED_UNIT ( * ) SI_UNIT ( $, .STERADIAN. ) SOLID_ANGLE_UNIT ( ) );
#11537=CARTESIAN_POINT ( 'NONE',  ( -153.0531000319306258, -192.1622583705451746, 39.65701158161628115 ) ) ;
#11541=CARTESIAN_POINT ( 'NONE',  ( -153.0531000319306827, -181.8160212151857422, 59.65701158161632378 ) ) ;
#11542=CARTESIAN_POINT ( 'NONE',  ( -151.4692556286852607, -168.2391397928654442, 39.65701158161629536 ) ) ;
#11547=CYLINDRICAL_SURFACE ( 'NONE', #2299, 10.00000000000000888 ) ;
#11549=ORIENTED_EDGE ( 'NONE', *, *, #2767, .F. ) ;
#11558=CARTESIAN_POINT ( 'NONE',  ( -151.4692556286852891, -163.4084106276440309, 59.56931450028537967 ) ) ;
#11559=CARTESIAN_POINT ( 'NONE',  ( -148.5561028927606344, -186.9938272943107336, 58.62277379824867296 ) ) ;
#11560=CARTESIAN_POINT ( 'NONE',  ( -159.5594255724347761, -178.2630981290893146, 55.53486410454104316 ) ) ;
#11562=CARTESIAN_POINT ( 'NONE',  ( -143.3790856849358306, -188.7630981290893146, 43.77915905869157598 ) ) ;
#11569=CARTESIAN_POINT ( 'NONE',  ( -159.0959885057557983, -163.5938272943107279, 55.19815736654470584 ) ) ;
#11570=CARTESIAN_POINT ( 'NONE',  ( -142.0420953463936087, -177.6584106276440309, 49.65701158161630957 ) ) ;
#11573=CARTESIAN_POINT ( 'NONE',  ( -151.4692556286852891, -163.4084106276440309, 59.56931450028537967 ) ) ;
#11575=DIRECTION ( 'NONE',  ( 1.000000000000000000, 0.000000000000000000, -0.000000000000000000 ) ) ;
#11578=ORIENTED_EDGE ( 'NONE', *, *, #11278, .T. ) ;
#11582=( BOUNDED_CURVE ( )  B_SPLINE_CURVE ( 2, ( #10016, #5267, #18713, #13530, #16832, #10342, #17045, #18607, #20265, #10453, #8689, #3511, #13319 ),
 .UNSPECIFIED., .F., .F. ) 
 B_SPLINE_CURVE_WITH_KNOTS ( ( 3, 2, 2, 2, 2, 2, 3 ),
 ( 0.1964285714285714524, 0.2000000000000000111, 0.2071428571428571563, 0.2142857142857142738, 0.2214285714285714191, 0.2285714285714285643, 0.2321428571428571508 ),
 .UNSPECIFIED. ) 
 CURVE ( )  GEOMETRIC_REPRESENTATION_ITEM ( )  RATIONAL_B_SPLINE_CURVE ( ( 0.9755282581475767101, 0.9755282581475768211, 1.000000000000000000, 0.9510565162951535312, 1.000000000000000000, 0.9510565162951535312, 1.000000000000000000, 0.9510565162951535312, 1.000000000000000000, 0.9510565162951535312, 1.000000000000000000, 0.9755282581475765991, 0.9755282581475767101 ) ) 
 REPRESENTATION_ITEM ( '' )  );
#11585=VECTOR ( 'NONE', #12309, 1000.000000000000000 ) ;
#11598=CARTESIAN_POINT ( 'NONE',  ( -151.4692556286852891, -157.1438272943107393, 59.56931450028537967 ) ) ;
#11600=CARTESIAN_POINT ( 'NONE',  ( -159.0959885057557983, -187.8584106276440480, 55.19815736654470584 ) ) ;
#11619=CARTESIAN_POINT ( 'NONE',  ( -157.6495955161842062, -176.9391397928654897, 41.15050349809590102 ) ) ;
#11622=CARTESIAN_POINT ( 'NONE',  ( -157.2955611005346270, -194.3438272943106995, 41.63779006702063867 ) ) ;
#11627=CARTESIAN_POINT ( 'NONE',  ( -143.3790856849358306, -190.2891397928654555, 55.53486410454105027 ) ) ;
#11641=CARTESIAN_POINT ( 'NONE',  ( -142.0420953463936087, -162.3938272943107393, 49.65701158161630957 ) ) ;
#11643=CARTESIAN_POINT ( 'NONE',  ( -141.4692556286852891, -177.2130981290892748, 52.90620854394536821 ) ) ;
#11658=DIRECTION ( 'NONE',  ( 0.000000000000000000, 0.000000000000000000, 1.000000000000000000 ) ) ;
#11662=CARTESIAN_POINT ( 'NONE',  ( -142.0420953463936087, -171.6584106276440593, 49.65701158161630957 ) ) ;
#11663=CARTESIAN_POINT ( 'NONE',  ( -159.0959885057557983, -194.1938272943107222, 44.11586579668791330 ) ) ;
#11677=CARTESIAN_POINT ( 'NONE',  ( -148.5561028927606344, -161.7938272943107449, 40.69124936498395328 ) ) ;
#11678=CARTESIAN_POINT ( 'NONE',  ( -157.2955611005345986, -173.6084106276440480, 41.63779006702063867 ) ) ;
#11681=CARTESIAN_POINT ( 'NONE',  ( -154.3824083646099439, -158.7584106276440536, 40.69124936498395328 ) ) ;
#11697=CARTESIAN_POINT ( 'NONE',  ( -143.3790856849358306, -170.7630981290892862, 43.77915905869157598 ) ) ;
#11704=CARTESIAN_POINT ( 'NONE',  ( -145.6429501568359797, -189.2084106276440423, 41.63779006702063867 ) ) ;
#11707=CARTESIAN_POINT ( 'NONE',  ( -145.6429501568359797, -178.1084106276440480, 57.67623309621198047 ) ) ;
#11708=ORIENTED_EDGE ( 'NONE', *, *, #9214, .F. ) ;
#11723=CYLINDRICAL_SURFACE ( 'NONE', #13173, 10.00000000000000888 ) ;
#11724=CARTESIAN_POINT ( 'NONE',  ( -151.4692556286852891, -175.7391397928654442, 60.17163382399899518 ) ) ;
#11732=CARTESIAN_POINT ( 'NONE',  ( -148.5561028927606344, -177.9938272943107336, 58.62277379824867296 ) ) ;
#11736=CARTESIAN_POINT ( 'NONE',  ( -141.4692556286852891, -190.1391397928654783, 52.90620854394536821 ) ) ;
#11740=EDGE_CURVE ( 'NONE', #7746, #2272, #12481, .T. ) ;
#11749=CARTESIAN_POINT ( 'NONE',  ( -145.6429501568359797, -161.9438272943107222, 41.63779006702063867 ) ) ;
#11751=CARTESIAN_POINT ( 'NONE',  ( -157.6495955161842062, -172.1130981290892805, 58.16351966513671812 ) ) ;
#11759=CARTESIAN_POINT ( 'NONE',  ( -153.0531000319306827, -183.1622583705452314, 39.65701158161630957 ) ) ;
#11764=CARTESIAN_POINT ( 'NONE',  ( -143.3790856849358306, -155.7630981290893146, 43.77915905869157598 ) ) ;
#11769=CARTESIAN_POINT ( 'NONE',  ( -141.4692556286852891, -168.0630981290893260, 49.65701158161630957 ) ) ;
#11771=( BOUNDED_CURVE ( )  B_SPLINE_CURVE ( 2, ( #8096, #19773, #1040, #12941, #11276 ),
 .UNSPECIFIED., .F., .T. ) 
 B_SPLINE_CURVE_WITH_KNOTS ( ( 3, 2, 3 ),
 ( 0.9464285714285713969, 0.9499999999999999556, 0.9523897199067097308 ),
 .UNSPECIFIED. ) 
 CURVE ( )  GEOMETRIC_REPRESENTATION_ITEM ( )  RATIONAL_B_SPLINE_CURVE ( ( 0.9755282581475768211, 0.9755282581475768211, 1.000000000000000000, 0.9836254295761526212, 0.9782074374858980015 ) ) 
 REPRESENTATION_ITEM ( '' )  );
#11777=CARTESIAN_POINT ( 'NONE',  ( -159.0959885057557983, -161.4584106276440423, 44.11586579668791330 ) ) ;
#11778=CARTESIAN_POINT ( 'NONE',  ( -142.0420953463935803, -192.2438272943107336, 46.59394152635518083 ) ) ;
#11782=CARTESIAN_POINT ( 'NONE',  ( -149.8854112254399524, -177.7362167067690564, 59.65701158161632378 ) ) ;
#11785=DIRECTION ( 'NONE',  ( 0.5000000000000002220, 0.000000000000000000, -0.8660254037844384856 ) ) ;
#11788=CARTESIAN_POINT ( 'NONE',  ( -154.3824083646099439, -163.2938272943107449, 58.62277379824867296 ) ) ;
#11789=CARTESIAN_POINT ( 'NONE',  ( -142.0420953463935803, -171.8084106276440082, 52.72008163687743831 ) ) ;
#11793=CARTESIAN_POINT ( 'NONE',  ( -145.6429501568359797, -157.1084106276440480, 57.67623309621198047 ) ) ;
#11799=CARTESIAN_POINT ( 'NONE',  ( -153.0531000319306827, -161.2362167067690280, 39.65701158161629536 ) ) ;
#11818=CARTESIAN_POINT ( 'NONE',  ( -142.0420953463935803, -186.5084106276440536, 46.59394152635518793 ) ) ;
#11820=CARTESIAN_POINT ( 'NONE',  ( -143.8425227516148084, -174.3584106276440480, 44.11586579668791330 ) ) ;
#11823=LINE ( 'NONE', #14797, #2173 ) ;
#11826=ORIENTED_EDGE ( 'NONE', *, *, #4067, .T. ) ;
#11827=AXIS2_PLACEMENT_3D ( 'NONE', #19754, #18318, #11472 ) ;
#11837=DIRECTION ( 'NONE',  ( 0.000000000000000000, 0.000000000000000000, 1.000000000000000000 ) ) ;
#11838=CARTESIAN_POINT ( 'NONE',  ( -151.4692556286852891, -181.7391397928654726, 60.17163382399899518 ) ) ;
#11839=CARTESIAN_POINT ( 'NONE',  ( -161.4692556286852891, -181.7130981290893033, 46.40781461928724383 ) ) ;
#11840=CARTESIAN_POINT ( 'NONE',  ( -161.4692556286853176, -194.4891397928654726, 49.65701158161630957 ) ) ;
#11846=CARTESIAN_POINT ( 'NONE',  ( -143.8425227516148084, -174.6938272943107506, 55.19815736654470584 ) ) ;
#11849=CARTESIAN_POINT ( 'NONE',  ( -143.3790856849358306, -195.6891397928654897, 43.77915905869157598 ) ) ;
#11861=DIRECTION ( 'NONE',  ( -0.000000000000000000, 1.000000000000000000, -0.000000000000000000 ) ) ;
#11862=CYLINDRICAL_SURFACE ( 'NONE', #18009, 10.00000000000000888 ) ;
#11865=CARTESIAN_POINT ( 'NONE',  ( -161.4692556286852607, -169.7130981290892748, 46.40781461928724383 ) ) ;
#11870=CARTESIAN_POINT ( 'NONE',  ( -145.2889157411863437, -183.5391397928654840, 41.15050349809589392 ) ) ;
#11876=CARTESIAN_POINT ( 'NONE',  ( -141.4692556286852891, -156.0630981290892976, 49.65701158161630957 ) ) ;
#11881=CARTESIAN_POINT ( 'NONE',  ( -148.3790856849358306, -168.6630981290892919, 59.16757674456786020 ) ) ;
#11883=CARTESIAN_POINT ( 'NONE',  ( -158.9748091281504401, -116.9891397928655010, 62.65701158161630957 ) ) ;
#11888=CARTESIAN_POINT ( 'NONE',  ( -157.2955611005346270, -161.6084106276440480, 41.63779006702063867 ) ) ;
#11889=CARTESIAN_POINT ( 'NONE',  ( -148.5561028927606344, -189.9938272943107336, 58.62277379824867296 ) ) ;
#11893=CARTESIAN_POINT ( 'NONE',  ( -151.4692556286853176, -174.2391397928654726, 39.65701158161629536 ) ) ;
#11895=CARTESIAN_POINT ( 'NONE',  ( -161.4692556286852891, -184.7130981290893033, 46.40781461928724383 ) ) ;
#11899=CARTESIAN_POINT ( 'NONE',  ( -145.6429501568359797, -164.9438272943106938, 41.63779006702063867 ) ) ;
#11900=CARTESIAN_POINT ( 'NONE',  ( -159.0959885057557983, -172.8584106276440764, 55.19815736654470584 ) ) ;
#11902=CARTESIAN_POINT ( 'NONE',  ( -148.5561028927606344, -162.0584106276440366, 40.69124936498395328 ) ) ;
#11907=ORIENTED_EDGE ( 'NONE', *, *, #13263, .F. ) ;
#11926=CARTESIAN_POINT ( 'NONE',  ( -160.8964159109769696, -191.1584106276440593, 49.65701158161630957 ) ) ;
#11928=CARTESIAN_POINT ( 'NONE',  ( -159.0959885057557983, -173.4584106276440423, 44.11586579668791330 ) ) ;
#11941=CARTESIAN_POINT ( 'NONE',  ( -151.4692556286852607, -156.2391397928654726, 39.65701158161629536 ) ) ;
#11946=CARTESIAN_POINT ( 'NONE',  ( -145.2889157411863721, -184.4391397928654328, 58.16351966513671812 ) ) ;
#11953=CARTESIAN_POINT ( 'NONE',  ( -142.0420953463936087, -171.3938272943107393, 49.65701158161630957 ) ) ;
#11955=CARTESIAN_POINT ( 'NONE',  ( -161.4692556286852891, -170.3391397928654669, 52.90620854394536821 ) ) ;
#11958=CARTESIAN_POINT ( 'NONE',  ( -149.8854112254399524, -190.6622583705452030, 59.65701158161632378 ) ) ;
#11961=EDGE_CURVE ( 'NONE', #12248, #1664, #9980, .T. ) ;
#11962=EDGE_CURVE ( 'NONE', #4977, #9846, #12228, .T. ) ;
#11969=FACE_OUTER_BOUND ( 'NONE', #3542, .T. ) ;
#11972=CARTESIAN_POINT ( 'NONE',  ( -151.4692556286853176, -174.8130981290893260, 59.65701158161632378 ) ) ;
#11974=CARTESIAN_POINT ( 'NONE',  ( -141.4692556286852891, -168.2130981290892748, 52.90620854394536821 ) ) ;
#11992=CARTESIAN_POINT ( 'NONE',  ( -143.3790856849358306, -195.6891397928654897, 43.77915905869157598 ) ) ;
#11993=CARTESIAN_POINT ( 'NONE',  ( -148.5561028927606344, -176.7938272943107165, 40.69124936498395328 ) ) ;
#11997=CARTESIAN_POINT ( 'NONE',  ( -159.5594255724347761, -173.1891397928654897, 55.53486410454104316 ) ) ;
#12003=CARTESIAN_POINT ( 'NONE',  ( -145.6429501568359797, -171.2084106276440423, 41.63779006702063867 ) ) ;
#12009=CARTESIAN_POINT ( 'NONE',  ( -149.8854112254399524, -193.6622583705451461, 59.65701158161632378 ) ) ;
#12013=PRODUCT_DEFINITION_SHAPE ( 'NONE', 'NONE',  #12422 ) ;
#12024=CARTESIAN_POINT ( 'NONE',  ( -142.0420953463935803, -183.2438272943107336, 46.59394152635518793 ) ) ;
#12029=CARTESIAN_POINT ( 'NONE',  ( -143.8425227516148084, -189.9584106276440423, 55.19815736654470584 ) ) ;
#12031=CARTESIAN_POINT ( 'NONE',  ( -148.5561028927606344, -174.0584106276440366, 40.69124936498395328 ) ) ;
#12049=CARTESIAN_POINT ( 'NONE',  ( -145.2889157411863437, -180.5130981290893146, 58.16351966513671812 ) ) ;
#12050=CARTESIAN_POINT ( 'NONE',  ( -157.6495955161842062, -173.9391397928654328, 41.15050349809590102 ) ) ;
#12051=CARTESIAN_POINT ( 'NONE',  ( -151.4692556286852891, -182.3130981290892976, 39.65701158161629536 ) ) ;
#12056=CARTESIAN_POINT ( 'NONE',  ( -145.6429501568359797, -177.8438272943106995, 57.67623309621198047 ) ) ;
#12059=CARTESIAN_POINT ( 'NONE',  ( -154.5594255724347761, -157.8891397928654783, 59.16757674456785310 ) ) ;
#12061=CARTESIAN_POINT ( 'NONE',  ( -154.5594255724347761, -176.1630981290893203, 40.14644641866476604 ) ) ;
#12066=ORIENTED_EDGE ( 'NONE', *, *, #3557, .T. ) ;
#12068=ORIENTED_EDGE ( 'NONE', *, *, #827, .T. ) ;
#12072=FACE_OUTER_BOUND ( 'NONE', #675, .T. ) ;
#12077=CARTESIAN_POINT ( 'NONE',  ( -159.5594255724347761, -172.8630981290893089, 43.77915905869157598 ) ) ;
#12079=CARTESIAN_POINT ( 'NONE',  ( -161.4692556286853176, -191.4891397928654726, 49.65701158161630957 ) ) ;
#12096=CARTESIAN_POINT ( 'NONE',  ( -160.8964159109769696, -158.1584106276440593, 49.65701158161630957 ) ) ;
#12098=CARTESIAN_POINT ( 'NONE',  ( -159.0959885057557983, -184.5938272943107279, 55.19815736654470584 ) ) ;
#12099=CARTESIAN_POINT ( 'NONE',  ( -151.4692556286852891, -177.2391397928654442, 39.65701158161629536 ) ) ;
#12109=CARTESIAN_POINT ( 'NONE',  ( -151.4692556286852891, -161.9084106276440593, 39.74470866294723947 ) ) ;
#12116=CARTESIAN_POINT ( 'NONE',  ( -159.5594255724347761, -179.1891397928654612, 55.53486410454104316 ) ) ;
#12126=CARTESIAN_POINT ( 'NONE',  ( -154.5594255724347761, -171.9630981290893033, 59.16757674456785310 ) ) ;
#12130=CARTESIAN_POINT ( 'NONE',  ( -154.3824083646099439, -178.2938272943107165, 58.62277379824867296 ) ) ;
#12133=CARTESIAN_POINT ( 'NONE',  ( -143.8425227516148084, -186.3584106276440480, 44.11586579668791330 ) ) ;
#12152=CARTESIAN_POINT ( 'NONE',  ( -143.3790856849358306, -166.2891397928654840, 55.53486410454105027 ) ) ;
#12153=( BOUNDED_CURVE ( )  B_SPLINE_CURVE ( 2, ( #16817, #1730, #8464, #15283, #15171, #74, #13518, #20251, #18593, #178, #5253, #7238, #10543 ),
 .UNSPECIFIED., .F., .F. ) 
 B_SPLINE_CURVE_WITH_KNOTS ( ( 3, 2, 2, 2, 2, 2, 3 ),
 ( 0.5892857142857143016, 0.5928571428571428603, 0.5999999999999999778, 0.6071428571428570953, 0.6142857142857143238, 0.6214285714285714413, 0.6250000000000000000 ),
 .UNSPECIFIED. ) 
 CURVE ( )  GEOMETRIC_REPRESENTATION_ITEM ( )  RATIONAL_B_SPLINE_CURVE ( ( 0.9755282581475768211, 0.9755282581475768211, 1.000000000000000000, 0.9510565162951535312, 1.000000000000000000, 0.9510565162951535312, 1.000000000000000000, 0.9510565162951535312, 1.000000000000000000, 0.9510565162951535312, 1.000000000000000000, 0.9755282581475768211, 0.9755282581475768211 ) ) 
 REPRESENTATION_ITEM ( '' )  );
#12160=CARTESIAN_POINT ( 'NONE',  ( -160.8964159109769696, -175.7438272943107052, 52.72008163687743121 ) ) ;
#12176=DIRECTION ( 'NONE',  ( 8.659560562354814529E-17, 0.7071067811865573427, -0.7071067811865378028 ) ) ;
#12178=AXIS2_PLACEMENT_3D ( 'NONE', #21434, #14695, #6550 ) ;
#12183=CARTESIAN_POINT ( 'NONE',  ( -151.4692556286852891, -168.8130981290893260, 60.17163382399899518 ) ) ;
#12184=CARTESIAN_POINT ( 'NONE',  ( -161.4692556286852891, -191.3391397928654669, 52.90620854394536821 ) ) ;
#12203=CARTESIAN_POINT ( 'NONE',  ( -151.4692556286852607, -171.2391397928654726, 39.65701158161629536 ) ) ;
#12207=CARTESIAN_POINT ( 'NONE',  ( -154.5594255724347761, -195.0891397928654669, 40.14644641866476604 ) ) ;
#12208=CARTESIAN_POINT ( 'NONE',  ( -154.3824083646099439, -184.2938272943107449, 58.62277379824867296 ) ) ;
#12219=CARTESIAN_POINT ( 'NONE',  ( -142.0420953463935803, -165.8084106276440366, 52.72008163687743831 ) ) ;
#12228=CIRCLE ( 'NONE', #3094, 10.00000000000000888 ) ;
#12229=EDGE_CURVE ( 'NONE', #8, #21213, #17809, .T. ) ;
#12237=VECTOR ( 'NONE', #10123, 1000.000000000000000 ) ;
#12246=CARTESIAN_POINT ( 'NONE',  ( -160.8964159109769696, -178.7438272943107052, 52.72008163687743121 ) ) ;
#12248=VERTEX_POINT ( 'NONE', #17218 ) ;
#12265=CARTESIAN_POINT ( 'NONE',  ( -157.6495955161842062, -167.9391397928654897, 41.15050349809590102 ) ) ;
#12270=CARTESIAN_POINT ( 'NONE',  ( -160.8964159109769696, -160.8938272943107393, 49.65701158161630957 ) ) ;
#12281=VERTEX_POINT ( 'NONE', #2136 ) ;
#12288=CARTESIAN_POINT ( 'NONE',  ( -142.0420953463936087, -156.3938272943107393, 49.65701158161630957 ) ) ;
#12290=CARTESIAN_POINT ( 'NONE',  ( -143.3790856849358306, -162.3630981290893089, 55.53486410454105027 ) ) ;
#12291=CARTESIAN_POINT ( 'NONE',  ( -151.4692556286852891, -190.7391397928654726, 59.65701158161632378 ) ) ;
#12299=B_SPLINE_CURVE_WITH_KNOTS ( 'NONE', 1,
 ( #13278, #4445 ),
 .UNSPECIFIED., .F., .F.,
 ( 2, 2 ),
 ( 0.000000000000000000, 1.000000000000000000 ),
 .UNSPECIFIED. ) ;
#12302=CARTESIAN_POINT ( 'NONE',  ( -141.4692556286852891, -169.1391397928654214, 52.90620854394536821 ) ) ;
#12304=ADVANCED_FACE ( 'NONE', ( #480 ), #6890, .T. ) ;
#12309=DIRECTION ( 'NONE',  ( -0.000000000000000000, -1.000000000000000000, -0.000000000000000000 ) ) ;
#12314=CARTESIAN_POINT ( 'NONE',  ( -154.3824083646099439, -182.4938272943107336, 40.69124936498395328 ) ) ;
#12316=CARTESIAN_POINT ( 'NONE',  ( -157.6495955161842062, -187.1130981290893089, 58.16351966513671812 ) ) ;
#12320=FACE_OUTER_BOUND ( 'NONE', #13799, .T. ) ;
#12326=CARTESIAN_POINT ( 'NONE',  ( -143.8425227516148084, -165.3584106276440480, 44.11586579668791330 ) ) ;
#12327=CARTESIAN_POINT ( 'NONE',  ( -151.4692556286853176, -163.7391397928654726, 59.65701158161632378 ) ) ;
#12335=CARTESIAN_POINT ( 'NONE',  ( -151.4692556286852891, -178.7391397928654726, 59.65701158161631668 ) ) ;
#12348=( BOUNDED_CURVE ( )  B_SPLINE_CURVE ( 1, ( #4435, #2791 ),
 .UNSPECIFIED., .F., .F. ) 
 B_SPLINE_CURVE_WITH_KNOTS ( ( 2, 2 ),
 ( 0.000000000000000000, 1.000000000000000000 ),
 .UNSPECIFIED. ) 
 CURVE ( )  GEOMETRIC_REPRESENTATION_ITEM ( )  RATIONAL_B_SPLINE_CURVE ( ( 0.9782074146920120006, 0.9782074146920120006 ) ) 
 REPRESENTATION_ITEM ( '' )  );
#12351=CARTESIAN_POINT ( 'NONE',  ( -151.4692556286852891, -184.1438272943107108, 59.56931450028537967 ) ) ;
#12353=VERTEX_POINT ( 'NONE', #20869 ) ;
#12354=CARTESIAN_POINT ( 'NONE',  ( -154.3824083646099439, -178.5584106276440366, 58.62277379824867296 ) ) ;
#12360=ORIENTED_EDGE ( 'NONE', *, *, #1349, .T. ) ;
#12361=VERTEX_POINT ( 'NONE', #12702 ) ;
#12369=CARTESIAN_POINT ( 'NONE',  ( -151.4692556286852891, -180.8130981290893260, 59.65701158161631668 ) ) ;
#12370=CARTESIAN_POINT ( 'NONE',  ( -148.3790856849358306, -168.3891397928654499, 40.14644641866477315 ) ) ;
#12373=ADVANCED_FACE ( 'NONE', ( #12486 ), #19423, .T. ) ;
#12377=CARTESIAN_POINT ( 'NONE',  ( -157.6495955161842062, -164.0130981290892578, 41.15050349809589392 ) ) ;
#12381=CARTESIAN_POINT ( 'NONE',  ( -143.8425227516148084, -165.6938272943107222, 55.19815736654470584 ) ) ;
#12384=CARTESIAN_POINT ( 'NONE',  ( -160.8964159109769696, -194.0084106276440252, 52.72008163687743121 ) ) ;
#12403=CARTESIAN_POINT ( 'NONE',  ( -141.4692556286852891, -156.2130981290893317, 52.90620854394536821 ) ) ;
#12405=CARTESIAN_POINT ( 'NONE',  ( -151.4692556286852891, -196.9891397928655010, 39.65701158161630246 ) ) ;
#12409=CARTESIAN_POINT ( 'NONE',  ( -143.8425227516148084, -195.0938272943107279, 44.11586579668791330 ) ) ;
#12414=EDGE_CURVE ( 'NONE', #1800, #12361, #21510, .T. ) ;
#12422=PRODUCT_DEFINITION ( 'UNKNOWN', '', #3173, #8411 ) ;
#12423=CARTESIAN_POINT ( 'NONE',  ( -149.8854112254399240, -172.6622583705452314, 59.65701158161632378 ) ) ;
#12428=CARTESIAN_POINT ( 'NONE',  ( -145.6429501568359797, -170.9438272943107222, 41.63779006702063867 ) ) ;
#12430=CARTESIAN_POINT ( 'NONE',  ( -141.4692556286852891, -186.0630981290892976, 49.65701158161630957 ) ) ;
#12433=CARTESIAN_POINT ( 'NONE',  ( -151.4692556286852607, -162.2391397928654442, 39.65701158161629536 ) ) ;
#12439=CARTESIAN_POINT ( 'NONE',  ( -151.4692556286852891, -166.4084106276440593, 59.56931450028537256 ) ) ;
#12445=ORIENTED_EDGE ( 'NONE', *, *, #15641, .F. ) ;
#12446=CARTESIAN_POINT ( 'NONE',  ( -154.5594255724347761, -161.1630981290892919, 40.14644641866476604 ) ) ;
#12456=CARTESIAN_POINT ( 'NONE',  ( -154.5594255724347761, -156.9630981290893317, 59.16757674456785310 ) ) ;
#12461=CARTESIAN_POINT ( 'NONE',  ( -148.5561028927606344, -179.7938272943107449, 40.69124936498395328 ) ) ;
#12462=CARTESIAN_POINT ( 'NONE',  ( -151.4692556286852891, -190.4084106276440309, 59.56931450028537256 ) ) ;
#12464=CARTESIAN_POINT ( 'NONE',  ( -157.2955611005346270, -181.7084106276440423, 57.67623309621198047 ) ) ;
#12473=ORIENTED_EDGE ( 'NONE', *, *, #12699, .F. ) ;
#12481=( BOUNDED_CURVE ( )  B_SPLINE_CURVE ( 2, ( #11972, #17357, #2262, #8999, #75, #6813, #18701, #17141, #13519, #20252, #3607, #294, #10330 ),
 .UNSPECIFIED., .F., .F. ) 
 B_SPLINE_CURVE_WITH_KNOTS ( ( 3, 2, 2, 2, 2, 2, 3 ),
 ( 0.4821428571428571508, 0.4857142857142857095, 0.4928571428571428825, 0.5000000000000000000, 0.5071428571428571175, 0.5142857142857142350, 0.5178571428571429047 ),
 .UNSPECIFIED. ) 
 CURVE ( )  GEOMETRIC_REPRESENTATION_ITEM ( )  RATIONAL_B_SPLINE_CURVE ( ( 0.9755282581475768211, 0.9755282581475768211, 1.000000000000000000, 0.9510565162951535312, 1.000000000000000000, 0.9510565162951535312, 1.000000000000000000, 0.9510565162951535312, 1.000000000000000000, 0.9510565162951535312, 1.000000000000000000, 0.9755282581475763770, 0.9755282581475768211 ) ) 
 REPRESENTATION_ITEM ( '' )  );
#12485=CARTESIAN_POINT ( 'NONE',  ( -154.5594255724347761, -172.8891397928654783, 59.16757674456785310 ) ) ;
#12486=FACE_OUTER_BOUND ( 'NONE', #978, .T. ) ;
#12488=CARTESIAN_POINT ( 'NONE',  ( -153.0531000319307111, -164.2362167067690564, 39.65701158161631668 ) ) ;
#12491=CARTESIAN_POINT ( 'NONE',  ( -159.0959885057557983, -166.5938272943107563, 55.19815736654470584 ) ) ;
#12495=CARTESIAN_POINT ( 'NONE',  ( -148.5561028927606344, -192.0584106276440650, 40.69124936498395328 ) ) ;
#12501=EDGE_LOOP ( 'NONE', ( #7844, #9339, #6990, #17562 ) ) ;
#12514=CARTESIAN_POINT ( 'NONE',  ( -154.5594255724347761, -155.1630981290892919, 40.14644641866476604 ) ) ;
#12516=VECTOR ( 'NONE', #13391, 1000.000000000000000 ) ;
#12531=ORIENTED_EDGE ( 'NONE', *, *, #19202, .T. ) ;
#12536=CARTESIAN_POINT ( 'NONE',  ( -151.4692556286852891, -172.1438272943107393, 59.56931450028537256 ) ) ;
#12538=CARTESIAN_POINT ( 'NONE',  ( -159.5594255724347761, -184.8630981290893089, 43.77915905869157598 ) ) ;
#12546=CARTESIAN_POINT ( 'NONE',  ( -142.0420953463935803, -162.5084106276440536, 46.59394152635518083 ) ) ;
#12548=VECTOR ( 'NONE', #18670, 1000.000000000000000 ) ;
#12568=LINE ( 'NONE', #7731, #13258 ) ;
#12572=CARTESIAN_POINT ( 'NONE',  ( -157.2955611005346270, -169.4438272943107222, 57.67623309621198047 ) ) ;
#12573=CARTESIAN_POINT ( 'NONE',  ( -151.4692556286852891, -196.9891397928655010, 49.65701158161630957 ) ) ;
#12575=CARTESIAN_POINT ( 'NONE',  ( -151.4692556286852891, -179.9084106276440593, 39.74470866294723947 ) ) ;
#12586=ORIENTED_EDGE ( 'NONE', *, *, #8508, .T. ) ;
#12597=CARTESIAN_POINT ( 'NONE',  ( -141.4692556286852891, -157.1391397928654783, 52.90620854394536821 ) ) ;
#12602=CARTESIAN_POINT ( 'NONE',  ( -145.6429501568359797, -168.8438272943107563, 57.67623309621198047 ) ) ;
#12604=CARTESIAN_POINT ( 'NONE',  ( -160.8964159109769696, -191.3084106276440650, 46.59394152635518793 ) ) ;
#12606=EDGE_CURVE ( 'NONE', #6960, #13046, #19840, .T. ) ;
#12615=DIRECTION ( 'NONE',  ( 0.5000000000000002220, 0.000000000000000000, -0.8660254037844384856 ) ) ;
#12619=CARTESIAN_POINT ( 'NONE',  ( -157.6495955161842062, -188.0391397928654555, 58.16351966513671812 ) ) ;
#12622=CARTESIAN_POINT ( 'NONE',  ( -154.5594255724347761, -162.9630981290893317, 59.16757674456785310 ) ) ;
#12646=CARTESIAN_POINT ( 'NONE',  ( -154.3824083646099439, -170.4938272943107336, 40.69124936498395328 ) ) ;
#12648=CARTESIAN_POINT ( 'NONE',  ( -148.3790856849358306, -188.4630981290893317, 40.14644641866477315 ) ) ;
#12654=EDGE_CURVE ( 'NONE', #14419, #6804, #19367, .T. ) ;
#12656=CARTESIAN_POINT ( 'NONE',  ( -160.8964159109769696, -158.1584106276440593, 49.65701158161630957 ) ) ;
#12657=AXIS2_PLACEMENT_3D ( 'NONE', #2403, #7050, #17169 ) ;
#12658=CARTESIAN_POINT ( 'NONE',  ( -154.5594255724347761, -165.0891397928654669, 40.14644641866476604 ) ) ;
#12659=CARTESIAN_POINT ( 'NONE',  ( -153.0531000319306827, -156.1622583705452030, 39.65701158161629536 ) ) ;
#12679=CARTESIAN_POINT ( 'NONE',  ( -154.3824083646099439, -167.4938272943107336, 40.69124936498395328 ) ) ;
#12680=CARTESIAN_POINT ( 'NONE',  ( -143.8425227516148084, -195.3584106276440480, 44.11586579668791330 ) ) ;
#12699=EDGE_CURVE ( 'NONE', #13046, #16234, #10020, .T. ) ;
#12701=CARTESIAN_POINT ( 'NONE',  ( -151.4692556286852891, -165.2391397928654442, 39.14238933923362396 ) ) ;
#12702=CARTESIAN_POINT ( 'NONE',  ( -151.4692556286852607, -158.3130981290892692, 39.65701158161629536 ) ) ;
#12704=CARTESIAN_POINT ( 'NONE',  ( -151.4692556286853176, -162.8130981290893260, 59.65701158161632378 ) ) ;
#12707=CARTESIAN_POINT ( 'NONE',  ( -154.3824083646099439, -164.4938272943107336, 40.69124936498395328 ) ) ;
#12708=EDGE_CURVE ( 'NONE', #19941, #10182, #5190, .T. ) ;
#12710=CARTESIAN_POINT ( 'NONE',  ( -159.0959885057557983, -193.8584106276440480, 55.19815736654470584 ) ) ;
#12713=CARTESIAN_POINT ( 'NONE',  ( -151.4692556286852891, -196.9891397928655010, 49.65701158161630957 ) ) ;
#12726=CARTESIAN_POINT ( 'NONE',  ( -145.2889157411863721, -192.5391397928654840, 41.15050349809590102 ) ) ;
#12729=CARTESIAN_POINT ( 'NONE',  ( -161.4692556286853176, -163.5630981290893260, 49.65701158161630957 ) ) ;
#12735=CARTESIAN_POINT ( 'NONE',  ( -154.3824083646099439, -193.2938272943107449, 58.62277379824867296 ) ) ;
#12737=CARTESIAN_POINT ( 'NONE',  ( -151.4692556286852607, -161.3130981290892976, 39.65701158161629536 ) ) ;
#12738=ORIENTED_EDGE ( 'NONE', *, *, #7925, .T. ) ;
#12741=( BOUNDED_CURVE ( )  B_SPLINE_CURVE ( 2, ( #17840, #17626, #17948, #9269, #667, #15970, #11125, #20840, #7404, #7728, #12456, #12780, #881 ),
 .UNSPECIFIED., .F., .F. ) 
 B_SPLINE_CURVE_WITH_KNOTS ( ( 3, 2, 2, 2, 2, 2, 3 ),
 ( 0.8750000000000000000, 0.8785714285714285587, 0.8857142857142856762, 0.8928571428571429047, 0.9000000000000000222, 0.9071428571428571397, 0.9107142857142856984 ),
 .UNSPECIFIED. ) 
 CURVE ( )  GEOMETRIC_REPRESENTATION_ITEM ( )  RATIONAL_B_SPLINE_CURVE ( ( 0.9755282581475768211, 0.9755282581475768211, 1.000000000000000000, 0.9510565162951535312, 1.000000000000000000, 0.9510565162951535312, 1.000000000000000000, 0.9510565162951535312, 1.000000000000000000, 0.9510565162951535312, 1.000000000000000000, 0.9755282581475768211, 0.9755282581475768211 ) ) 
 REPRESENTATION_ITEM ( '' )  );
#12747=ORIENTED_EDGE ( 'NONE', *, *, #2011, .F. ) ;
#12754=CARTESIAN_POINT ( 'NONE',  ( -157.2955611005345986, -169.4438272943106938, 57.67623309621197336 ) ) ;
#12756=CARTESIAN_POINT ( 'NONE',  ( -145.2889157411863721, -186.5130981290893430, 58.16351966513671812 ) ) ;
#12763=CARTESIAN_POINT ( 'NONE',  ( -142.0420953463935803, -156.8084106276440366, 52.72008163687743831 ) ) ;
#12767=FACE_OUTER_BOUND ( 'NONE', #12798, .T. ) ;
#12774=EDGE_CURVE ( 'NONE', #13802, #846, #5056, .T. ) ;
#12780=CARTESIAN_POINT ( 'NONE',  ( -153.0531000319306827, -156.8899795514095672, 59.65701158161631668 ) ) ;
#12786=EDGE_CURVE ( 'NONE', #10404, #1447, #4300, .T. ) ;
#12788=CARTESIAN_POINT ( 'NONE',  ( -151.4692556286852607, -155.3130981290892976, 39.65701158161629536 ) ) ;
#12789=CARTESIAN_POINT ( 'NONE',  ( -154.3824083646099439, -175.2938272943107165, 58.62277379824867296 ) ) ;
#12790=CARTESIAN_POINT ( 'NONE',  ( -148.5561028927606344, -181.2584106276440536, 58.62277379824867296 ) ) ;
#12792=CARTESIAN_POINT ( 'NONE',  ( -157.2955611005346270, -167.6084106276440480, 41.63779006702063867 ) ) ;
#12798=EDGE_LOOP ( 'NONE', ( #16014, #7854, #14446, #16779 ) ) ;
#12800=APPLICATION_CONTEXT ( 'automotive_design' ) ;
#12801=CARTESIAN_POINT ( 'NONE',  ( -151.4692556286852607, -192.2391397928655010, 39.65701158161629536 ) ) ;
#12809=CARTESIAN_POINT ( 'NONE',  ( -145.2889157411863721, -159.5391397928654840, 41.15050349809590102 ) ) ;
#12815=CARTESIAN_POINT ( 'NONE',  ( -148.5561028927606344, -156.9938272943107052, 58.62277379824867296 ) ) ;
#12817=CARTESIAN_POINT ( 'NONE',  ( -157.2955611005346270, -184.7084106276440423, 57.67623309621198047 ) ) ;
#12825=ORIENTED_EDGE ( 'NONE', *, *, #12414, .F. ) ;
#12827=CARTESIAN_POINT ( 'NONE',  ( -136.4581486297550441, -126.9891397928655010, 49.65701158161631668 ) ) ;
#12834=CARTESIAN_POINT ( 'NONE',  ( -145.2889157411863721, -189.5391397928654271, 41.15050349809590102 ) ) ;
#12837=CARTESIAN_POINT ( 'NONE',  ( -142.0420953463935803, -186.5438272943107449, 52.72008163687743831 ) ) ;
#12842=CARTESIAN_POINT ( 'NONE',  ( -145.6429501568359797, -182.9438272943106938, 41.63779006702063867 ) ) ;
#12844=CARTESIAN_POINT ( 'NONE',  ( -148.3790856849358306, -161.4630981290893317, 40.14644641866477315 ) ) ;
#12850=VERTEX_POINT ( 'NONE', #21596 ) ;
#12853=CARTESIAN_POINT ( 'NONE',  ( -159.5594255724347761, -193.8630981290893089, 43.77915905869157598 ) ) ;
#12860=CARTESIAN_POINT ( 'NONE',  ( -160.8964159109769696, -173.0438272943107165, 46.59394152635518083 ) ) ;
#12862=CARTESIAN_POINT ( 'NONE',  ( -141.4692556286852891, -179.9130981290893487, 46.40781461928724383 ) ) ;
#12872=CARTESIAN_POINT ( 'NONE',  ( -154.3824083646099439, -155.7584106276440536, 40.69124936498395328 ) ) ;
#12876=AXIS2_PLACEMENT_3D ( 'NONE', #15232, #1678, #8519 ) ;
#12892=AXIS2_PLACEMENT_3D ( 'NONE', #18100, #14361, #7664 ) ;
#12899=CARTESIAN_POINT ( 'NONE',  ( -160.8964159109769696, -176.0438272943107165, 46.59394152635518793 ) ) ;
#12900=CARTESIAN_POINT ( 'NONE',  ( -148.5561028927606344, -189.0584106276440650, 40.69124936498395328 ) ) ;
#12903=CARTESIAN_POINT ( 'NONE',  ( -151.4692556286852891, -166.4084106276440878, 59.56931450028537967 ) ) ;
#12920=CARTESIAN_POINT ( 'NONE',  ( -143.3790856849358306, -159.6891397928654897, 43.77915905869157598 ) ) ;
#12927=CARTESIAN_POINT ( 'NONE',  ( -154.3824083646099439, -155.4938272943107052, 40.69124936498395328 ) ) ;
#12928=ADVANCED_FACE ( 'NONE', ( #16131 ), #5375, .T. ) ;
#12930=CARTESIAN_POINT ( 'NONE',  ( -160.8964159109769696, -185.0084106276440821, 52.72008163687743121 ) ) ;
#12934=( BOUNDED_CURVE ( )  B_SPLINE_CURVE ( 1, ( #13717, #18794 ),
 .UNSPECIFIED., .F., .F. ) 
 B_SPLINE_CURVE_WITH_KNOTS ( ( 2, 2 ),
 ( 0.000000000000000000, 1.000000000000000000 ),
 .UNSPECIFIED. ) 
 CURVE ( )  GEOMETRIC_REPRESENTATION_ITEM ( )  RATIONAL_B_SPLINE_CURVE ( ( 0.9782074374858980015, 0.9782074374858980015 ) ) 
 REPRESENTATION_ITEM ( '' )  );
#12941=CARTESIAN_POINT ( 'NONE',  ( -155.5590433672037705, -155.1145756620584564, 40.47124192889010885 ) ) ;
#12946=CARTESIAN_POINT ( 'NONE',  ( -151.4692556286853176, -175.7391397928654726, 59.65701158161632378 ) ) ;
#12947=CARTESIAN_POINT ( 'NONE',  ( -154.5594255724347761, -190.8891397928654783, 59.16757674456785310 ) ) ;
#12951=CARTESIAN_POINT ( 'NONE',  ( -143.8425227516148084, -186.0938272943107279, 44.11586579668791330 ) ) ;
#12955=CARTESIAN_POINT ( 'NONE',  ( -145.6429501568359797, -183.8438272943107563, 57.67623309621198047 ) ) ;
#12972=CARTESIAN_POINT ( 'NONE',  ( -142.0420953463935803, -162.2438272943107336, 46.59394152635518083 ) ) ;
#12973=CARTESIAN_POINT ( 'NONE',  ( -143.3790856849358306, -166.2891397928654840, 55.53486410454105027 ) ) ;
#12974=CARTESIAN_POINT ( 'NONE',  ( -157.6495955161842062, -179.0130981290892578, 41.15050349809590102 ) ) ;
#12977=EDGE_CURVE ( 'NONE', #8279, #18561, #10345, .T. ) ;
#12982=CARTESIAN_POINT ( 'NONE',  ( -154.5594255724347761, -166.8891397928654499, 59.16757674456785310 ) ) ;
#12993=CARTESIAN_POINT ( 'NONE',  ( -148.3790856849358306, -156.3891397928654783, 40.14644641866477315 ) ) ;
#13000=CARTESIAN_POINT ( 'NONE',  ( -157.2955611005346270, -170.6084106276440480, 41.63779006702063867 ) ) ;
#13002=CARTESIAN_POINT ( 'NONE',  ( -151.4692556286853176, -179.3130981290892976, 39.65701158161629536 ) ) ;
#13006=CARTESIAN_POINT ( 'NONE',  ( -151.4692556286852891, -188.3130981290893260, 39.65701158161629536 ) ) ;
#13011=CARTESIAN_POINT ( 'NONE',  ( -151.4692556286852891, -169.1438272943107108, 59.56931450028537967 ) ) ;
#13012=CARTESIAN_POINT ( 'NONE',  ( -154.3824083646099439, -187.5584106276440650, 58.62277379824867296 ) ) ;
#13013=ADVANCED_FACE ( 'NONE', ( #14582 ), #4670, .T. ) ;
#13016=CARTESIAN_POINT ( 'NONE',  ( -145.6429501568359797, -172.1084106276439911, 57.67623309621198047 ) ) ;
#13030=PLANE ( 'NONE',  #11827 ) ;
#13032=CARTESIAN_POINT ( 'NONE',  ( -161.4692556286852607, -158.6391397928654783, 46.40781461928724383 ) ) ;
#13036=CARTESIAN_POINT ( 'NONE',  ( -151.4692556286852891, -196.9891397928655010, 59.65701158161632378 ) ) ;
#13039=CARTESIAN_POINT ( 'NONE',  ( -151.4692556286852891, -194.9084106276440025, 39.74470866294723947 ) ) ;
#13041=CARTESIAN_POINT ( 'NONE',  ( -160.8964159109769696, -182.1584106276440309, 49.65701158161630957 ) ) ;
#13044=CARTESIAN_POINT ( 'NONE',  ( -145.2889157411863437, -159.5391397928654555, 41.15050349809589392 ) ) ;
#13046=VERTEX_POINT ( 'NONE', #12827 ) ;
#13047=DIRECTION ( 'NONE',  ( -0.000000000000000000, 1.000000000000000000, -0.000000000000000000 ) ) ;
#13052=EDGE_CURVE ( 'NONE', #5698, #8850, #11771, .T. ) ;
#13056=CARTESIAN_POINT ( 'NONE',  ( -161.4692556286853176, -188.4891397928654726, 49.65701158161630957 ) ) ;
#13059=CARTESIAN_POINT ( 'NONE',  ( -160.8964159109769696, -191.0438272943107449, 46.59394152635518793 ) ) ;
#13064=CARTESIAN_POINT ( 'NONE',  ( -142.0420953463936087, -180.3938272943107108, 49.65701158161630957 ) ) ;
#13067=ORIENTED_EDGE ( 'NONE', *, *, #8693, .T. ) ;
#13080=CARTESIAN_POINT ( 'NONE',  ( -145.6429501568359797, -159.8438272943107279, 57.67623309621197336 ) ) ;
#13082=CARTESIAN_POINT ( 'NONE',  ( -151.4692556286852891, -176.3130981290892692, 39.14238933923362396 ) ) ;
#13083=FACE_OUTER_BOUND ( 'NONE', #9043, .T. ) ;
#13089=LINE ( 'NONE', #3058, #19933 ) ;
#13100=CARTESIAN_POINT ( 'NONE',  ( -149.8854112254399240, -167.3899795514095672, 39.65701158161629536 ) ) ;
#13109=ADVANCED_FACE ( 'NONE', ( #4556 ), #14910, .F. ) ;
#13110=CARTESIAN_POINT ( 'NONE',  ( -159.0959885057557983, -167.4584106276440423, 44.11586579668791330 ) ) ;
#13111=CARTESIAN_POINT ( 'NONE',  ( -151.4692556286852891, -191.6438272943107108, 39.74470866294723947 ) ) ;
#13115=CARTESIAN_POINT ( 'NONE',  ( -151.4692556286853176, -174.2391397928654726, 39.65701158161629536 ) ) ;
#13117=CARTESIAN_POINT ( 'NONE',  ( -154.5594255724347761, -183.9630981290893033, 59.16757674456785310 ) ) ;
#13120=CARTESIAN_POINT ( 'NONE',  ( -148.5561028927606344, -158.7938272943107449, 40.69124936498395328 ) ) ;
#13121=CARTESIAN_POINT ( 'NONE',  ( -160.8964159109769696, -182.0084106276440536, 52.72008163687743121 ) ) ;
#13124=CARTESIAN_POINT ( 'NONE',  ( -143.8425227516148084, -171.9584106276440423, 55.19815736654470584 ) ) ;
#13126=PLANE ( 'NONE',  #10 ) ;
#13146=CARTESIAN_POINT ( 'NONE',  ( -160.8964159109769696, -157.7438272943107336, 52.72008163687743121 ) ) ;
#13148=CARTESIAN_POINT ( 'NONE',  ( -157.2955611005346270, -185.6084106276440195, 41.63779006702063867 ) ) ;
#13151=CARTESIAN_POINT ( 'NONE',  ( -151.4692556286852607, -159.2391397928654726, 39.65701158161629536 ) ) ;
#13162=CARTESIAN_POINT ( 'NONE',  ( -158.9748091281504401, -126.9891397928655010, 62.65701158161630957 ) ) ;
#13164=CARTESIAN_POINT ( 'NONE',  ( -145.2889157411863721, -177.5391397928654840, 41.15050349809590102 ) ) ;
#13167=CARTESIAN_POINT ( 'NONE',  ( -145.6429501568359797, -185.9438272943107506, 41.63779006702063867 ) ) ;
#13172=CARTESIAN_POINT ( 'NONE',  ( -157.2955611005346270, -184.4438272943107506, 57.67623309621198047 ) ) ;
#13173=AXIS2_PLACEMENT_3D ( 'NONE', #18457, #10083, #11837 ) ;
#13184=AXIS2_PLACEMENT_3D ( 'NONE', #10874, #20898, #11259 ) ;
#13187=CARTESIAN_POINT ( 'NONE',  ( -143.8425227516148084, -156.3584106276440480, 44.11586579668791330 ) ) ;
#13189=CARTESIAN_POINT ( 'NONE',  ( -148.5561028927606344, -161.7938272943107449, 40.69124936498395328 ) ) ;
#13190=CARTESIAN_POINT ( 'NONE',  ( -151.4692556286852607, -166.7391397928654158, 59.65701158161632378 ) ) ;
#13191=CARTESIAN_POINT ( 'NONE',  ( -148.3790856849358306, -174.6630981290893203, 59.16757674456786020 ) ) ;
#13197=CARTESIAN_POINT ( 'NONE',  ( -159.5594255724347761, -182.1891397928654612, 55.53486410454104316 ) ) ;
#13202=CARTESIAN_POINT ( 'NONE',  ( -145.2889157411863437, -186.5391397928654271, 41.15050349809589392 ) ) ;
#13206=CARTESIAN_POINT ( 'NONE',  ( -151.4692556286852607, -167.3130981290893260, 39.65701158161629536 ) ) ;
#13214=CARTESIAN_POINT ( 'NONE',  ( -154.3824083646099439, -169.5584106276440366, 58.62277379824867296 ) ) ;
#13215=CARTESIAN_POINT ( 'NONE',  ( -154.3824083646099439, -187.2938272943107449, 58.62277379824867296 ) ) ;
#13227=CARTESIAN_POINT ( 'NONE',  ( -157.2955611005346270, -157.4438272943107506, 57.67623309621198047 ) ) ;
#13228=CARTESIAN_POINT ( 'NONE',  ( -157.2955611005345986, -172.7084106276440423, 57.67623309621197336 ) ) ;
#13231=CARTESIAN_POINT ( 'NONE',  ( -160.8964159109769696, -158.1584106276440593, 49.65701158161630957 ) ) ;
#13247=AXIS2_PLACEMENT_3D ( 'NONE', #21631, #2879, #7752 ) ;
#13257=CARTESIAN_POINT ( 'NONE',  ( -151.4692556286852891, -155.6438272943107393, 39.74470866294723947 ) ) ;
#13258=VECTOR ( 'NONE', #19295, 1000.000000000000000 ) ;
#13260=CARTESIAN_POINT ( 'NONE',  ( -160.8964159109769696, -188.3084106276440366, 46.59394152635518793 ) ) ;
#13263=EDGE_CURVE ( 'NONE', #2272, #21208, #17884, .T. ) ;
#13278=CARTESIAN_POINT ( 'NONE',  ( -141.4692556286852891, -195.0630981290893260, 49.65701158161630957 ) ) ;
#13281=CARTESIAN_POINT ( 'NONE',  ( -148.3790856849358306, -177.3891397928654783, 40.14644641866477315 ) ) ;
#13284=CARTESIAN_POINT ( 'NONE',  ( -145.6429501568359797, -194.9438272943107222, 41.63779006702063867 ) ) ;
#13288=CARTESIAN_POINT ( 'NONE',  ( -151.4692556286852891, -187.1438272943106824, 59.56931450028537967 ) ) ;
#13300=CARTESIAN_POINT ( 'NONE',  ( -151.4692556286852607, -171.2391397928654726, 39.65701158161629536 ) ) ;
#13305=CARTESIAN_POINT ( 'NONE',  ( -151.4692556286852891, -157.1438272943107393, 59.56931450028537256 ) ) ;
#13307=CARTESIAN_POINT ( 'NONE',  ( -143.3790856849358306, -165.6891397928654897, 43.77915905869157598 ) ) ;
#13308=CARTESIAN_POINT ( 'NONE',  ( -148.3790856849358306, -179.4630981290893033, 40.14644641866477315 ) ) ;
#13310=CARTESIAN_POINT ( 'NONE',  ( -161.4692556286852891, -191.6391397928654499, 46.40781461928724383 ) ) ;
#13319=CARTESIAN_POINT ( 'NONE',  ( -151.4692556286852891, -185.3130981290893260, 39.65701158161630246 ) ) ;
#13325=( BOUNDED_CURVE ( )  B_SPLINE_CURVE ( 2, ( #17625, #15969, #880, #1427, #20069, #4956, #6732, #3301, #14860, #8155, #8268, #16510, #4615 ),
 .UNSPECIFIED., .F., .F. ) 
 B_SPLINE_CURVE_WITH_KNOTS ( ( 3, 2, 2, 2, 2, 2, 3 ),
 ( 0.6607142857142856984, 0.6642857142857142572, 0.6714285714285713746, 0.6785714285714286031, 0.6857142857142857206, 0.6928571428571428381, 0.6964285714285713969 ),
 .UNSPECIFIED. ) 
 CURVE ( )  GEOMETRIC_REPRESENTATION_ITEM ( )  RATIONAL_B_SPLINE_CURVE ( ( 0.9755282581475768211, 0.9755282581475768211, 1.000000000000000000, 0.9510565162951535312, 1.000000000000000000, 0.9510565162951535312, 1.000000000000000000, 0.9510565162951535312, 1.000000000000000000, 0.9510565162951535312, 1.000000000000000000, 0.9755282581475768211, 0.9755282581475768211 ) ) 
 REPRESENTATION_ITEM ( '' )  );
#13331=CARTESIAN_POINT ( 'NONE',  ( -160.8964159109769696, -170.0084106276440252, 52.72008163687743121 ) ) ;
#13332=CARTESIAN_POINT ( 'NONE',  ( -143.8425227516148084, -186.0938272943107279, 44.11586579668791330 ) ) ;
#13341=CARTESIAN_POINT ( 'NONE',  ( -151.4692556286852891, -161.6438272943107393, 39.74470866294723947 ) ) ;
#13342=CARTESIAN_POINT ( 'NONE',  ( -145.6429501568359797, -178.1084106276440480, 57.67623309621197336 ) ) ;
#13345=CARTESIAN_POINT ( 'NONE',  ( -160.8964159109769696, -164.3084106276440650, 46.59394152635518793 ) ) ;
#13352=CARTESIAN_POINT ( 'NONE',  ( -148.3790856849358306, -192.3891397928654783, 40.14644641866477315 ) ) ;
#13359=FACE_OUTER_BOUND ( 'NONE', #6064, .T. ) ;
#13361=DIRECTION ( 'NONE',  ( -0.000000000000000000, 1.000000000000000000, -0.000000000000000000 ) ) ;
#13368=CARTESIAN_POINT ( 'NONE',  ( -143.8425227516148084, -189.3584106276440480, 44.11586579668791330 ) ) ;
#13370=CARTESIAN_POINT ( 'NONE',  ( -148.5561028927606344, -177.0584106276440366, 40.69124936498395328 ) ) ;
#13373=CARTESIAN_POINT ( 'NONE',  ( -145.2889157411863437, -160.4391397928654612, 58.16351966513671812 ) ) ;
#13386=DIRECTION ( 'NONE',  ( -0.000000000000000000, 1.000000000000000000, -0.000000000000000000 ) ) ;
#13388=CARTESIAN_POINT ( 'NONE',  ( -154.5594255724347761, -178.8891397928654783, 59.16757674456785310 ) ) ;
#13391=DIRECTION ( 'NONE',  ( -0.000000000000000000, 1.000000000000000000, -0.000000000000000000 ) ) ;
#13395=CARTESIAN_POINT ( 'NONE',  ( -151.4692556286852891, -176.6438272943107393, 39.74470866294723947 ) ) ;
#13404=CARTESIAN_POINT ( 'NONE',  ( -145.6429501568359797, -191.9438272943106938, 41.63779006702063867 ) ) ;
#13413=CARTESIAN_POINT ( 'NONE',  ( -142.0420953463935803, -165.2438272943107052, 46.59394152635518083 ) ) ;
#13415=CARTESIAN_POINT ( 'NONE',  ( -141.4692556286852891, -167.9130981290892635, 46.40781461928724383 ) ) ;
#13421=CARTESIAN_POINT ( 'NONE',  ( -157.6495955161842062, -167.9391397928654897, 41.15050349809589392 ) ) ;
#13425=CARTESIAN_POINT ( 'NONE',  ( -149.8854112254399240, -155.3899795514095672, 39.65701158161629536 ) ) ;
#13432=DIRECTION ( 'NONE',  ( 1.000000000000000000, 0.000000000000000000, 0.000000000000000000 ) ) ;
#13436=CARTESIAN_POINT ( 'NONE',  ( -154.3824083646099439, -167.7584106276440536, 40.69124936498395328 ) ) ;
#13437=CARTESIAN_POINT ( 'NONE',  ( -143.8425227516148084, -189.0938272943107279, 44.11586579668791330 ) ) ;
#13449=CARTESIAN_POINT ( 'NONE',  ( -142.0420953463935803, -159.2438272943107620, 46.59394152635518793 ) ) ;
#13450=CARTESIAN_POINT ( 'NONE',  ( -157.2955611005345986, -175.7084106276440707, 57.67623309621197336 ) ) ;
#13451=ORIENTED_EDGE ( 'NONE', *, *, #1011, .F. ) ;
#13453=CARTESIAN_POINT ( 'NONE',  ( -157.2955611005346270, -163.7084106276440139, 57.67623309621198047 ) ) ;
#13461=CARTESIAN_POINT ( 'NONE',  ( -145.2889157411863437, -193.4391397928654612, 58.16351966513671812 ) ) ;
#13462=VERTEX_POINT ( 'NONE', #11941 ) ;
#13466=EDGE_CURVE ( 'NONE', #9846, #3209, #3573, .T. ) ;
#13470=DIRECTION ( 'NONE',  ( -0.000000000000000000, 1.000000000000000000, -0.000000000000000000 ) ) ;
#13474=ORIENTED_EDGE ( 'NONE', *, *, #21595, .F. ) ;
#13476=CARTESIAN_POINT ( 'NONE',  ( -145.6429501568359797, -183.2084106276440423, 41.63779006702063867 ) ) ;
#13478=CARTESIAN_POINT ( 'NONE',  ( -151.4692556286852891, -176.9084106276440309, 39.74470866294723947 ) ) ;
#13495=CARTESIAN_POINT ( 'NONE',  ( -141.4692556286852891, -175.1391397928654783, 52.90620854394536821 ) ) ;
#13496=CARTESIAN_POINT ( 'NONE',  ( -157.6495955161842062, -181.1130981290893089, 58.16351966513671812 ) ) ;
#13503=CARTESIAN_POINT ( 'NONE',  ( -160.8964159109769696, -169.8938272943107393, 49.65701158161630957 ) ) ;
#13518=CARTESIAN_POINT ( 'NONE',  ( -161.4692556286853176, -169.5630981290893260, 49.65701158161630957 ) ) ;
#13519=CARTESIAN_POINT ( 'NONE',  ( -143.3790856849358306, -173.7630981290892862, 43.77915905869157598 ) ) ;
#13521=CARTESIAN_POINT ( 'NONE',  ( -161.4692556286852607, -166.4130981290893203, 52.90620854394536821 ) ) ;
#13525=CARTESIAN_POINT ( 'NONE',  ( -143.3790856849358306, -183.6891397928654612, 43.77915905869157598 ) ) ;
#13530=CARTESIAN_POINT ( 'NONE',  ( -145.2889157411863437, -186.5130981290893146, 58.16351966513671812 ) ) ;
#13540=CARTESIAN_POINT ( 'NONE',  ( -141.4692556286852891, -195.9891397928654726, 49.65701158161630957 ) ) ;
#13541=CARTESIAN_POINT ( 'NONE',  ( -154.3824083646099439, -193.2938272943107449, 58.62277379824867296 ) ) ;
#13546=CARTESIAN_POINT ( 'NONE',  ( -143.9637021292201950, -126.9891397928655010, 62.65701158161630957 ) ) ;
#13549=CARTESIAN_POINT ( 'NONE',  ( -142.0420953463935803, -165.5438272943107165, 52.72008163687743831 ) ) ;
#13550=CARTESIAN_POINT ( 'NONE',  ( -157.2955611005345986, -178.7084106276440423, 57.67623309621197336 ) ) ;
#13554=CARTESIAN_POINT ( 'NONE',  ( -159.0959885057557983, -157.8584106276440480, 55.19815736654470584 ) ) ;
#13577=CARTESIAN_POINT ( 'NONE',  ( -157.2955611005346270, -182.6084106276440480, 41.63779006702063867 ) ) ;
#13579=CARTESIAN_POINT ( 'NONE',  ( -148.5561028927606344, -178.2584106276440536, 58.62277379824867296 ) ) ;
#13596=CARTESIAN_POINT ( 'NONE',  ( -161.4692556286852607, -179.3391397928654953, 52.90620854394536821 ) ) ;
#13604=CARTESIAN_POINT ( 'NONE',  ( -159.0959885057557983, -176.1938272943107506, 44.11586579668791330 ) ) ;
#13617=DIRECTION ( 'NONE',  ( -0.000000000000000000, 1.000000000000000000, -0.000000000000000000 ) ) ;
#13619=DIRECTION ( 'NONE',  ( 0.000000000000000000, 1.000000000000000000, 0.000000000000000000 ) ) ;
#13622=CARTESIAN_POINT ( 'NONE',  ( -141.4692556286852891, -165.0630981290893260, 49.65701158161630957 ) ) ;
#13634=CARTESIAN_POINT ( 'NONE',  ( -148.3790856849358306, -155.4630981290893033, 40.14644641866477315 ) ) ;
#13636=( BOUNDED_CURVE ( )  B_SPLINE_CURVE ( 2, ( #12369, #20867, #9190, #12049, #2450, #18999, #8758, #376, #7105, #20548, #4108, #2342, #10844 ),
 .UNSPECIFIED., .F., .F. ) 
 B_SPLINE_CURVE_WITH_KNOTS ( ( 3, 2, 2, 2, 2, 2, 3 ),
 ( 0.3392857142857142461, 0.3428571428571428603, 0.3499999999999999778, 0.3571428571428571508, 0.3642857142857142683, 0.3714285714285714413, 0.3750000000000000000 ),
 .UNSPECIFIED. ) 
 CURVE ( )  GEOMETRIC_REPRESENTATION_ITEM ( )  RATIONAL_B_SPLINE_CURVE ( ( 0.9755282581475768211, 0.9755282581475765991, 1.000000000000000000, 0.9510565162951535312, 1.000000000000000000, 0.9510565162951535312, 1.000000000000000000, 0.9510565162951535312, 1.000000000000000000, 0.9510565162951535312, 1.000000000000000000, 0.9755282581475768211, 0.9755282581475768211 ) ) 
 REPRESENTATION_ITEM ( '' )  );
#13639=DIRECTION ( 'NONE',  ( -0.000000000000000000, 1.000000000000000000, -0.000000000000000000 ) ) ;
#13647=CARTESIAN_POINT ( 'NONE',  ( -148.5561028927606344, -157.2584106276440536, 58.62277379824867296 ) ) ;
#13648=CARTESIAN_POINT ( 'NONE',  ( -157.2955611005345986, -181.4438272943107506, 57.67623309621197336 ) ) ;
#13659=CARTESIAN_POINT ( 'NONE',  ( -142.0420953463936087, -171.6584106276440593, 49.65701158161630957 ) ) ;
#13661=CARTESIAN_POINT ( 'NONE',  ( -160.8964159109769696, -158.3084106276440650, 46.59394152635518793 ) ) ;
#13682=CARTESIAN_POINT ( 'NONE',  ( -160.8964159109769696, -179.0438272943107449, 46.59394152635518793 ) ) ;
#13685=CARTESIAN_POINT ( 'NONE',  ( -159.0959885057557983, -185.4584106276440707, 44.11586579668791330 ) ) ;
#13687=CARTESIAN_POINT ( 'NONE',  ( -160.8964159109769696, -173.0084106276440821, 52.72008163687743121 ) ) ;
#13704=CARTESIAN_POINT ( 'NONE',  ( -143.3790856849358306, -169.2891397928654840, 55.53486410454105027 ) ) ;
#13711=CARTESIAN_POINT ( 'NONE',  ( -157.2955611005346270, -169.4438272943107222, 57.67623309621198047 ) ) ;
#13716=CARTESIAN_POINT ( 'NONE',  ( -151.4692556286852891, -176.3130981290892976, 39.65701158161629536 ) ) ;
#13717=CARTESIAN_POINT ( 'NONE',  ( -156.1828648351502409, -155.3945647575688156, 41.49286807254280518 ) ) ;
#13720=VERTEX_POINT ( 'NONE', #11361 ) ;
#13729=CARTESIAN_POINT ( 'NONE',  ( -142.0420953463935803, -156.5438272943107449, 52.72008163687743831 ) ) ;
#13731=CARTESIAN_POINT ( 'NONE',  ( -143.3790856849358306, -171.3630981290893089, 55.53486410454105027 ) ) ;
#13752=CARTESIAN_POINT ( 'NONE',  ( -148.3790856849358306, -195.3891397928654783, 40.14644641866477315 ) ) ;
#13753=CARTESIAN_POINT ( 'NONE',  ( -157.2955611005345986, -176.3438272943106995, 41.63779006702063867 ) ) ;
#13754=CARTESIAN_POINT ( 'NONE',  ( -145.2889157411863437, -177.5391397928654840, 41.15050349809589392 ) ) ;
#13755=CARTESIAN_POINT ( 'NONE',  ( -157.6495955161842062, -193.1130981290893374, 58.16351966513671812 ) ) ;
#13763=CARTESIAN_POINT ( 'NONE',  ( -151.4692556286852891, -163.4084106276440309, 59.56931450028537256 ) ) ;
#13765=( BOUNDED_CURVE ( )  B_SPLINE_CURVE ( 2, ( #2260, #8997, #15705, #611, #7347, #14051, #4341 ),
 .UNSPECIFIED., .F., .F. ) 
 B_SPLINE_CURVE_WITH_KNOTS ( ( 3, 2, 2, 3 ),
 ( 0.000000000000000000, 0.007142857142857142634, 0.01428571428571428527, 0.01785714285714287350 ),
 .UNSPECIFIED. ) 
 CURVE ( )  GEOMETRIC_REPRESENTATION_ITEM ( )  RATIONAL_B_SPLINE_CURVE ( ( 1.000000000000000000, 0.9510565162951535312, 1.000000000000000000, 0.9510565162951535312, 1.000000000000000000, 0.9755282581475765991, 0.9755282581475767101 ) ) 
 REPRESENTATION_ITEM ( '' )  );
#13780=FACE_OUTER_BOUND ( 'NONE', #14989, .T. ) ;
#13786=CARTESIAN_POINT ( 'NONE',  ( -145.6429501568359797, -177.8438272943106995, 57.67623309621198047 ) ) ;
#13789=CARTESIAN_POINT ( 'NONE',  ( -160.8964159109769696, -188.1584106276440593, 49.65701158161630957 ) ) ;
#13791=CARTESIAN_POINT ( 'NONE',  ( -157.2955611005346270, -179.6084106276440764, 41.63779006702063867 ) ) ;
#13793=VECTOR ( 'NONE', #8082, 1000.000000000000000 ) ;
#13799=EDGE_LOOP ( 'NONE', ( #8744, #18422, #6115, #1586, #20797, #5767 ) ) ;
#13802=VERTEX_POINT ( 'NONE', #6522 ) ;
#13810=CARTESIAN_POINT ( 'NONE',  ( -151.4692556286853176, -175.7391397928654726, 59.65701158161632378 ) ) ;
#13811=CARTESIAN_POINT ( 'NONE',  ( -161.4692556286853176, -173.4891397928654726, 49.65701158161630957 ) ) ;
#13812=DIRECTION ( 'NONE',  ( -0.000000000000000000, 1.000000000000000000, -0.000000000000000000 ) ) ;
#13817=CARTESIAN_POINT ( 'NONE',  ( -148.5561028927606344, -173.7938272943107165, 40.69124936498395328 ) ) ;
#13819=CARTESIAN_POINT ( 'NONE',  ( -161.4692556286852891, -170.6391397928654499, 46.40781461928724383 ) ) ;
#13823=EDGE_CURVE ( 'NONE', #9846, #10182, #920, .T. ) ;
#13834=CARTESIAN_POINT ( 'NONE',  ( -151.4692556286852891, -196.9891397928655010, 40.65701158161630246 ) ) ;
#13839=CARTESIAN_POINT ( 'NONE',  ( -141.4692556286852891, -171.2130981290893033, 52.90620854394536821 ) ) ;
#13851=CARTESIAN_POINT ( 'NONE',  ( -151.4692556286852891, -196.9891397928655010, 59.65701158161632378 ) ) ;
#13855=CARTESIAN_POINT ( 'NONE',  ( -141.4692556286852891, -171.8391397928654669, 46.40781461928724383 ) ) ;
#13859=CARTESIAN_POINT ( 'NONE',  ( -157.2955611005346270, -158.6084106276440480, 41.63779006702063867 ) ) ;
#13860=CARTESIAN_POINT ( 'NONE',  ( -145.6429501568359797, -177.8438272943106995, 57.67623309621197336 ) ) ;
#13864=CARTESIAN_POINT ( 'NONE',  ( -158.9748091281504401, -116.9891397928655010, 62.65701158161630957 ) ) ;
#13871=CARTESIAN_POINT ( 'NONE',  ( -145.6429501568359797, -169.1084106276440480, 57.67623309621197336 ) ) ;
#13894=CARTESIAN_POINT ( 'NONE',  ( -148.5561028927606344, -183.9938272943107336, 58.62277379824867296 ) ) ;
#13895=CARTESIAN_POINT ( 'NONE',  ( -142.0420953463935803, -192.5084106276440252, 46.59394152635518083 ) ) ;
#13897=CARTESIAN_POINT ( 'NONE',  ( -148.5561028927606344, -177.0584106276440366, 40.69124936498395328 ) ) ;
#13906=ORIENTED_EDGE ( 'NONE', *, *, #13052, .T. ) ;
#13915=CARTESIAN_POINT ( 'NONE',  ( -157.6495955161842062, -170.9391397928654328, 41.15050349809590102 ) ) ;
#13916=CARTESIAN_POINT ( 'NONE',  ( -151.4692556286852891, -196.9891397928655010, 49.65701158161630957 ) ) ;
#13922=CARTESIAN_POINT ( 'NONE',  ( -157.2955611005346270, -163.4438272943107506, 57.67623309621198047 ) ) ;
#13932=EDGE_LOOP ( 'NONE', ( #16264, #19632, #18865, #6459 ) ) ;
#13937=CARTESIAN_POINT ( 'NONE',  ( -148.3790856849358306, -180.3891397928654783, 40.14644641866477315 ) ) ;
#13945=CARTESIAN_POINT ( 'NONE',  ( -159.5594255724347761, -157.2630981290893146, 55.53486410454104316 ) ) ;
#13950=CARTESIAN_POINT ( 'NONE',  ( -151.4692556286853176, -179.3130981290892976, 39.65701158161629536 ) ) ;
#13955=VECTOR ( 'NONE', #12176, 1000.000000000000000 ) ;
#13959=( BOUNDED_CURVE ( )  B_SPLINE_CURVE ( 2, ( #20481, #5372, #3724, #308, #18818, #7036, #11876, #8253, #11764, #10126, #13634, #13425, #191 ),
 .UNSPECIFIED., .F., .F. ) 
 B_SPLINE_CURVE_WITH_KNOTS ( ( 3, 2, 2, 2, 2, 2, 3 ),
 ( 0.9107142857142856984, 0.9142857142857142572, 0.9214285714285713746, 0.9285714285714286031, 0.9357142857142857206, 0.9428571428571428381, 0.9464285714285713969 ),
 .UNSPECIFIED. ) 
 CURVE ( )  GEOMETRIC_REPRESENTATION_ITEM ( )  RATIONAL_B_SPLINE_CURVE ( ( 0.9755282581475768211, 0.9755282581475768211, 1.000000000000000000, 0.9510565162951535312, 1.000000000000000000, 0.9510565162951535312, 1.000000000000000000, 0.9510565162951535312, 1.000000000000000000, 0.9510565162951535312, 1.000000000000000000, 0.9755282581475768211, 0.9755282581475768211 ) ) 
 REPRESENTATION_ITEM ( '' )  );
#13967=CARTESIAN_POINT ( 'NONE',  ( -145.6429501568359797, -182.9438272943107222, 41.63779006702063867 ) ) ;
#13977=CARTESIAN_POINT ( 'NONE',  ( -142.0420953463936087, -156.3938272943107393, 49.65701158161630957 ) ) ;
#13978=CARTESIAN_POINT ( 'NONE',  ( -159.0959885057557983, -161.4584106276440423, 44.11586579668791330 ) ) ;
#13983=CARTESIAN_POINT ( 'NONE',  ( -151.4692556286852891, -187.7391397928655010, 59.65701158161632378 ) ) ;
#13987=CARTESIAN_POINT ( 'NONE',  ( -161.4692556286852891, -179.3391397928654669, 52.90620854394536821 ) ) ;
#14000=CARTESIAN_POINT ( 'NONE',  ( -153.0531000319307111, -173.2362167067690564, 39.65701158161631668 ) ) ;
#14004=CARTESIAN_POINT ( 'NONE',  ( -157.2955611005346270, -185.3438272943106995, 41.63779006702063867 ) ) ;
#14005=CARTESIAN_POINT ( 'NONE',  ( -157.2955611005345986, -191.6084106276440480, 41.63779006702063867 ) ) ;
#14007=CARTESIAN_POINT ( 'NONE',  ( -160.8964159109769696, -176.0084106276440536, 52.72008163687743121 ) ) ;
#14021=( BOUNDED_SURFACE ( )  B_SPLINE_SURFACE ( 1, 2, ( 
 ( #2355, #14035, #10637, #6089, #17341, #9094, #14359, #916, #5983, #7662, #5661, #12384, #12710, #19119, #4014, #19433, #17662, #15795, #17551, #705, #7438, #14141, #20878, #5766, #12495, #2460, #9200, #19221, #4119, #12604, #15898, #810, #7547, #20989, #5874, #11162, #21753, #19877, #2787, #19997, #4881, #9850, #21648, #6426, #6539, #8305, #9529, #16226, #3230, #13260, #1137, #11485, #11600, #15013, #16552, #18330, #17986, #14571, #18214, #7872, #4546, #4430, #2900, #17875, #3119, #21313, #1577, #13148, #9963, #16666, #1467, #12930, #9745, #12817, #6198, #4764, #7978, #19536, #19654, #3008, #11267, #14900, #14685, #8199, #9635, #16335, #21425, #16442, #1244, #6314, #13041, #19765, #4662, #11377, #18098, #1356, #8087, #14794, #21536, #3561, #8743, #8633, #15352, #16778, #1897, #8418, #20421, #13791, #18442, #6663, #15128, #6769, #15460, #16882, #31, #10396, #13579, #11707, #20107, #15243, #10285, #3458, #5104, #18765, #13370, #13478, #3666, #6872, #246, #10069, #360, #20316, #17096, #2012, #7088, #4996, #3341, #1688, #20211, #6984, #10181, #8530, #11820, #18552, #12031, #1799, #141, #5214, #11928, #18657, #16990, #13687, #5318, #8153, #17945, #19721, #2962, #4954, #14966, #14858, #11662, #6269, #4502, #16402, #14752, #3299, #21493, #13000, #9594, #9918, #1425, #13331, #16733, #18286, #13214, #6615, #2851, #11225, #20067, #6380, #11442, #8376, #18400, #10027, #1644, #21605, #13436, #8048, #13110, #16624, #9702, #3189, #4613, #1313, #19832, #15085, #14775, #6730, #4722, #19951, #16295, #6495, #11334, #1533, #18167, #3075, #14640, #9812, #16508, #1201, #21713, #8266, #4836, #7936, #21382, #11558, #18055, #10139, #15422, #3521, #15521, #20381, #17165, #10247, #102, #3735, #8490, #11888, #11777, #16945, #3417, #10465, #6834, #8917, #20492, #17270, #10569, #2079, #20275, #17056, #15620, #18506, #5381, #15310, #7562, #2182, #10353, #13859, #424, #202, #12096, #826, #3842, #6941, #1968, #7156, #13647, #16842, #5168, #18829, #1861, #20174, #1755, #8810, #5278, #317, #8702, #7046, #15199 ),
 ( #13540, #5482, #11992, #18722, #13752, #20596, #12207, #5064, #18617, #18942, #8591, #3629, #21006, #16021, #7677, #21439, #11284, #7887, #5996, #4240, #14260, #18114, #3025, #12726, #9650, #18004, #16351, #4563, #9760, #17678, #1260, #16458, #10966, #2916, #12947, #14375, #6104, #4675, #2690, #6330, #2581, #14702, #7997, #12834, #19552, #9319, #9434, #14588, #933, #4448, #13056, #2804, #21114, #12619, #1370, #21331, #19449, #19782, #11391, #5888, #19340, #6216, #4342, #11068, #17782, #16137, #1046, #7780, #14480, #19669, #21224, #11178, #17891, #9542, #16244, #1152, #3474, #11946, #14809, #16901, #10198, #20016, #21551, #9867, #1485, #15259, #5120, #1706, #21666, #19895, #8102, #18676, #3578, #6557, #1814, #11838, #8547, #20228, #10305, #11504, #157, #17007, #4784, #18568, #6790, #8217, #21773, #20334, #18347, #6889, #18234, #13596, #5231, #6679, #13388, #3136, #3250, #8436, #16566, #20123, #6442, #18458, #14916, #13164, #13281, #15145, #4900, #11619, #9979, #16683, #1593, #45, #8324, #15034, #5016, #11724, #3359, #10084, #16794, #13495, #10734, #4109, #5652, #15787, #7106, #3683, #7325, #12050, #15476, #15372, #13811, #7000, #14026, #10411, #12485, #2239, #20868, #14129, #20759, #2029, #20654, #19212, #265, #8973, #18885, #10845, #5756, #13915, #17435, #4005, #3793, #15678, #1915, #7429, #10522, #5538, #2343, #17217, #13704, #8759, #582, #20549, #8650, #20440, #12370, #2135, #3901, #12265, #10625, #5332, #377, #19110, #9081, #694, #18779, #17332, #17113, #5432, #12152, #8867, #15575, #479, #7215, #19000, #4423, #12701, #7652, #11256, #19756, #4216, #19645, #2661, #17868, #7536, #1234, #9406, #4536, #17977, #2888, #4650, #6304, #21305, #7864, #17759, #802, #5866, #21196, #6189, #11043, #16115, #11153, #2780, #15997, #17542, #9626, #9520, #16325, #6082, #9192, #10946, #907, #7969, #12920, #12809, #14675, #19318, #2451, #14351, #5973, #13032, #19422, #17653, #14239, #1129, #14456, #15889, #20978, #16219, #14563, #12597, #2559, #9296, #21092, #4319, #1021, #7757, #19529, #16873, #10173 ) ),
 .UNSPECIFIED., .F., .F., .F. ) 
 B_SPLINE_SURFACE_WITH_KNOTS ( ( 2, 2 ),
 ( 3, 2, 2, 2, 2, 2, 2, 2, 2, 2, 2, 2, 2, 2, 2, 2, 2, 2, 2, 2, 2, 2, 2, 2, 2, 2, 2, 2, 2, 2, 2, 2, 2, 2, 2, 2, 2, 2, 2, 2, 2, 2, 2, 2, 2, 2, 2, 2, 2, 2, 2, 2, 2, 2, 2, 2, 2, 2, 2, 2, 2, 2, 2, 2, 2, 2, 2, 2, 2, 2, 2, 2, 2, 2, 2, 2, 2, 2, 2, 2, 2, 2, 2, 2, 2, 2, 2, 2, 2, 2, 2, 2, 2, 2, 2, 2, 2, 2, 2, 2, 2, 2, 2, 2, 2, 2, 2, 2, 2, 2, 2, 2, 2, 2, 2, 2, 2, 2, 2, 2, 2, 2, 2, 2, 2, 2, 2, 2, 2, 2, 2, 2, 2, 2, 3 ),
 ( 0.000000000000000000, 1.000000000000000000 ),
 ( 0.000000000000000000, 0.007142857142857142634, 0.01428571428571428527, 0.02142857142857142877, 0.02857142857142857054, 0.03571428571428571230, 0.04285714285714285754, 0.05000000000000000278, 0.05714285714285714107, 0.06428571428571427937, 0.07142857142857142461, 0.07857142857142856984, 0.08571428571428571508, 0.09285714285714286031, 0.1000000000000000056, 0.1071428571428571369, 0.1142857142857142821, 0.1214285714285714274, 0.1285714285714285587, 0.1357142857142857040, 0.1428571428571428492, 0.1499999999999999944, 0.1571428571428571397, 0.1642857142857142849, 0.1714285714285714302, 0.1785714285714285754, 0.1857142857142857206, 0.1928571428571428659, 0.2000000000000000111, 0.2071428571428571563, 0.2142857142857142738, 0.2214285714285714191, 0.2285714285714285643, 0.2357142857142857095, 0.2428571428571428548, 0.2500000000000000000, 0.2571428571428571175, 0.2642857142857142905, 0.2714285714285714080, 0.2785714285714285809, 0.2857142857142856984, 0.2928571428571428714, 0.2999999999999999889, 0.3071428571428571619, 0.3142857142857142794, 0.3214285714285714524, 0.3285714285714285698, 0.3357142857142856873, 0.3428571428571428603, 0.3499999999999999778, 0.3571428571428571508, 0.3642857142857142683, 0.3714285714285714413, 0.3785714285714285587, 0.3857142857142857317, 0.3928571428571428492, 0.4000000000000000222, 0.4071428571428571397, 0.4142857142857143127, 0.4214285714285714302, 0.4285714285714285476, 0.4357142857142857206, 0.4428571428571428381, 0.4500000000000000111, 0.4571428571428571286, 0.4642857142857143016, 0.4714285714285714191, 0.4785714285714285920, 0.4857142857142857095, 0.4928571428571428825, 0.5000000000000000000, 0.5071428571428571175, 0.5142857142857142350, 0.5214285714285714635, 0.5285714285714285809, 0.5357142857142856984, 0.5428571428571428159, 0.5500000000000000444, 0.5571428571428571619, 0.5642857142857142794, 0.5714285714285713969, 0.5785714285714286254, 0.5857142857142857428, 0.5928571428571428603, 0.5999999999999999778, 0.6071428571428570953, 0.6142857142857143238, 0.6214285714285714413, 0.6285714285714285587, 0.6357142857142856762, 0.6428571428571429047, 0.6500000000000000222, 0.6571428571428571397, 0.6642857142857142572, 0.6714285714285713746, 0.6785714285714286031, 0.6857142857142857206, 0.6928571428571428381, 0.6999999999999999556, 0.7071428571428571841, 0.7142857142857143016, 0.7214285714285714191, 0.7285714285714285365, 0.7357142857142857650, 0.7428571428571428825, 0.7500000000000000000, 0.7571428571428571175, 0.7642857142857142350, 0.7714285714285714635, 0.7785714285714285809, 0.7857142857142856984, 0.7928571428571428159, 0.8000000000000000444, 0.8071428571428571619, 0.8142857142857142794, 0.8214285714285713969, 0.8285714285714286254, 0.8357142857142857428, 0.8428571428571428603, 0.8499999999999999778, 0.8571428571428570953, 0.8642857142857143238, 0.8714285714285714413, 0.8785714285714285587, 0.8857142857142856762, 0.8928571428571429047, 0.9000000000000000222, 0.9071428571428571397, 0.9142857142857142572, 0.9214285714285713746, 0.9285714285714286031, 0.9357142857142857206, 0.9428571428571428381, 0.9499999999999999556, 0.9523897249335829818 ),
 .UNSPECIFIED. ) 
 GEOMETRIC_REPRESENTATION_ITEM ( )  RATIONAL_B_SPLINE_SURFACE ( (
 ( 1.000000000000000000, 0.9510565162951535312, 1.000000000000000000, 0.9510565162951535312, 1.000000000000000000, 0.9510565162951535312, 1.000000000000000000, 0.9510565162951535312, 1.000000000000000000, 0.9510565162951535312, 1.000000000000000000, 0.9510565162951535312, 1.000000000000000000, 0.9510565162951535312, 1.000000000000000000, 0.9510565162951535312, 1.000000000000000000, 0.9510565162951535312, 1.000000000000000000, 0.9510565162951535312, 1.000000000000000000, 0.9510565162951535312, 1.000000000000000000, 0.9510565162951535312, 1.000000000000000000, 0.9510565162951535312, 1.000000000000000000, 0.9510565162951535312, 1.000000000000000000, 0.9510565162951535312, 1.000000000000000000, 0.9510565162951535312, 1.000000000000000000, 0.9510565162951535312, 1.000000000000000000, 0.9510565162951535312, 1.000000000000000000, 0.9510565162951535312, 1.000000000000000000, 0.9510565162951535312, 1.000000000000000000, 0.9510565162951535312, 1.000000000000000000, 0.9510565162951535312, 1.000000000000000000, 0.9510565162951535312, 1.000000000000000000, 0.9510565162951535312, 1.000000000000000000, 0.9510565162951535312, 1.000000000000000000, 0.9510565162951535312, 1.000000000000000000, 0.9510565162951535312, 1.000000000000000000, 0.9510565162951535312, 1.000000000000000000, 0.9510565162951535312, 1.000000000000000000, 0.9510565162951535312, 1.000000000000000000, 0.9510565162951535312, 1.000000000000000000, 0.9510565162951535312, 1.000000000000000000, 0.9510565162951535312, 1.000000000000000000, 0.9510565162951535312, 1.000000000000000000, 0.9510565162951535312, 1.000000000000000000, 0.9510565162951535312, 1.000000000000000000, 0.9510565162951535312, 1.000000000000000000, 0.9510565162951535312, 1.000000000000000000, 0.9510565162951535312, 1.000000000000000000, 0.9510565162951535312, 1.000000000000000000, 0.9510565162951535312, 1.000000000000000000, 0.9510565162951535312, 1.000000000000000000, 0.9510565162951535312, 1.000000000000000000, 0.9510565162951535312, 1.000000000000000000, 0.9510565162951535312, 1.000000000000000000, 0.9510565162951535312, 1.000000000000000000, 0.9510565162951535312, 1.000000000000000000, 0.9510565162951535312, 1.000000000000000000, 0.9510565162951535312, 1.000000000000000000, 0.9510565162951535312, 1.000000000000000000, 0.9510565162951535312, 1.000000000000000000, 0.9510565162951535312, 1.000000000000000000, 0.9510565162951535312, 1.000000000000000000, 0.9510565162951535312, 1.000000000000000000, 0.9510565162951535312, 1.000000000000000000, 0.9510565162951535312, 1.000000000000000000, 0.9510565162951535312, 1.000000000000000000, 0.9510565162951535312, 1.000000000000000000, 0.9510565162951535312, 1.000000000000000000, 0.9510565162951535312, 1.000000000000000000, 0.9510565162951535312, 1.000000000000000000, 0.9510565162951535312, 1.000000000000000000, 0.9510565162951535312, 1.000000000000000000, 0.9510565162951535312, 1.000000000000000000, 0.9510565162951535312, 1.000000000000000000, 0.9510565162951535312, 1.000000000000000000, 0.9510565162951535312, 1.000000000000000000, 0.9510565162951535312, 1.000000000000000000, 0.9510565162951535312, 1.000000000000000000, 0.9510565162951535312, 1.000000000000000000, 0.9510565162951535312, 1.000000000000000000, 0.9510565162951535312, 1.000000000000000000, 0.9510565162951535312, 1.000000000000000000, 0.9510565162951535312, 1.000000000000000000, 0.9510565162951535312, 1.000000000000000000, 0.9510565162951535312, 1.000000000000000000, 0.9510565162951535312, 1.000000000000000000, 0.9510565162951535312, 1.000000000000000000, 0.9510565162951535312, 1.000000000000000000, 0.9510565162951535312, 1.000000000000000000, 0.9510565162951535312, 1.000000000000000000, 0.9510565162951535312, 1.000000000000000000, 0.9510565162951535312, 1.000000000000000000, 0.9510565162951535312, 1.000000000000000000, 0.9510565162951535312, 1.000000000000000000, 0.9510565162951535312, 1.000000000000000000, 0.9510565162951535312, 1.000000000000000000, 0.9510565162951535312, 1.000000000000000000, 0.9510565162951535312, 1.000000000000000000, 0.9510565162951535312, 1.000000000000000000, 0.9510565162951535312, 1.000000000000000000, 0.9510565162951535312, 1.000000000000000000, 0.9510565162951535312, 1.000000000000000000, 0.9510565162951535312, 1.000000000000000000, 0.9510565162951535312, 1.000000000000000000, 0.9510565162951535312, 1.000000000000000000, 0.9510565162951535312, 1.000000000000000000, 0.9510565162951535312, 1.000000000000000000, 0.9510565162951535312, 1.000000000000000000, 0.9510565162951535312, 1.000000000000000000, 0.9510565162951535312, 1.000000000000000000, 0.9510565162951535312, 1.000000000000000000, 0.9510565162951535312, 1.000000000000000000, 0.9510565162951535312, 1.000000000000000000, 0.9510565162951535312, 1.000000000000000000, 0.9510565162951535312, 1.000000000000000000, 0.9510565162951535312, 1.000000000000000000, 0.9510565162951535312, 1.000000000000000000, 0.9510565162951535312, 1.000000000000000000, 0.9510565162951535312, 1.000000000000000000, 0.9510565162951535312, 1.000000000000000000, 0.9510565162951535312, 1.000000000000000000, 0.9510565162951535312, 1.000000000000000000, 0.9510565162951535312, 1.000000000000000000, 0.9510565162951535312, 1.000000000000000000, 0.9510565162951535312, 1.000000000000000000, 0.9510565162951535312, 1.000000000000000000, 0.9510565162951535312, 1.000000000000000000, 0.9510565162951535312, 1.000000000000000000, 0.9510565162951535312, 1.000000000000000000, 0.9510565162951535312, 1.000000000000000000, 0.9510565162951535312, 1.000000000000000000, 0.9510565162951535312, 1.000000000000000000, 0.9510565162951535312, 1.000000000000000000, 0.9510565162951535312, 1.000000000000000000, 0.9510565162951535312, 1.000000000000000000, 0.9510565162951535312, 1.000000000000000000, 0.9510565162951535312, 1.000000000000000000, 0.9510565162951535312, 1.000000000000000000, 0.9510565162951535312, 1.000000000000000000, 0.9510565162951535312, 1.000000000000000000, 0.9510565162951535312, 1.000000000000000000, 0.9510565162951535312, 1.000000000000000000, 0.9836253951315760968, 0.9782074146920120006),
 ( 1.000000000000000000, 0.9510565162951535312, 1.000000000000000000, 0.9510565162951535312, 1.000000000000000000, 0.9510565162951535312, 1.000000000000000000, 0.9510565162951535312, 1.000000000000000000, 0.9510565162951535312, 1.000000000000000000, 0.9510565162951535312, 1.000000000000000000, 0.9510565162951535312, 1.000000000000000000, 0.9510565162951535312, 1.000000000000000000, 0.9510565162951535312, 1.000000000000000000, 0.9510565162951535312, 1.000000000000000000, 0.9510565162951535312, 1.000000000000000000, 0.9510565162951535312, 1.000000000000000000, 0.9510565162951535312, 1.000000000000000000, 0.9510565162951535312, 1.000000000000000000, 0.9510565162951535312, 1.000000000000000000, 0.9510565162951535312, 1.000000000000000000, 0.9510565162951535312, 1.000000000000000000, 0.9510565162951535312, 1.000000000000000000, 0.9510565162951535312, 1.000000000000000000, 0.9510565162951535312, 1.000000000000000000, 0.9510565162951535312, 1.000000000000000000, 0.9510565162951535312, 1.000000000000000000, 0.9510565162951535312, 1.000000000000000000, 0.9510565162951535312, 1.000000000000000000, 0.9510565162951535312, 1.000000000000000000, 0.9510565162951535312, 1.000000000000000000, 0.9510565162951535312, 1.000000000000000000, 0.9510565162951535312, 1.000000000000000000, 0.9510565162951535312, 1.000000000000000000, 0.9510565162951535312, 1.000000000000000000, 0.9510565162951535312, 1.000000000000000000, 0.9510565162951535312, 1.000000000000000000, 0.9510565162951535312, 1.000000000000000000, 0.9510565162951535312, 1.000000000000000000, 0.9510565162951535312, 1.000000000000000000, 0.9510565162951535312, 1.000000000000000000, 0.9510565162951535312, 1.000000000000000000, 0.9510565162951535312, 1.000000000000000000, 0.9510565162951535312, 1.000000000000000000, 0.9510565162951535312, 1.000000000000000000, 0.9510565162951535312, 1.000000000000000000, 0.9510565162951535312, 1.000000000000000000, 0.9510565162951535312, 1.000000000000000000, 0.9510565162951535312, 1.000000000000000000, 0.9510565162951535312, 1.000000000000000000, 0.9510565162951535312, 1.000000000000000000, 0.9510565162951535312, 1.000000000000000000, 0.9510565162951535312, 1.000000000000000000, 0.9510565162951535312, 1.000000000000000000, 0.9510565162951535312, 1.000000000000000000, 0.9510565162951535312, 1.000000000000000000, 0.9510565162951535312, 1.000000000000000000, 0.9510565162951535312, 1.000000000000000000, 0.9510565162951535312, 1.000000000000000000, 0.9510565162951535312, 1.000000000000000000, 0.9510565162951535312, 1.000000000000000000, 0.9510565162951535312, 1.000000000000000000, 0.9510565162951535312, 1.000000000000000000, 0.9510565162951535312, 1.000000000000000000, 0.9510565162951535312, 1.000000000000000000, 0.9510565162951535312, 1.000000000000000000, 0.9510565162951535312, 1.000000000000000000, 0.9510565162951535312, 1.000000000000000000, 0.9510565162951535312, 1.000000000000000000, 0.9510565162951535312, 1.000000000000000000, 0.9510565162951535312, 1.000000000000000000, 0.9510565162951535312, 1.000000000000000000, 0.9510565162951535312, 1.000000000000000000, 0.9510565162951535312, 1.000000000000000000, 0.9510565162951535312, 1.000000000000000000, 0.9510565162951535312, 1.000000000000000000, 0.9510565162951535312, 1.000000000000000000, 0.9510565162951535312, 1.000000000000000000, 0.9510565162951535312, 1.000000000000000000, 0.9510565162951535312, 1.000000000000000000, 0.9510565162951535312, 1.000000000000000000, 0.9510565162951535312, 1.000000000000000000, 0.9510565162951535312, 1.000000000000000000, 0.9510565162951535312, 1.000000000000000000, 0.9510565162951535312, 1.000000000000000000, 0.9510565162951535312, 1.000000000000000000, 0.9510565162951535312, 1.000000000000000000, 0.9510565162951535312, 1.000000000000000000, 0.9510565162951535312, 1.000000000000000000, 0.9510565162951535312, 1.000000000000000000, 0.9510565162951535312, 1.000000000000000000, 0.9510565162951535312, 1.000000000000000000, 0.9510565162951535312, 1.000000000000000000, 0.9510565162951535312, 1.000000000000000000, 0.9510565162951535312, 1.000000000000000000, 0.9510565162951535312, 1.000000000000000000, 0.9510565162951535312, 1.000000000000000000, 0.9510565162951535312, 1.000000000000000000, 0.9510565162951535312, 1.000000000000000000, 0.9510565162951535312, 1.000000000000000000, 0.9510565162951535312, 1.000000000000000000, 0.9510565162951535312, 1.000000000000000000, 0.9510565162951535312, 1.000000000000000000, 0.9510565162951535312, 1.000000000000000000, 0.9510565162951535312, 1.000000000000000000, 0.9510565162951535312, 1.000000000000000000, 0.9510565162951535312, 1.000000000000000000, 0.9510565162951535312, 1.000000000000000000, 0.9510565162951535312, 1.000000000000000000, 0.9510565162951535312, 1.000000000000000000, 0.9510565162951535312, 1.000000000000000000, 0.9510565162951535312, 1.000000000000000000, 0.9510565162951535312, 1.000000000000000000, 0.9510565162951535312, 1.000000000000000000, 0.9510565162951535312, 1.000000000000000000, 0.9510565162951535312, 1.000000000000000000, 0.9510565162951535312, 1.000000000000000000, 0.9510565162951535312, 1.000000000000000000, 0.9510565162951535312, 1.000000000000000000, 0.9510565162951535312, 1.000000000000000000, 0.9510565162951535312, 1.000000000000000000, 0.9510565162951535312, 1.000000000000000000, 0.9510565162951535312, 1.000000000000000000, 0.9510565162951535312, 1.000000000000000000, 0.9510565162951535312, 1.000000000000000000, 0.9510565162951535312, 1.000000000000000000, 0.9510565162951535312, 1.000000000000000000, 0.9510565162951535312, 1.000000000000000000, 0.9510565162951535312, 1.000000000000000000, 0.9510565162951535312, 1.000000000000000000, 0.9510565162951535312, 1.000000000000000000, 0.9510565162951535312, 1.000000000000000000, 0.9510565162951535312, 1.000000000000000000, 0.9510565162951535312, 1.000000000000000000, 0.9510565162951535312, 1.000000000000000000, 0.9510565162951535312, 1.000000000000000000, 0.9510565162951535312, 1.000000000000000000, 0.9510565162951535312, 1.000000000000000000, 0.9836253951315760968, 0.9782074146920120006) ) ) 
 REPRESENTATION_ITEM ( '' )  SURFACE ( )  );
#14026=CARTESIAN_POINT ( 'NONE',  ( -159.5594255724347761, -173.1891397928654897, 55.53486410454104316 ) ) ;
#14032=CARTESIAN_POINT ( 'NONE',  ( -157.2955611005346270, -167.3438272943106995, 41.63779006702063867 ) ) ;
#14035=CARTESIAN_POINT ( 'NONE',  ( -142.0420953463935803, -195.5084106276440536, 46.59394152635518793 ) ) ;
#14037=CARTESIAN_POINT ( 'NONE',  ( -161.4692556286852891, -175.7130981290892748, 46.40781461928724383 ) ) ;
#14038=DIRECTION ( 'NONE',  ( -1.000000000000000000, 0.000000000000000000, -4.622506457652816058E-16 ) ) ;
#14051=CARTESIAN_POINT ( 'NONE',  ( -149.8854112254399524, -194.3899795514095388, 39.65701158161630246 ) ) ;
#14056=CARTESIAN_POINT ( 'NONE',  ( -151.4692556286852891, -156.8130981290892692, 60.17163382399899518 ) ) ;
#14060=CARTESIAN_POINT ( 'NONE',  ( -157.2955611005346270, -190.4438272943107506, 57.67623309621198047 ) ) ;
#14063=ORIENTED_EDGE ( 'NONE', *, *, #7909, .T. ) ;
#14067=LINE ( 'NONE', #13851, #9002 ) ;
#14069=ORIENTED_EDGE ( 'NONE', *, *, #16764, .T. ) ;
#14072=CARTESIAN_POINT ( 'NONE',  ( -141.4692556286852891, -165.2130981290893033, 52.90620854394536821 ) ) ;
#14076=CARTESIAN_POINT ( 'NONE',  ( -142.0420953463935803, -177.2438272943107336, 46.59394152635518083 ) ) ;
#14078=CARTESIAN_POINT ( 'NONE',  ( -154.5594255724347761, -189.9630981290893317, 59.16757674456785310 ) ) ;
#14079=VECTOR ( 'NONE', #9718, 1000.000000000000114 ) ;
#14081=CARTESIAN_POINT ( 'NONE',  ( -149.8854112254399809, -163.6622583705451746, 59.65701158161633089 ) ) ;
#14086=CARTESIAN_POINT ( 'NONE',  ( -148.5561028927606344, -155.7938272943107449, 40.69124936498395328 ) ) ;
#14087=CARTESIAN_POINT ( 'NONE',  ( -159.0959885057557983, -160.8584106276440480, 55.19815736654470584 ) ) ;
#14089=DIRECTION ( 'NONE',  ( 0.000000000000000000, 1.000000000000000000, 0.000000000000000000 ) ) ;
#14096=CARTESIAN_POINT ( 'NONE',  ( -161.4692556286852891, -160.7130981290893033, 46.40781461928724383 ) ) ;
#14097=ORIENTED_EDGE ( 'NONE', *, *, #19040, .F. ) ;
#14104=DIRECTION ( 'NONE',  ( 0.000000000000000000, 1.000000000000000000, 0.000000000000000000 ) ) ;
#14106=CARTESIAN_POINT ( 'NONE',  ( -154.5594255724347761, -191.1630981290893203, 40.14644641866476604 ) ) ;
#14109=CARTESIAN_POINT ( 'NONE',  ( -151.4692556286852891, -178.1438272943106824, 59.56931450028537967 ) ) ;
#14112=CARTESIAN_POINT ( 'NONE',  ( -142.0420953463936087, -180.6584106276440309, 49.65701158161630957 ) ) ;
#14115=ORIENTED_EDGE ( 'NONE', *, *, #7870, .T. ) ;
#14121=ORIENTED_EDGE ( 'NONE', *, *, #882, .T. ) ;
#14128=PLANE ( 'NONE',  #8964 ) ;
#14129=CARTESIAN_POINT ( 'NONE',  ( -145.2889157411863721, -172.4391397928654612, 58.16351966513671812 ) ) ;
#14136=EDGE_LOOP ( 'NONE', ( #10850, #8802, #18474, #14447 ) ) ;
#14138=CARTESIAN_POINT ( 'NONE',  ( -151.4692556286852891, -166.1438272943107393, 59.56931450028537967 ) ) ;
#14141=CARTESIAN_POINT ( 'NONE',  ( -142.0420953463935803, -192.5084106276439968, 46.59394152635518793 ) ) ;
#14156=CARTESIAN_POINT ( 'NONE',  ( -151.4692556286852607, -168.8130981290893260, 59.65701158161632378 ) ) ;
#14163=CARTESIAN_POINT ( 'NONE',  ( -159.5594255724347761, -160.2630981290893146, 55.53486410454104316 ) ) ;
#14180=CARTESIAN_POINT ( 'NONE',  ( -149.8854112254399809, -164.3899795514095672, 39.65701158161628825 ) ) ;
#14184=CARTESIAN_POINT ( 'NONE',  ( -151.4692556286852891, -175.1438272943107393, 59.56931450028537256 ) ) ;
#14186=CARTESIAN_POINT ( 'NONE',  ( -151.4692556286852891, -186.8130981290893260, 60.17163382399899518 ) ) ;
#14194=CARTESIAN_POINT ( 'NONE',  ( -157.2955611005345986, -166.7084106276440423, 57.67623309621197336 ) ) ;
#14203=DIRECTION ( 'NONE',  ( -0.4999999999999993894, 0.000000000000000000, 0.8660254037844389297 ) ) ;
#14218=CARTESIAN_POINT ( 'NONE',  ( -159.0959885057557983, -175.5938272943107279, 55.19815736654470584 ) ) ;
#14219=CARTESIAN_POINT ( 'NONE',  ( -143.8425227516148084, -192.3584106276440480, 44.11586579668791330 ) ) ;
#14221=CARTESIAN_POINT ( 'NONE',  ( -142.0420953463935803, -177.5084106276440536, 46.59394152635518793 ) ) ;
#14237=ADVANCED_FACE ( 'NONE', ( #5880 ), #5668, .T. ) ;
#14239=CARTESIAN_POINT ( 'NONE',  ( -159.5594255724347761, -158.1891397928654612, 55.53486410454104316 ) ) ;
#14255=DIRECTION ( 'NONE',  ( 0.000000000000000000, 0.000000000000000000, 1.000000000000000000 ) ) ;
#14260=CARTESIAN_POINT ( 'NONE',  ( -141.4692556286852891, -192.9891397928654726, 49.65701158161630957 ) ) ;
#14264=CARTESIAN_POINT ( 'NONE',  ( -143.3790856849358306, -156.3630981290893089, 55.53486410454105027 ) ) ;
#14266=AXIS2_PLACEMENT_3D ( 'NONE', #5678, #21116, #2263 ) ;
#14271=CARTESIAN_POINT ( 'NONE',  ( -142.0420953463935803, -189.2438272943107336, 46.59394152635518793 ) ) ;
#14279=CARTESIAN_POINT ( 'NONE',  ( -143.3790856849358306, -169.2891397928654840, 55.53486410454105027 ) ) ;
#14290=CARTESIAN_POINT ( 'NONE',  ( -160.8964159109769696, -172.8938272943107393, 49.65701158161630957 ) ) ;
#14292=CARTESIAN_POINT ( 'NONE',  ( -145.2889157411863721, -183.5130981290892578, 58.16351966513671812 ) ) ;
#14311=ORIENTED_EDGE ( 'NONE', *, *, #11249, .F. ) ;
#14314=VECTOR ( 'NONE', #8214, 1000.000000000000000 ) ;
#14327=EDGE_CURVE ( 'NONE', #21028, #393, #7669, .T. ) ;
#14328=CARTESIAN_POINT ( 'NONE',  ( -151.4692556286852607, -160.7391397928654442, 59.65701158161632378 ) ) ;
#14329=CARTESIAN_POINT ( 'NONE',  ( -159.0959885057557983, -173.1938272943107506, 44.11586579668791330 ) ) ;
#14332=CARTESIAN_POINT ( 'NONE',  ( -154.3824083646099439, -181.5584106276440650, 58.62277379824867296 ) ) ;
#14338=ORIENTED_EDGE ( 'NONE', *, *, #16206, .T. ) ;
#14351=CARTESIAN_POINT ( 'NONE',  ( -157.6495955161842062, -158.9391397928654897, 41.15050349809590102 ) ) ;
#14352=CARTESIAN_POINT ( 'NONE',  ( -151.4692556286852891, -196.9891397928655010, 49.65701158161630957 ) ) ;
#14357=CARTESIAN_POINT ( 'NONE',  ( -160.8964159109769696, -166.7438272943107336, 52.72008163687743121 ) ) ;
#14359=CARTESIAN_POINT ( 'NONE',  ( -154.3824083646099439, -194.7584106276440536, 40.69124936498395328 ) ) ;
#14361=DIRECTION ( 'NONE',  ( -0.000000000000000000, 1.000000000000000000, -0.000000000000000000 ) ) ;
#14374=CARTESIAN_POINT ( 'NONE',  ( -159.5594255724347761, -176.1891397928654612, 55.53486410454104316 ) ) ;
#14375=CARTESIAN_POINT ( 'NONE',  ( -151.4692556286852891, -190.7391397928654726, 60.17163382399899518 ) ) ;
#14377=FACE_OUTER_BOUND ( 'NONE', #3647, .T. ) ;
#14378=CARTESIAN_POINT ( 'NONE',  ( -141.4692556286852891, -159.2130981290892748, 52.90620854394536821 ) ) ;
#14383=CARTESIAN_POINT ( 'NONE',  ( -159.0959885057557983, -193.5938272943107279, 55.19815736654470584 ) ) ;
#14390=EDGE_CURVE ( 'NONE', #14419, #2439, #4127, .T. ) ;
#14402=CARTESIAN_POINT ( 'NONE',  ( -160.8964159109769696, -175.7438272943107052, 52.72008163687743121 ) ) ;
#14404=CARTESIAN_POINT ( 'NONE',  ( -141.4692556286852891, -191.9130981290893203, 46.40781461928724383 ) ) ;
#14419=VERTEX_POINT ( 'NONE', #1250 ) ;
#14420=CARTESIAN_POINT ( 'NONE',  ( -143.3790856849358306, -156.6891397928654612, 43.77915905869157598 ) ) ;
#14437=CARTESIAN_POINT ( 'NONE',  ( -160.8964159109769696, -166.8938272943107393, 49.65701158161630957 ) ) ;
#14438=CARTESIAN_POINT ( 'NONE',  ( -151.4692556286852891, -185.9084106276440025, 39.74470866294723947 ) ) ;
#14440=CARTESIAN_POINT ( 'NONE',  ( -157.2955611005346270, -169.7084106276440139, 57.67623309621198047 ) ) ;
#14442=VERTEX_POINT ( 'NONE', #4774 ) ;
#14446=ORIENTED_EDGE ( 'NONE', *, *, #9404, .T. ) ;
#14447=ORIENTED_EDGE ( 'NONE', *, *, #21316, .F. ) ;
#14456=CARTESIAN_POINT ( 'NONE',  ( -154.5594255724347761, -157.8891397928654783, 59.16757674456785310 ) ) ;
#14461=CARTESIAN_POINT ( 'NONE',  ( -151.4692556286852891, -158.6438272943107108, 39.74470866294723947 ) ) ;
#14467=( BOUNDED_CURVE ( )  B_SPLINE_CURVE ( 2, ( #5929, #12659, #21151, #19380, #4275 ),
 .UNSPECIFIED., .F., .F. ) 
 B_SPLINE_CURVE_WITH_KNOTS ( ( 3, 2, 3 ),
 ( 0.9464285714285713969, 0.9499999999999999556, 0.9523897249335829818 ),
 .UNSPECIFIED. ) 
 CURVE ( )  GEOMETRIC_REPRESENTATION_ITEM ( )  RATIONAL_B_SPLINE_CURVE ( ( 0.9755282581475768211, 0.9755282581475768211, 1.000000000000000000, 0.9836253951315760968, 0.9782074146920120006 ) ) 
 REPRESENTATION_ITEM ( '' )  );
#14477=CARTESIAN_POINT ( 'NONE',  ( -156.4692864601533131, -155.0638355923473455, 40.99677534440144200 ) ) ;
#14480=CARTESIAN_POINT ( 'NONE',  ( -159.5594255724347761, -185.7891397928654840, 43.77915905869157598 ) ) ;
#14483=CARTESIAN_POINT ( 'NONE',  ( -160.8964159109769696, -190.7438272943107336, 52.72008163687743121 ) ) ;
#14491=CARTESIAN_POINT ( 'NONE',  ( -157.2955611005346270, -194.3438272943106995, 41.63779006702063867 ) ) ;
#14505=CARTESIAN_POINT ( 'NONE',  ( -153.0531000319306827, -194.2362167067690564, 39.65701158161629536 ) ) ;
#14510=CARTESIAN_POINT ( 'NONE',  ( -154.3824083646099439, -173.4938272943107336, 40.69124936498395328 ) ) ;
#14512=CARTESIAN_POINT ( 'NONE',  ( -154.5594255724347761, -188.1630981290893203, 40.14644641866476604 ) ) ;
#14527=DIRECTION ( 'NONE',  ( -0.000000000000000000, 1.000000000000000000, -0.000000000000000000 ) ) ;
#14539=CARTESIAN_POINT ( 'NONE',  ( -151.4692556286852891, -189.8130981290892976, 59.65701158161632378 ) ) ;
#14544=CARTESIAN_POINT ( 'NONE',  ( -142.0420953463935803, -171.2438272943107052, 46.59394152635518793 ) ) ;
#14545=CARTESIAN_POINT ( 'NONE',  ( -142.0420953463935803, -180.8084106276440366, 52.72008163687743831 ) ) ;
#14548=CARTESIAN_POINT ( 'NONE',  ( -160.8964159109769696, -167.1584106276440593, 49.65701158161630957 ) ) ;
#14551=DIRECTION ( 'NONE',  ( 0.5000000000000004441, 0.000000000000000000, 0.8660254037844383745 ) ) ;
#14553=EDGE_LOOP ( 'NONE', ( #19386, #7762, #1363, #19537 ) ) ;
#14563=CARTESIAN_POINT ( 'NONE',  ( -143.3790856849358306, -157.2891397928654555, 55.53486410454105027 ) ) ;
#14569=CARTESIAN_POINT ( 'NONE',  ( -145.6429501568359797, -193.1084106276440480, 57.67623309621198047 ) ) ;
#14571=CARTESIAN_POINT ( 'NONE',  ( -145.6429501568359797, -187.1084106276440480, 57.67623309621198047 ) ) ;
#14572=VERTEX_POINT ( 'NONE', #12801 ) ;
#14573=CARTESIAN_POINT ( 'NONE',  ( -159.5594255724347761, -161.7891397928654555, 43.77915905869157598 ) ) ;
#14582=FACE_OUTER_BOUND ( 'NONE', #17322, .T. ) ;
#14587=CARTESIAN_POINT ( 'NONE',  ( -154.5594255724347761, -175.8891397928654783, 59.16757674456785310 ) ) ;
#14588=CARTESIAN_POINT ( 'NONE',  ( -157.6495955161842062, -188.9391397928654612, 41.15050349809590102 ) ) ;
#14592=CARTESIAN_POINT ( 'NONE',  ( -145.6429501568359797, -191.9438272943106938, 41.63779006702063867 ) ) ;
#14597=CARTESIAN_POINT ( 'NONE',  ( -145.6429501568359797, -185.9438272943107506, 41.63779006702063867 ) ) ;
#14601=VERTEX_POINT ( 'NONE', #4861 ) ;
#14610=CYLINDRICAL_SURFACE ( 'NONE', #19674, 10.00000000000000888 ) ;
#14612=EDGE_CURVE ( 'NONE', #3209, #14572, #16394, .T. ) ;
#14616=CARTESIAN_POINT ( 'NONE',  ( -159.0959885057557983, -175.5938272943107279, 55.19815736654470584 ) ) ;
#14618=CARTESIAN_POINT ( 'NONE',  ( -145.2889157411863721, -179.6130981290892805, 41.15050349809590102 ) ) ;
#14640=CARTESIAN_POINT ( 'NONE',  ( -154.3824083646099439, -164.7584106276440536, 40.69124936498395328 ) ) ;
#14653=CARTESIAN_POINT ( 'NONE',  ( -160.8964159109769696, -169.8938272943107393, 49.65701158161630957 ) ) ;
#14654=CARTESIAN_POINT ( 'NONE',  ( -157.2955611005345986, -181.7084106276440423, 57.67623309621197336 ) ) ;
#14657=CARTESIAN_POINT ( 'NONE',  ( -145.6429501568359797, -165.2084106276440423, 41.63779006702063867 ) ) ;
#14662=ORIENTED_EDGE ( 'NONE', *, *, #11740, .T. ) ;
#14675=CARTESIAN_POINT ( 'NONE',  ( -148.3790856849358306, -159.3891397928654783, 40.14644641866477315 ) ) ;
#14681=ORIENTED_EDGE ( 'NONE', *, *, #7908, .T. ) ;
#14683=CARTESIAN_POINT ( 'NONE',  ( -148.5561028927606344, -192.0584106276440650, 40.69124936498395328 ) ) ;
#14685=CARTESIAN_POINT ( 'NONE',  ( -143.8425227516148084, -183.3584106276440480, 44.11586579668791330 ) ) ;
#14686=ORIENTED_EDGE ( 'NONE', *, *, #10598, .F. ) ;
#14695=DIRECTION ( 'NONE',  ( 0.000000000000000000, 0.000000000000000000, -1.000000000000000000 ) ) ;
#14698=EDGE_CURVE ( 'NONE', #12353, #1800, #20922, .T. ) ;
#14701=CARTESIAN_POINT ( 'NONE',  ( -161.4692556286852891, -176.6391397928654783, 46.40781461928724383 ) ) ;
#14702=CARTESIAN_POINT ( 'NONE',  ( -141.4692556286852891, -189.8391397928654953, 46.40781461928724383 ) ) ;
#14707=CARTESIAN_POINT ( 'NONE',  ( -160.8964159109769696, -194.0438272943107165, 46.59394152635518793 ) ) ;
#14712=CARTESIAN_POINT ( 'NONE',  ( -159.0959885057557983, -182.1938272943107506, 44.11586579668791330 ) ) ;
#14730=CARTESIAN_POINT ( 'NONE',  ( -143.8425227516148084, -162.0938272943107279, 44.11586579668791330 ) ) ;
#14732=CARTESIAN_POINT ( 'NONE',  ( -161.4692556286852607, -181.4130981290892919, 52.90620854394536821 ) ) ;
#14739=CARTESIAN_POINT ( 'NONE',  ( -143.8425227516148084, -159.9584106276440423, 55.19815736654470584 ) ) ;
#14752=CARTESIAN_POINT ( 'NONE',  ( -148.5561028927606344, -171.0584106276440366, 40.69124936498395328 ) ) ;
#14753=CARTESIAN_POINT ( 'NONE',  ( -160.8964159109769696, -194.0438272943107165, 46.59394152635518083 ) ) ;
#14754=CARTESIAN_POINT ( 'NONE',  ( -153.0531000319306827, -179.2362167067689995, 39.65701158161629536 ) ) ;
#14756=CARTESIAN_POINT ( 'NONE',  ( -148.3790856849358306, -189.6630981290893203, 59.16757674456786020 ) ) ;
#14762=CARTESIAN_POINT ( 'NONE',  ( -157.2955611005346270, -161.3438272943107563, 41.63779006702063867 ) ) ;
#14763=CARTESIAN_POINT ( 'NONE',  ( -143.8425227516148084, -183.3584106276440480, 44.11586579668791330 ) ) ;
#14765=EDGE_CURVE ( 'NONE', #4022, #8340, #3613, .T. ) ;
#14768=CARTESIAN_POINT ( 'NONE',  ( -143.8425227516148084, -174.3584106276440480, 44.11586579668791330 ) ) ;
#14773=ORIENTED_EDGE ( 'NONE', *, *, #7909, .F. ) ;
#14775=CARTESIAN_POINT ( 'NONE',  ( -148.5561028927606344, -166.2584106276440536, 58.62277379824867296 ) ) ;
#14784=CARTESIAN_POINT ( 'NONE',  ( -141.4692556286852891, -170.9130981290893203, 46.40781461928724383 ) ) ;
#14788=CARTESIAN_POINT ( 'NONE',  ( -151.4692556286852891, -196.9891397928655010, 49.65701158161630957 ) ) ;
#14790=EDGE_LOOP ( 'NONE', ( #21395, #17613, #15457, #1904 ) ) ;
#14792=CARTESIAN_POINT ( 'NONE',  ( -142.0420953463935803, -156.2438272943106767, 46.59394152635518793 ) ) ;
#14794=CARTESIAN_POINT ( 'NONE',  ( -145.6429501568359797, -181.1084106276440195, 57.67623309621198047 ) ) ;
#14797=CARTESIAN_POINT ( 'NONE',  ( -151.4692556286852891, -196.9891397928655010, 59.65701158161632378 ) ) ;
#14809=CARTESIAN_POINT ( 'NONE',  ( -143.3790856849358306, -184.2891397928654840, 55.53486410454105027 ) ) ;
#14811=CARTESIAN_POINT ( 'NONE',  ( -157.2955611005346270, -187.4438272943106938, 57.67623309621198047 ) ) ;
#14815=CARTESIAN_POINT ( 'NONE',  ( -145.6429501568359797, -179.9438272943107506, 41.63779006702063867 ) ) ;
#14830=CARTESIAN_POINT ( 'NONE',  ( -151.4692556286852891, -195.9891397928654726, 49.65701158161630957 ) ) ;
#14831=CARTESIAN_POINT ( 'NONE',  ( -154.3824083646099439, -158.4938272943107052, 40.69124936498395328 ) ) ;
#14832=CARTESIAN_POINT ( 'NONE',  ( -148.3790856849358306, -166.5891397928654669, 59.16757674456786020 ) ) ;
#14833=CARTESIAN_POINT ( 'NONE',  ( -154.5594255724347761, -179.1630981290893203, 40.14644641866476604 ) ) ;
#14834=DIRECTION ( 'NONE',  ( -0.000000000000000000, 1.000000000000000000, -0.000000000000000000 ) ) ;
#14839=CARTESIAN_POINT ( 'NONE',  ( -154.5594255724347761, -181.8891397928654783, 59.16757674456785310 ) ) ;
#14846=CARTESIAN_POINT ( 'NONE',  ( -145.2889157411863437, -187.4391397928654612, 58.16351966513671812 ) ) ;
#14850=CARTESIAN_POINT ( 'NONE',  ( -141.4692556286852891, -168.2130981290892748, 52.90620854394536821 ) ) ;
#14858=CARTESIAN_POINT ( 'NONE',  ( -142.0420953463935803, -171.8084106276440366, 52.72008163687743831 ) ) ;
#14859=CARTESIAN_POINT ( 'NONE',  ( -142.0420953463935803, -195.2438272943107336, 46.59394152635518083 ) ) ;
#14860=CARTESIAN_POINT ( 'NONE',  ( -159.5594255724347761, -166.2630981290893146, 55.53486410454104316 ) ) ;
#14863=EDGE_CURVE ( 'NONE', #10856, #13802, #5824, .T. ) ;
#14867=CARTESIAN_POINT ( 'NONE',  ( -154.5594255724347761, -185.1630981290893203, 40.14644641866476604 ) ) ;
#14871=CARTESIAN_POINT ( 'NONE',  ( -142.0420953463935803, -162.5438272943106881, 52.72008163687743831 ) ) ;
#14872=CARTESIAN_POINT ( 'NONE',  ( -142.0420953463935803, -183.8084106276440082, 52.72008163687743831 ) ) ;
#14875=CARTESIAN_POINT ( 'NONE',  ( -142.0420953463935803, -171.8084106276440366, 52.72008163687743831 ) ) ;
#14881=ORIENTED_EDGE ( 'NONE', *, *, #3444, .F. ) ;
#14882=CARTESIAN_POINT ( 'NONE',  ( -143.3790856849358306, -192.6891397928654897, 43.77915905869157598 ) ) ;
#14898=CARTESIAN_POINT ( 'NONE',  ( -160.8964159109769696, -157.8938272943107393, 49.65701158161630957 ) ) ;
#14900=CARTESIAN_POINT ( 'NONE',  ( -142.0420953463935803, -183.5084106276440252, 46.59394152635518793 ) ) ;
#14903=CARTESIAN_POINT ( 'NONE',  ( -143.3790856849358306, -160.2891397928654555, 55.53486410454105027 ) ) ;
#14910=PLANE ( 'NONE',  #12178 ) ;
#14916=CARTESIAN_POINT ( 'NONE',  ( -143.3790856849358306, -177.6891397928654612, 43.77915905869157598 ) ) ;
#14919=CARTESIAN_POINT ( 'NONE',  ( -148.5561028927606344, -191.7938272943107449, 40.69124936498395328 ) ) ;
#14924=CARTESIAN_POINT ( 'NONE',  ( -157.2955611005346270, -182.3438272943106995, 41.63779006702063867 ) ) ;
#14942=CARTESIAN_POINT ( 'NONE',  ( -154.3824083646099439, -157.2938272943107449, 58.62277379824867296 ) ) ;
#14944=CARTESIAN_POINT ( 'NONE',  ( -143.3790856849358306, -180.3630981290893089, 55.53486410454105027 ) ) ;
#14945=CARTESIAN_POINT ( 'NONE',  ( -157.6495955161842062, -191.9391397928654612, 41.15050349809589392 ) ) ;
#14950=CARTESIAN_POINT ( 'NONE',  ( -157.6495955161842062, -182.9391397928654612, 41.15050349809589392 ) ) ;
#14956=ORIENTED_EDGE ( 'NONE', *, *, #14390, .F. ) ;
#14966=CARTESIAN_POINT ( 'NONE',  ( -143.8425227516148084, -171.9584106276440423, 55.19815736654470584 ) ) ;
#14967=CARTESIAN_POINT ( 'NONE',  ( -157.2955611005345986, -194.3438272943106710, 41.63779006702063867 ) ) ;
#14970=CARTESIAN_POINT ( 'NONE',  ( -141.4692556286852891, -188.9130981290893203, 46.40781461928724383 ) ) ;
#14978=CARTESIAN_POINT ( 'NONE',  ( -151.4692556286852891, -164.6438272943107108, 39.74470866294723947 ) ) ;
#14979=CARTESIAN_POINT ( 'NONE',  ( -160.8964159109769696, -179.0084106276440252, 52.72008163687743121 ) ) ;
#14982=CARTESIAN_POINT ( 'NONE',  ( -148.5561028927606344, -163.2584106276440536, 58.62277379824867296 ) ) ;
#14989=EDGE_LOOP ( 'NONE', ( #14881, #16330, #20960, #10484, #19194 ) ) ;
#15010=CARTESIAN_POINT ( 'NONE',  ( -154.3824083646099439, -190.5584106276440650, 58.62277379824867296 ) ) ;
#15013=CARTESIAN_POINT ( 'NONE',  ( -157.2955611005346270, -187.7084106276440139, 57.67623309621198047 ) ) ;
#15034=CARTESIAN_POINT ( 'NONE',  ( -157.6495955161842062, -176.0391397928654271, 58.16351966513671812 ) ) ;
#15036=CARTESIAN_POINT ( 'NONE',  ( -154.5594255724347761, -195.0891397928654669, 40.14644641866476604 ) ) ;
#15040=CARTESIAN_POINT ( 'NONE',  ( -142.0420953463935803, -186.5438272943107449, 52.72008163687743831 ) ) ;
#15044=ORIENTED_EDGE ( 'NONE', *, *, #21327, .T. ) ;
#15045=EDGE_CURVE ( 'NONE', #6394, #13462, #5845, .T. ) ;
#15055=CARTESIAN_POINT ( 'NONE',  ( -154.5594255724347761, -192.9630981290893317, 59.16757674456785310 ) ) ;
#15060=CARTESIAN_POINT ( 'NONE',  ( -160.8964159109769696, -163.7438272943107336, 52.72008163687743121 ) ) ;
#15062=CARTESIAN_POINT ( 'NONE',  ( -141.4692556286852891, -168.0630981290893260, 49.65701158161630957 ) ) ;
#15069=EDGE_CURVE ( 'NONE', #1800, #6394, #9261, .T. ) ;
#15074=LINE ( 'NONE', #4942, #18125 ) ;
#15077=ORIENTED_EDGE ( 'NONE', *, *, #16609, .T. ) ;
#15085=CARTESIAN_POINT ( 'NONE',  ( -151.4692556286852891, -166.4084106276440878, 59.56931450028537967 ) ) ;
#15086=CARTESIAN_POINT ( 'NONE',  ( -148.5561028927606344, -188.7938272943107449, 40.69124936498395328 ) ) ;
#15090=CARTESIAN_POINT ( 'NONE',  ( -149.8854112254399240, -176.3899795514095672, 39.65701158161629536 ) ) ;
#15096=CARTESIAN_POINT ( 'NONE',  ( -160.8964159109769696, -161.0438272943107449, 46.59394152635518793 ) ) ;
#15097=CARTESIAN_POINT ( 'NONE',  ( -142.0420953463935803, -177.5084106276440536, 46.59394152635518083 ) ) ;
#15100=CARTESIAN_POINT ( 'NONE',  ( -157.2955611005346270, -160.7084106276440423, 57.67623309621198047 ) ) ;
#15107=CARTESIAN_POINT ( 'NONE',  ( -141.4692556286852891, -193.1391397928654783, 52.90620854394536821 ) ) ;
#15116=FACE_OUTER_BOUND ( 'NONE', #14136, .T. ) ;
#15125=CARTESIAN_POINT ( 'NONE',  ( -143.8425227516148084, -183.9584106276440707, 55.19815736654470584 ) ) ;
#15128=CARTESIAN_POINT ( 'NONE',  ( -160.8964159109769696, -179.1584106276440309, 49.65701158161630957 ) ) ;
#15132=CARTESIAN_POINT ( 'NONE',  ( -148.3790856849358306, -159.3891397928654783, 40.14644641866477315 ) ) ;
#15145=CARTESIAN_POINT ( 'NONE',  ( -151.4692556286852891, -177.2391397928654726, 39.14238933923362396 ) ) ;
#15153=CARTESIAN_POINT ( 'NONE',  ( -151.4692556286852891, -178.1438272943106824, 59.56931450028537967 ) ) ;
#15157=ORIENTED_EDGE ( 'NONE', *, *, #21322, .T. ) ;
#15171=CARTESIAN_POINT ( 'NONE',  ( -159.5594255724347761, -169.8630981290893089, 43.77915905869157598 ) ) ;
#15173=CARTESIAN_POINT ( 'NONE',  ( -145.6429501568359797, -162.8438272943106995, 57.67623309621197336 ) ) ;
#15175=CARTESIAN_POINT ( 'NONE',  ( -143.3790856849358306, -168.3630981290893089, 55.53486410454105027 ) ) ;
#15176=( LENGTH_UNIT ( ) NAMED_UNIT ( * ) SI_UNIT ( .MILLI., .METRE. ) );
#15182=CARTESIAN_POINT ( 'NONE',  ( -151.4692556286852607, -168.2391397928654442, 39.65701158161629536 ) ) ;
#15187=PRODUCT ( 'bolt', 'bolt', '', ( #18008 ) ) ;
#15199=CARTESIAN_POINT ( 'NONE',  ( -156.1828684652448658, -155.6591478762521490, 41.49287016839723918 ) ) ;
#15200=CARTESIAN_POINT ( 'NONE',  ( -143.8425227516148084, -195.0938272943107279, 44.11586579668791330 ) ) ;
#15206=DIRECTION ( 'NONE',  ( 0.000000000000000000, -0.000000000000000000, 1.000000000000000000 ) ) ;
#15212=CARTESIAN_POINT ( 'NONE',  ( -151.4692556286852891, -166.1438272943107393, 59.56931450028537967 ) ) ;
#15213=CARTESIAN_POINT ( 'NONE',  ( -145.6429501568359797, -174.2084106276440139, 41.63779006702063867 ) ) ;
#15216=CARTESIAN_POINT ( 'NONE',  ( -143.8425227516148084, -162.3584106276440480, 44.11586579668791330 ) ) ;
#15232=CARTESIAN_POINT ( 'NONE',  ( -151.4692556286852891, -196.9891397928655010, 49.65701158161630957 ) ) ;
#15233=CARTESIAN_POINT ( 'NONE',  ( -143.3790856849358306, -171.3630981290893089, 55.53486410454105027 ) ) ;
#15241=CARTESIAN_POINT ( 'NONE',  ( -142.0420953463935803, -183.5084106276440252, 46.59394152635518793 ) ) ;
#15243=CARTESIAN_POINT ( 'NONE',  ( -142.0420953463935803, -177.8084106276440650, 52.72008163687743831 ) ) ;
#15259=CARTESIAN_POINT ( 'NONE',  ( -151.4692556286852891, -183.2391397928654726, 39.14238933923362396 ) ) ;
#15262=CARTESIAN_POINT ( 'NONE',  ( -151.4692556286853176, -173.3130981290892976, 39.65701158161629536 ) ) ;
#15267=CARTESIAN_POINT ( 'NONE',  ( -148.5561028927606344, -174.9938272943107336, 58.62277379824867296 ) ) ;
#15269=LINE ( 'NONE', #2039, #15357 ) ;
#15274=VECTOR ( 'NONE', #13470, 1000.000000000000000 ) ;
#15275=ADVANCED_FACE ( 'NONE', ( #11047 ), #10849, .F. ) ;
#15279=EDGE_CURVE ( 'NONE', #10182, #11010, #9410, .T. ) ;
#15283=CARTESIAN_POINT ( 'NONE',  ( -157.6495955161842062, -170.0130981290892862, 41.15050349809589392 ) ) ;
#15285=EDGE_CURVE ( 'NONE', #13720, #18280, #954, .T. ) ;
#15288=CARTESIAN_POINT ( 'NONE',  ( -145.2889157411863721, -165.5130981290892862, 58.16351966513671812 ) ) ;
#15303=CARTESIAN_POINT ( 'NONE',  ( -151.4692556286852607, -168.8130981290893260, 59.65701158161632378 ) ) ;
#15310=CARTESIAN_POINT ( 'NONE',  ( -145.6429501568359797, -159.2084106276439854, 41.63779006702063867 ) ) ;
#15311=CARTESIAN_POINT ( 'NONE',  ( -143.8425227516148084, -177.0938272943107279, 44.11586579668791330 ) ) ;
#15313=CARTESIAN_POINT ( 'NONE',  ( -151.4692556286852891, -194.3130981290892976, 39.14238933923362396 ) ) ;
#15321=CARTESIAN_POINT ( 'NONE',  ( -157.6495955161842062, -188.0391397928654555, 58.16351966513671812 ) ) ;
#15322=CARTESIAN_POINT ( 'NONE',  ( -160.8964159109769696, -173.1584106276440593, 49.65701158161630957 ) ) ;
#15324=( BOUNDED_CURVE ( )  B_SPLINE_CURVE ( 2, ( #10779, #524, #17593, #17485, #19259, #14072, #2395, #7584, #20592, #19150, #10460, #14180, #9132 ),
 .UNSPECIFIED., .F., .F. ) 
 B_SPLINE_CURVE_WITH_KNOTS ( ( 3, 2, 2, 2, 2, 2, 3 ),
 ( 0.6964285714285713969, 0.6999999999999999556, 0.7071428571428571841, 0.7142857142857143016, 0.7214285714285714191, 0.7285714285714285365, 0.7321428571428572063 ),
 .UNSPECIFIED. ) 
 CURVE ( )  GEOMETRIC_REPRESENTATION_ITEM ( )  RATIONAL_B_SPLINE_CURVE ( ( 0.9755282581475768211, 0.9755282581475768211, 1.000000000000000000, 0.9510565162951535312, 1.000000000000000000, 0.9510565162951535312, 1.000000000000000000, 0.9510565162951535312, 1.000000000000000000, 0.9510565162951535312, 1.000000000000000000, 0.9755282581475763770, 0.9755282581475768211 ) ) 
 REPRESENTATION_ITEM ( '' )  );
#15325=CARTESIAN_POINT ( 'NONE',  ( -151.4692556286852891, -161.9084106276440593, 39.74470866294723947 ) ) ;
#15328=DIRECTION ( 'NONE',  ( -0.000000000000000000, 1.000000000000000000, -0.000000000000000000 ) ) ;
#15346=CARTESIAN_POINT ( 'NONE',  ( -142.0420953463935803, -180.2438272943107052, 46.59394152635518793 ) ) ;
#15349=CARTESIAN_POINT ( 'NONE',  ( -159.0959885057557983, -181.8584106276440480, 55.19815736654470584 ) ) ;
#15352=CARTESIAN_POINT ( 'NONE',  ( -143.8425227516148084, -180.3584106276440480, 44.11586579668791330 ) ) ;
#15357=VECTOR ( 'NONE', #5546, 1000.000000000000000 ) ;
#15358=DIRECTION ( 'NONE',  ( 0.000000000000000000, -1.000000000000000000, 0.000000000000000000 ) ) ;
#15361=ORIENTED_EDGE ( 'NONE', *, *, #6294, .F. ) ;
#15368=EDGE_CURVE ( 'NONE', #846, #10835, #5655, .T. ) ;
#15372=CARTESIAN_POINT ( 'NONE',  ( -161.4692556286852607, -173.6391397928654214, 46.40781461928724383 ) ) ;
#15374=DIRECTION ( 'NONE',  ( -0.000000000000000000, 1.000000000000000000, -0.000000000000000000 ) ) ;
#15380=CARTESIAN_POINT ( 'NONE',  ( -143.8425227516148084, -177.0938272943107279, 44.11586579668791330 ) ) ;
#15382=CARTESIAN_POINT ( 'NONE',  ( -157.6495955161842062, -170.0391397928654840, 58.16351966513671812 ) ) ;
#15383=CARTESIAN_POINT ( 'NONE',  ( -157.6495955161842062, -158.9391397928654612, 41.15050349809589392 ) ) ;
#15385=CARTESIAN_POINT ( 'NONE',  ( -143.9637021292202235, -116.9891397928655010, 36.65701158161628825 ) ) ;
#15397=CARTESIAN_POINT ( 'NONE',  ( -156.1828684652451784, -155.6591478762521206, 41.49287016839741682 ) ) ;
#15400=CARTESIAN_POINT ( 'NONE',  ( -154.5594255724347761, -168.9630981290893033, 59.16757674456785310 ) ) ;
#15414=VECTOR ( 'NONE', #3904, 1000.000000000000000 ) ;
#15422=CARTESIAN_POINT ( 'NONE',  ( -143.8425227516148084, -162.9584106276440423, 55.19815736654470584 ) ) ;
#15423=CARTESIAN_POINT ( 'NONE',  ( -148.5561028927606344, -180.9938272943107336, 58.62277379824867296 ) ) ;
#15424=CARTESIAN_POINT ( 'NONE',  ( -141.4692556286852891, -177.8391397928654385, 46.40781461928724383 ) ) ;
#15432=CARTESIAN_POINT ( 'NONE',  ( -161.4692556286852891, -188.3391397928654953, 52.90620854394536821 ) ) ;
#15433=CARTESIAN_POINT ( 'NONE',  ( -160.8964159109769696, -173.0084106276440536, 52.72008163687743121 ) ) ;
#15455=CARTESIAN_POINT ( 'NONE',  ( -143.8425227516148084, -180.0938272943107279, 44.11586579668791330 ) ) ;
#15457=ORIENTED_EDGE ( 'NONE', *, *, #14327, .T. ) ;
#15458=CARTESIAN_POINT ( 'NONE',  ( -160.8964159109769696, -185.3084106276440082, 46.59394152635518793 ) ) ;
#15460=CARTESIAN_POINT ( 'NONE',  ( -159.0959885057557983, -178.8584106276440480, 55.19815736654470584 ) ) ;
#15475=EDGE_CURVE ( 'NONE', #3465, #20771, #17870, .T. ) ;
#15476=CARTESIAN_POINT ( 'NONE',  ( -159.5594255724347761, -173.7891397928654840, 43.77915905869157598 ) ) ;
#15482=CARTESIAN_POINT ( 'NONE',  ( -142.0420953463935803, -177.5438272943107165, 52.72008163687743831 ) ) ;
#15485=CARTESIAN_POINT ( 'NONE',  ( -151.4692556286852607, -157.7391397928654726, 59.65701158161632378 ) ) ;
#15491=ORIENTED_EDGE ( 'NONE', *, *, #15045, .T. ) ;
#15496=CARTESIAN_POINT ( 'NONE',  ( -145.2889157411863437, -181.4391397928654612, 58.16351966513671812 ) ) ;
#15499=CARTESIAN_POINT ( 'NONE',  ( -149.8854112254399240, -192.7362167067690564, 59.65701158161632378 ) ) ;
#15503=CARTESIAN_POINT ( 'NONE',  ( -148.3790856849358306, -171.6630981290893203, 59.16757674456786020 ) ) ;
#15517=CARTESIAN_POINT ( 'NONE',  ( -148.3790856849358306, -172.5891397928654669, 59.16757674456786020 ) ) ;
#15521=CARTESIAN_POINT ( 'NONE',  ( -142.0420953463936087, -162.6584106276440593, 49.65701158161630957 ) ) ;
#15522=CARTESIAN_POINT ( 'NONE',  ( -148.5561028927606344, -177.9938272943107336, 58.62277379824867296 ) ) ;
#15531=CARTESIAN_POINT ( 'NONE',  ( -153.0531000319306258, -189.1622583705452030, 39.65701158161629536 ) ) ;
#15532=CARTESIAN_POINT ( 'NONE',  ( -160.8964159109769696, -164.1584106276440593, 49.65701158161630957 ) ) ;
#15538=CARTESIAN_POINT ( 'NONE',  ( -157.6495955161842062, -161.0130981290893146, 41.15050349809589392 ) ) ;
#15539=ORIENTED_EDGE ( 'NONE', *, *, #15475, .T. ) ;
#15541=EDGE_CURVE ( 'NONE', #1664, #19660, #11511, .T. ) ;
#15555=CARTESIAN_POINT ( 'NONE',  ( -151.4692556286852891, -182.6438272943107108, 39.74470866294723947 ) ) ;
#15556=CARTESIAN_POINT ( 'NONE',  ( -143.8425227516148084, -192.9584106276440423, 55.19815736654470584 ) ) ;
#15562=PLANE ( 'NONE',  #17295 ) ;
#15575=CARTESIAN_POINT ( 'NONE',  ( -141.4692556286852891, -165.9891397928654726, 49.65701158161630957 ) ) ;
#15576=CARTESIAN_POINT ( 'NONE',  ( -154.5594255724347761, -180.9630981290893033, 59.16757674456785310 ) ) ;
#15581=CARTESIAN_POINT ( 'NONE',  ( -154.3824083646099439, -175.2938272943107165, 58.62277379824867296 ) ) ;
#15598=CARTESIAN_POINT ( 'NONE',  ( -148.5561028927606344, -155.7938272943107449, 40.69124936498395328 ) ) ;
#15600=CARTESIAN_POINT ( 'NONE',  ( -161.4692556286852607, -157.7130981290893033, 46.40781461928724383 ) ) ;
#15620=CARTESIAN_POINT ( 'NONE',  ( -142.0420953463936087, -159.6584106276440593, 49.65701158161630957 ) ) ;
#15621=CARTESIAN_POINT ( 'NONE',  ( -143.8425227516148084, -180.6938272943107506, 55.19815736654470584 ) ) ;
#15632=CARTESIAN_POINT ( 'NONE',  ( -142.0420953463935803, -168.8084106276440366, 52.72008163687743831 ) ) ;
#15641=EDGE_CURVE ( 'NONE', #10404, #2985, #16329, .T. ) ;
#15653=CARTESIAN_POINT ( 'NONE',  ( -151.4692556286852607, -191.3130981290892976, 39.65701158161629536 ) ) ;
#15656=CARTESIAN_POINT ( 'NONE',  ( -157.2955611005346270, -176.3438272943106710, 41.63779006702063867 ) ) ;
#15657=ADVANCED_FACE ( 'NONE', ( #4657 ), #11372, .T. ) ;
#15659=CARTESIAN_POINT ( 'NONE',  ( -157.2955611005346270, -179.6084106276440764, 41.63779006702063867 ) ) ;
#15663=CARTESIAN_POINT ( 'NONE',  ( -151.4692556286852891, -196.9891397928655010, 49.65701158161630957 ) ) ;
#15670=ADVANCED_FACE ( 'NONE', ( #18436 ), #9957, .T. ) ;
#15678=CARTESIAN_POINT ( 'NONE',  ( -161.4692556286852607, -170.3391397928654953, 52.90620854394536821 ) ) ;
#15682=CARTESIAN_POINT ( 'NONE',  ( -161.4692556286852891, -163.4130981290892635, 52.90620854394536821 ) ) ;
#15685=CARTESIAN_POINT ( 'NONE',  ( -142.0420953463935803, -168.2438272943107336, 46.59394152635518793 ) ) ;
#15690=ORIENTED_EDGE ( 'NONE', *, *, #10597, .T. ) ;
#15702=AXIS2_PLACEMENT_3D ( 'NONE', #5602, #11108, #7495 ) ;
#15705=CARTESIAN_POINT ( 'NONE',  ( -143.3790856849358306, -194.7630981290893146, 43.77915905869157598 ) ) ;
#15710=CARTESIAN_POINT ( 'NONE',  ( -154.5594255724347761, -156.9630981290893317, 59.16757674456785310 ) ) ;
#15718=CARTESIAN_POINT ( 'NONE',  ( -160.8964159109769696, -191.0438272943107449, 46.59394152635518793 ) ) ;
#15720=AXIS2_PLACEMENT_3D ( 'NONE', #17767, #10954, #21100 ) ;
#15729=EDGE_LOOP ( 'NONE', ( #6167, #9534, #12586, #19544 ) ) ;
#15731=CARTESIAN_POINT ( 'NONE',  ( -143.3790856849358306, -171.6891397928654897, 43.77915905869157598 ) ) ;
#15736=CARTESIAN_POINT ( 'NONE',  ( -142.0420953463935803, -177.5438272943107165, 52.72008163687743831 ) ) ;
#15738=CARTESIAN_POINT ( 'NONE',  ( -159.5594255724347761, -190.8630981290893089, 43.77915905869157598 ) ) ;
#15739=LINE ( 'NONE', #7161, #11399 ) ;
#15746=CARTESIAN_POINT ( 'NONE',  ( -157.2955611005345986, -163.7084106276439854, 57.67623309621197336 ) ) ;
#15747=CARTESIAN_POINT ( 'NONE',  ( -151.4692556286852607, -156.8130981290892692, 59.65701158161632378 ) ) ;
#15765=CARTESIAN_POINT ( 'NONE',  ( -161.4692556286852891, -172.7130981290892748, 46.40781461928724383 ) ) ;
#15769=CARTESIAN_POINT ( 'NONE',  ( -160.8964159109769696, -181.8938272943107108, 49.65701158161630957 ) ) ;
#15770=CARTESIAN_POINT ( 'NONE',  ( -145.6429501568359797, -193.1084106276440480, 57.67623309621197336 ) ) ;
#15787=CARTESIAN_POINT ( 'NONE',  ( -145.2889157411863721, -174.5391397928654840, 41.15050349809590102 ) ) ;
#15792=CARTESIAN_POINT ( 'NONE',  ( -145.6429501568359797, -162.8438272943107279, 57.67623309621198047 ) ) ;
#15795=CARTESIAN_POINT ( 'NONE',  ( -145.6429501568359797, -193.1084106276440480, 57.67623309621198047 ) ) ;
#15809=ADVANCED_FACE ( 'NONE', ( #16876 ), #20310, .T. ) ;
#15813=CARTESIAN_POINT ( 'NONE',  ( -151.4692556286852891, -155.3130981290892976, 39.14238933923362396 ) ) ;
#15818=CARTESIAN_POINT ( 'NONE',  ( -143.8425227516148084, -189.6938272943107222, 55.19815736654470584 ) ) ;
#15829=ORIENTED_EDGE ( 'NONE', *, *, #6074, .T. ) ;
#15832=LINE ( 'NONE', #5585, #11585 ) ;
#15836=CARTESIAN_POINT ( 'NONE',  ( -145.6429501568359797, -167.9438272943107222, 41.63779006702063867 ) ) ;
#15838=CARTESIAN_POINT ( 'NONE',  ( -161.4692556286853176, -184.5630981290892976, 49.65701158161630957 ) ) ;
#15846=CARTESIAN_POINT ( 'NONE',  ( -151.4692556286852891, -164.9084106276440593, 39.74470866294723947 ) ) ;
#15852=ORIENTED_EDGE ( 'NONE', *, *, #6294, .T. ) ;
#15856=CARTESIAN_POINT ( 'NONE',  ( -159.5594255724347761, -179.7891397928654840, 43.77915905869157598 ) ) ;
#15865=SURFACE_STYLE_FILL_AREA ( #2315 ) ;
#15869=CARTESIAN_POINT ( 'NONE',  ( -160.8964159109769696, -170.0438272943107449, 46.59394152635518793 ) ) ;
#15870=CARTESIAN_POINT ( 'NONE',  ( -145.6429501568359797, -192.2084106276440139, 41.63779006702063867 ) ) ;
#15872=CARTESIAN_POINT ( 'NONE',  ( -145.6429501568359797, -177.2084106276440423, 41.63779006702063867 ) ) ;
#15881=ORIENTED_EDGE ( 'NONE', *, *, #13466, .T. ) ;
#15889=CARTESIAN_POINT ( 'NONE',  ( -151.4692556286852891, -157.7391397928654442, 60.17163382399899518 ) ) ;
#15896=CARTESIAN_POINT ( 'NONE',  ( -151.4692556286852891, -169.1438272943107108, 59.56931450028537967 ) ) ;
#15898=CARTESIAN_POINT ( 'NONE',  ( -160.8964159109769696, -191.1584106276440593, 49.65701158161630957 ) ) ;
#15899=AXIS2_PLACEMENT_3D ( 'NONE', #14830, #19920, #4697 ) ;
#15901=CARTESIAN_POINT ( 'NONE',  ( -153.0531000319306827, -174.8899795514095672, 59.65701158161631668 ) ) ;
#15907=EDGE_LOOP ( 'NONE', ( #20849, #16836, #4414, #10926 ) ) ;
#15911=ADVANCED_FACE ( 'NONE', ( #7628 ), #19193, .T. ) ;
#15915=CARTESIAN_POINT ( 'NONE',  ( -141.4692556286852891, -192.0630981290892976, 49.65701158161630957 ) ) ;
#15918=CYLINDRICAL_SURFACE ( 'NONE', #1960, 10.00000000000000888 ) ;
#15919=CARTESIAN_POINT ( 'NONE',  ( -148.3790856849358306, -158.4630981290893317, 40.14644641866477315 ) ) ;
#15925=CARTESIAN_POINT ( 'NONE',  ( -160.8964159109769696, -190.7438272943107336, 52.72008163687743121 ) ) ;
#15944=CARTESIAN_POINT ( 'NONE',  ( -143.8425227516148084, -171.6938272943107222, 55.19815736654470584 ) ) ;
#15946=CARTESIAN_POINT ( 'NONE',  ( -154.5594255724347761, -185.1630981290893203, 40.14644641866476604 ) ) ;
#15948=CARTESIAN_POINT ( 'NONE',  ( -145.2889157411863437, -163.4391397928654897, 58.16351966513671812 ) ) ;
#15953=CARTESIAN_POINT ( 'NONE',  ( -143.8425227516148084, -162.3584106276440480, 44.11586579668791330 ) ) ;
#15967=EDGE_CURVE ( 'NONE', #19941, #7201, #10817, .T. ) ;
#15969=CARTESIAN_POINT ( 'NONE',  ( -153.0531000319306827, -167.2362167067690280, 39.65701158161629536 ) ) ;
#15970=CARTESIAN_POINT ( 'NONE',  ( -161.4692556286852891, -157.7130981290893033, 46.40781461928724383 ) ) ;
#15972=DIRECTION ( 'NONE',  ( 0.4999999999999996114, 0.000000000000000000, 0.8660254037844388186 ) ) ;
#15977=CARTESIAN_POINT ( 'NONE',  ( -145.6429501568359797, -167.9438272943107506, 41.63779006702063867 ) ) ;
#15978=CARTESIAN_POINT ( 'NONE',  ( -154.3824083646099439, -191.7584106276440536, 40.69124936498395328 ) ) ;
#15980=CARTESIAN_POINT ( 'NONE',  ( -154.3824083646099439, -176.7584106276440536, 40.69124936498395328 ) ) ;
#15997=CARTESIAN_POINT ( 'NONE',  ( -159.5594255724347761, -161.1891397928654897, 55.53486410454104316 ) ) ;
#15998=DIRECTION ( 'NONE',  ( 0.000000000000000000, 0.000000000000000000, 1.000000000000000000 ) ) ;
#16001=CARTESIAN_POINT ( 'NONE',  ( -153.0531000319307111, -162.8899795514095672, 59.65701158161632378 ) ) ;
#16005=FACE_OUTER_BOUND ( 'NONE', #764, .T. ) ;
#16014=ORIENTED_EDGE ( 'NONE', *, *, #5010, .F. ) ;
#16020=CARTESIAN_POINT ( 'NONE',  ( -157.6495955161842062, -176.9391397928654612, 41.15050349809589392 ) ) ;
#16021=CARTESIAN_POINT ( 'NONE',  ( -157.6495955161842062, -194.0391397928654271, 58.16351966513671812 ) ) ;
#16023=CARTESIAN_POINT ( 'NONE',  ( -151.4692556286852891, -186.2391397928655010, 39.65701158161630246 ) ) ;
#16024=CARTESIAN_POINT ( 'NONE',  ( -161.4692556286852607, -160.7130981290892748, 46.40781461928724383 ) ) ;
#16039=ORIENTED_EDGE ( 'NONE', *, *, #11740, .F. ) ;
#16050=CARTESIAN_POINT ( 'NONE',  ( -148.5561028927606344, -168.9938272943107336, 58.62277379824867296 ) ) ;
#16052=CARTESIAN_POINT ( 'NONE',  ( -141.4692556286852891, -185.9130981290892919, 46.40781461928724383 ) ) ;
#16059=CARTESIAN_POINT ( 'NONE',  ( -151.4692556286853176, -174.8130981290893260, 59.65701158161632378 ) ) ;
#16068=CARTESIAN_POINT ( 'NONE',  ( -149.8854112254399240, -157.6622583705452030, 59.65701158161632378 ) ) ;
#16089=CARTESIAN_POINT ( 'NONE',  ( -145.6429501568359797, -174.8438272943107279, 57.67623309621198047 ) ) ;
#16090=CARTESIAN_POINT ( 'NONE',  ( -151.4692556286852891, -181.4084106276440025, 59.56931450028537256 ) ) ;
#16092=CARTESIAN_POINT ( 'NONE',  ( -142.0420953463936087, -171.6584106276440593, 49.65701158161630957 ) ) ;
#16112=COLOUR_RGB ( '', 0.09019608, 0.27058824, 0.51372549) ;
#16115=CARTESIAN_POINT ( 'NONE',  ( -161.4692556286852607, -161.6391397928654783, 46.40781461928724383 ) ) ;
#16116=CARTESIAN_POINT ( 'NONE',  ( -141.4692556286852891, -159.0630981290892976, 49.65701158161630957 ) ) ;
#16118=CARTESIAN_POINT ( 'NONE',  ( -153.0531000319306258, -184.8160212151856854, 59.65701158161632378 ) ) ;
#16121=CARTESIAN_POINT ( 'NONE',  ( -143.8425227516148084, -159.6938272943107222, 55.19815736654470584 ) ) ;
#16131=FACE_OUTER_BOUND ( 'NONE', #1245, .T. ) ;
#16137=CARTESIAN_POINT ( 'NONE',  ( -151.4692556286852891, -186.2391397928654726, 39.14238933923362396 ) ) ;
#16140=CARTESIAN_POINT ( 'NONE',  ( -142.0420953463936087, -192.3938272943107393, 49.65701158161630957 ) ) ;
#16156=VECTOR ( 'NONE', #13432, 1000.000000000000000 ) ;
#16162=CARTESIAN_POINT ( 'NONE',  ( -145.6429501568359797, -168.8438272943107563, 57.67623309621197336 ) ) ;
#16164=CARTESIAN_POINT ( 'NONE',  ( -151.4692556286852891, -189.8130981290892692, 60.17163382399899518 ) ) ;
#16176=CARTESIAN_POINT ( 'NONE',  ( -148.3790856849358306, -186.3891397928654783, 40.14644641866477315 ) ) ;
#16180=ORIENTED_EDGE ( 'NONE', *, *, #14765, .T. ) ;
#16195=CARTESIAN_POINT ( 'NONE',  ( -145.6429501568359797, -173.9438272943106938, 41.63779006702063867 ) ) ;
#16196=CARTESIAN_POINT ( 'NONE',  ( -143.8425227516148084, -186.3584106276440480, 44.11586579668791330 ) ) ;
#16199=CARTESIAN_POINT ( 'NONE',  ( -160.8964159109769696, -170.1584106276440593, 49.65701158161630957 ) ) ;
#16205=VERTEX_POINT ( 'NONE', #11542 ) ;
#16206=EDGE_CURVE ( 'NONE', #21208, #4150, #4751, .T. ) ;
#16219=CARTESIAN_POINT ( 'NONE',  ( -145.2889157411863721, -157.4391397928654612, 58.16351966513671812 ) ) ;
#16224=CARTESIAN_POINT ( 'NONE',  ( -148.5561028927606344, -195.0584106276440650, 40.69124936498395328 ) ) ;
#16226=CARTESIAN_POINT ( 'NONE',  ( -157.2955611005346270, -188.6084106276440764, 41.63779006702063867 ) ) ;
#16227=ORIENTED_EDGE ( 'NONE', *, *, #12414, .T. ) ;
#16234=VERTEX_POINT ( 'NONE', #1520 ) ;
#16243=CARTESIAN_POINT ( 'NONE',  ( -161.4692556286853176, -176.4891397928654442, 49.65701158161630957 ) ) ;
#16244=CARTESIAN_POINT ( 'NONE',  ( -154.5594255724347761, -184.8891397928654783, 59.16757674456785310 ) ) ;
#16247=CARTESIAN_POINT ( 'NONE',  ( -159.0959885057557983, -190.5938272943107279, 55.19815736654470584 ) ) ;
#16253=CARTESIAN_POINT ( 'NONE',  ( -157.2955611005346270, -187.4438272943106938, 57.67623309621198047 ) ) ;
#16256=ORIENTED_EDGE ( 'NONE', *, *, #21756, .F. ) ;
#16264=ORIENTED_EDGE ( 'NONE', *, *, #18272, .T. ) ;
#16265=ORIENTED_EDGE ( 'NONE', *, *, #6546, .F. ) ;
#16273=CARTESIAN_POINT ( 'NONE',  ( -159.0959885057557983, -172.5938272943107279, 55.19815736654470584 ) ) ;
#16275=CARTESIAN_POINT ( 'NONE',  ( -154.5594255724347761, -176.1630981290893203, 40.14644641866476604 ) ) ;
#16282=CARTESIAN_POINT ( 'NONE',  ( -151.4692556286852891, -157.4084106276440593, 59.56931450028537256 ) ) ;
#16286=CARTESIAN_POINT ( 'NONE',  ( -149.8854112254399240, -187.6622583705452030, 59.65701158161632378 ) ) ;
#16295=CARTESIAN_POINT ( 'NONE',  ( -142.0420953463936087, -165.6584106276440593, 49.65701158161630957 ) ) ;
#16300=CARTESIAN_POINT ( 'NONE',  ( -159.5594255724347761, -190.2630981290893146, 55.53486410454104316 ) ) ;
#16304=CARTESIAN_POINT ( 'NONE',  ( -143.8425227516148084, -174.0938272943107279, 44.11586579668791330 ) ) ;
#16305=CARTESIAN_POINT ( 'NONE',  ( -143.8425227516148084, -183.9584106276440707, 55.19815736654470584 ) ) ;
#16308=CARTESIAN_POINT ( 'NONE',  ( -154.3824083646099439, -167.7584106276440536, 40.69124936498395328 ) ) ;
#16325=CARTESIAN_POINT ( 'NONE',  ( -148.3790856849358306, -160.5891397928654953, 59.16757674456786020 ) ) ;
#16329=LINE ( 'NONE', #13036, #13793 ) ;
#16330=ORIENTED_EDGE ( 'NONE', *, *, #10163, .T. ) ;
#16332=CARTESIAN_POINT ( 'NONE',  ( -142.0420953463935803, -192.5084106276439968, 46.59394152635518793 ) ) ;
#16335=CARTESIAN_POINT ( 'NONE',  ( -151.4692556286852891, -182.9084106276440025, 39.74470866294723947 ) ) ;
#16336=ORIENTED_EDGE ( 'NONE', *, *, #15069, .F. ) ;
#16351=CARTESIAN_POINT ( 'NONE',  ( -154.5594255724347761, -192.0891397928654953, 40.14644641866476604 ) ) ;
#16354=CARTESIAN_POINT ( 'NONE',  ( -145.6429501568359797, -188.9438272943106938, 41.63779006702063867 ) ) ;
#16359=CARTESIAN_POINT ( 'NONE',  ( -145.6429501568359797, -180.8438272943106995, 57.67623309621198047 ) ) ;
#16371=DIRECTION ( 'NONE',  ( 0.000000000000000000, 0.000000000000000000, 1.000000000000000000 ) ) ;
#16376=CARTESIAN_POINT ( 'NONE',  ( -154.3824083646099439, -166.2938272943107165, 58.62277379824867296 ) ) ;
#16378=CARTESIAN_POINT ( 'NONE',  ( -159.5594255724347761, -181.2630981290893146, 55.53486410454104316 ) ) ;
#16379=CYLINDRICAL_SURFACE ( 'NONE', #3691, 10.00000000000000888 ) ;
#16394=( BOUNDED_CURVE ( )  B_SPLINE_CURVE ( 2, ( #5298, #12009, #6642, #13461, #18745, #15107, #11, #9832, #14882, #10161, #13352, #21628, #16861 ),
 .UNSPECIFIED., .F., .F. ) 
 B_SPLINE_CURVE_WITH_KNOTS ( ( 3, 2, 2, 2, 2, 2, 3 ),
 ( 0.05357142857142854764, 0.05714285714285714107, 0.06428571428571427937, 0.07142857142857142461, 0.07857142857142856984, 0.08571428571428571508, 0.08928571428571421831 ),
 .UNSPECIFIED. ) 
 CURVE ( )  GEOMETRIC_REPRESENTATION_ITEM ( )  RATIONAL_B_SPLINE_CURVE ( ( 0.9755282581475765991, 0.9755282581475765991, 1.000000000000000000, 0.9510565162951535312, 1.000000000000000000, 0.9510565162951535312, 1.000000000000000000, 0.9510565162951535312, 1.000000000000000000, 0.9510565162951535312, 1.000000000000000000, 0.9755282581475772652, 0.9755282581475768211 ) ) 
 REPRESENTATION_ITEM ( '' )  );
#16402=CARTESIAN_POINT ( 'NONE',  ( -145.6429501568359797, -171.2084106276440707, 41.63779006702063867 ) ) ;
#16403=CARTESIAN_POINT ( 'NONE',  ( -159.0959885057557983, -188.1938272943107222, 44.11586579668791330 ) ) ;
#16413=CARTESIAN_POINT ( 'NONE',  ( -148.5561028927606344, -162.9938272943107336, 58.62277379824867296 ) ) ;
#16414=CARTESIAN_POINT ( 'NONE',  ( -142.0420953463935803, -186.8084106276440650, 52.72008163687743831 ) ) ;
#16417=CARTESIAN_POINT ( 'NONE',  ( -151.4692556286852891, -172.4084106276440309, 59.56931450028537967 ) ) ;
#16422=ORIENTED_EDGE ( 'NONE', *, *, #6462, .F. ) ;
#16431=DIRECTION ( 'NONE',  ( 0.000000000000000000, 0.000000000000000000, 1.000000000000000000 ) ) ;
#16433=CARTESIAN_POINT ( 'NONE',  ( -151.4692556286852891, -196.9891397928655010, 39.65701158161630246 ) ) ;
#16438=ORIENTED_EDGE ( 'NONE', *, *, #15279, .F. ) ;
#16440=CARTESIAN_POINT ( 'NONE',  ( -142.0420953463936087, -195.6584106276440593, 49.65701158161630957 ) ) ;
#16442=CARTESIAN_POINT ( 'NONE',  ( -157.2955611005346270, -182.6084106276440480, 41.63779006702063867 ) ) ;
#16444=CARTESIAN_POINT ( 'NONE',  ( -153.0531000319306827, -162.1622583705451461, 39.65701158161629536 ) ) ;
#16450=ORIENTED_EDGE ( 'NONE', *, *, #15541, .F. ) ;
#16458=CARTESIAN_POINT ( 'NONE',  ( -161.4692556286852607, -191.3391397928654669, 52.90620854394536821 ) ) ;
#16460=DIRECTION ( 'NONE',  ( 0.000000000000000000, 0.000000000000000000, 1.000000000000000000 ) ) ;
#16461=CARTESIAN_POINT ( 'NONE',  ( -143.8425227516148084, -192.0938272943107279, 44.11586579668791330 ) ) ;
#16466=CARTESIAN_POINT ( 'NONE',  ( -157.2955611005346270, -181.4438272943107506, 57.67623309621198047 ) ) ;
#16483=CARTESIAN_POINT ( 'NONE',  ( -145.6429501568359797, -158.9438272943107222, 41.63779006702063867 ) ) ;
#16485=CARTESIAN_POINT ( 'NONE',  ( -141.4692556286852891, -174.0630981290893260, 49.65701158161630957 ) ) ;
#16501=ORIENTED_EDGE ( 'NONE', *, *, #11961, .T. ) ;
#16508=CARTESIAN_POINT ( 'NONE',  ( -159.0959885057557983, -164.4584106276440423, 44.11586579668791330 ) ) ;
#16509=CARTESIAN_POINT ( 'NONE',  ( -142.0420953463936087, -189.3938272943107393, 49.65701158161630957 ) ) ;
#16510=CARTESIAN_POINT ( 'NONE',  ( -153.0531000319306827, -165.8899795514095672, 59.65701158161631668 ) ) ;
#16511=LINE ( 'NONE', #6498, #2332 ) ;
#16513=CARTESIAN_POINT ( 'NONE',  ( -141.4692556286852891, -175.1391397928654783, 52.90620854394536821 ) ) ;
#16519=CARTESIAN_POINT ( 'NONE',  ( -159.0959885057557983, -161.1938272943107222, 44.11586579668791330 ) ) ;
#16520=CARTESIAN_POINT ( 'NONE',  ( -151.4692556286852891, -187.4084106276440309, 59.56931450028537256 ) ) ;
#16523=CARTESIAN_POINT ( 'NONE',  ( -143.8425227516148084, -168.3584106276440480, 44.11586579668791330 ) ) ;
#16528=( BOUNDED_CURVE ( )  B_SPLINE_CURVE ( 2, ( #15182, #1297, #8031, #13421, #21586, #1407, #16604, #6597, #1626, #6252, #12982, #6714, #8359 ),
 .UNSPECIFIED., .F., .F. ) 
 B_SPLINE_CURVE_WITH_KNOTS ( ( 3, 2, 2, 2, 2, 2, 3 ),
 ( 0.6607142857142856984, 0.6642857142857142572, 0.6714285714285713746, 0.6785714285714286031, 0.6857142857142857206, 0.6928571428571428381, 0.6964285714285713969 ),
 .UNSPECIFIED. ) 
 CURVE ( )  GEOMETRIC_REPRESENTATION_ITEM ( )  RATIONAL_B_SPLINE_CURVE ( ( 0.9755282581475768211, 0.9755282581475768211, 1.000000000000000000, 0.9510565162951535312, 1.000000000000000000, 0.9510565162951535312, 1.000000000000000000, 0.9510565162951535312, 1.000000000000000000, 0.9510565162951535312, 1.000000000000000000, 0.9755282581475768211, 0.9755282581475768211 ) ) 
 REPRESENTATION_ITEM ( '' )  );
#16549=CARTESIAN_POINT ( 'NONE',  ( -142.0420953463935803, -156.5438272943107165, 52.72008163687743831 ) ) ;
#16552=CARTESIAN_POINT ( 'NONE',  ( -154.3824083646099439, -187.5584106276440650, 58.62277379824867296 ) ) ;
#16566=CARTESIAN_POINT ( 'NONE',  ( -143.3790856849358306, -178.2891397928654840, 55.53486410454105027 ) ) ;
#16569=CARTESIAN_POINT ( 'NONE',  ( -154.3824083646099439, -188.4938272943107336, 40.69124936498395328 ) ) ;
#16574=CARTESIAN_POINT ( 'NONE',  ( -142.0420953463936087, -186.3938272943107393, 49.65701158161630957 ) ) ;
#16593=CARTESIAN_POINT ( 'NONE',  ( -160.8964159109769696, -157.7438272943107336, 52.72008163687743121 ) ) ;
#16595=CARTESIAN_POINT ( 'NONE',  ( -145.2889157411863721, -182.6130981290893374, 41.15050349809590102 ) ) ;
#16597=DIRECTION ( 'NONE',  ( -0.000000000000000000, 1.000000000000000000, -0.000000000000000000 ) ) ;
#16598=EDGE_CURVE ( 'NONE', #9959, #8850, #12934, .T. ) ;
#16604=CARTESIAN_POINT ( 'NONE',  ( -161.4692556286853176, -167.4891397928654726, 49.65701158161630957 ) ) ;
#16605=AXIS2_PLACEMENT_3D ( 'NONE', #6980, #3556, #136 ) ;
#16609=EDGE_CURVE ( 'NONE', #16234, #8233, #4017, .T. ) ;
#16614=ORIENTED_EDGE ( 'NONE', *, *, #2767, .T. ) ;
#16616=ORIENTED_EDGE ( 'NONE', *, *, #3264, .F. ) ;
#16624=CARTESIAN_POINT ( 'NONE',  ( -160.8964159109769696, -167.3084106276440366, 46.59394152635518793 ) ) ;
#16625=CARTESIAN_POINT ( 'NONE',  ( -157.2955611005345986, -187.4438272943106938, 57.67623309621197336 ) ) ;
#16627=CARTESIAN_POINT ( 'NONE',  ( -151.4692556286852607, -166.7391397928654442, 59.65701158161632378 ) ) ;
#16635=CARTESIAN_POINT ( 'NONE',  ( -142.0420953463935803, -159.5438272943107449, 52.72008163687743831 ) ) ;
#16636=CARTESIAN_POINT ( 'NONE',  ( -154.3824083646099439, -172.5584106276440366, 58.62277379824867296 ) ) ;
#16640=CARTESIAN_POINT ( 'NONE',  ( -151.4692556286852891, -157.4084106276440593, 59.56931450028537967 ) ) ;
#16654=CARTESIAN_POINT ( 'NONE',  ( -151.4692556286852607, -162.2391397928654442, 39.65701158161629536 ) ) ;
#16656=CARTESIAN_POINT ( 'NONE',  ( -145.2889157411863437, -171.5130981290893146, 58.16351966513671812 ) ) ;
#16664=CARTESIAN_POINT ( 'NONE',  ( -160.8964159109769696, -188.0084106276440252, 52.72008163687743121 ) ) ;
#16666=CARTESIAN_POINT ( 'NONE',  ( -160.8964159109769696, -185.3084106276440082, 46.59394152635518793 ) ) ;
#16672=VERTEX_POINT ( 'NONE', #2147 ) ;
#16683=CARTESIAN_POINT ( 'NONE',  ( -161.4692556286852607, -176.6391397928654783, 46.40781461928724383 ) ) ;
#16690=CARTESIAN_POINT ( 'NONE',  ( -151.4692556286852891, -184.1438272943107108, 59.56931450028537967 ) ) ;
#16692=ADVANCED_FACE ( 'NONE', ( #19539 ), #17989, .T. ) ;
#16695=CARTESIAN_POINT ( 'NONE',  ( -148.3790856849358306, -190.5891397928654953, 59.16757674456786020 ) ) ;
#16708=CARTESIAN_POINT ( 'NONE',  ( -143.8425227516148084, -165.0938272943107279, 44.11586579668791330 ) ) ;
#16710=CARTESIAN_POINT ( 'NONE',  ( -161.4692556286853176, -178.5630981290893260, 49.65701158161630957 ) ) ;
#16725=CARTESIAN_POINT ( 'NONE',  ( -142.0420953463936087, -195.6584106276440593, 49.65701158161630957 ) ) ;
#16733=CARTESIAN_POINT ( 'NONE',  ( -159.0959885057557983, -169.8584106276440764, 55.19815736654470584 ) ) ;
#16734=CARTESIAN_POINT ( 'NONE',  ( -142.0420953463936087, -195.3938272943107393, 49.65701158161630957 ) ) ;
#16735=CARTESIAN_POINT ( 'NONE',  ( -159.5594255724347761, -178.8630981290893089, 43.77915905869157598 ) ) ;
#16737=CARTESIAN_POINT ( 'NONE',  ( -149.8854112254399524, -189.7362167067690280, 59.65701158161632378 ) ) ;
#16744=CIRCLE ( 'NONE', #14266, 10.00000000000000888 ) ;
#16745=CARTESIAN_POINT ( 'NONE',  ( -160.8964159109769696, -164.0438272943107449, 46.59394152635518793 ) ) ;
#16746=CARTESIAN_POINT ( 'NONE',  ( -154.3824083646099439, -176.7584106276440536, 40.69124936498395328 ) ) ;
#16749=CARTESIAN_POINT ( 'NONE',  ( -159.0959885057557983, -160.8584106276440480, 55.19815736654470584 ) ) ;
#16759=CIRCLE ( 'NONE', #15702, 9.000000000000007105 ) ;
#16764=EDGE_CURVE ( 'NONE', #9830, #7201, #12348, .T. ) ;
#16766=CARTESIAN_POINT ( 'NONE',  ( -151.4692556286852891, -183.2391397928654726, 39.65701158161629536 ) ) ;
#16775=CARTESIAN_POINT ( 'NONE',  ( -160.8964159109769696, -191.0084106276440821, 52.72008163687743121 ) ) ;
#16778=CARTESIAN_POINT ( 'NONE',  ( -145.6429501568359797, -180.2084106276440707, 41.63779006702063867 ) ) ;
#16779=ORIENTED_EDGE ( 'NONE', *, *, #14765, .F. ) ;
#16794=CARTESIAN_POINT ( 'NONE',  ( -143.3790856849358306, -175.2891397928654840, 55.53486410454105027 ) ) ;
#16796=CARTESIAN_POINT ( 'NONE',  ( -151.4692556286853176, -193.7391397928655010, 59.65701158161632378 ) ) ;
#16800=CARTESIAN_POINT ( 'NONE',  ( -154.3824083646099439, -172.2938272943107165, 58.62277379824867296 ) ) ;
#16817=CARTESIAN_POINT ( 'NONE',  ( -151.4692556286852607, -170.3130981290892692, 39.65701158161629536 ) ) ;
#16818=CARTESIAN_POINT ( 'NONE',  ( -157.2955611005345986, -164.3438272943107279, 41.63779006702063867 ) ) ;
#16820=CARTESIAN_POINT ( 'NONE',  ( -148.3790856849358306, -170.4630981290893033, 40.14644641866477315 ) ) ;
#16832=CARTESIAN_POINT ( 'NONE',  ( -143.3790856849358306, -186.3630981290893089, 55.53486410454105027 ) ) ;
#16836=ORIENTED_EDGE ( 'NONE', *, *, #3797, .F. ) ;
#16842=CARTESIAN_POINT ( 'NONE',  ( -145.6429501568359797, -157.1084106276440480, 57.67623309621198047 ) ) ;
#16843=CARTESIAN_POINT ( 'NONE',  ( -151.4692556286852891, -190.1438272943107393, 59.56931450028537256 ) ) ;
#16850=CARTESIAN_POINT ( 'NONE',  ( -143.8425227516148084, -159.0938272943107279, 44.11586579668791330 ) ) ;
#16851=CARTESIAN_POINT ( 'NONE',  ( -154.3824083646099439, -170.7584106276440536, 40.69124936498395328 ) ) ;
#16855=CARTESIAN_POINT ( 'NONE',  ( -145.6429501568359797, -163.1084106276440195, 57.67623309621198047 ) ) ;
#16860=ORIENTED_EDGE ( 'NONE', *, *, #5917, .T. ) ;
#16861=CARTESIAN_POINT ( 'NONE',  ( -151.4692556286852607, -192.2391397928655010, 39.65701158161629536 ) ) ;
#16872=CARTESIAN_POINT ( 'NONE',  ( -148.3790856849358306, -171.6630981290893203, 59.16757674456786020 ) ) ;
#16873=CARTESIAN_POINT ( 'NONE',  ( -155.5590455049452316, -156.0406172220664303, 40.47124262348441448 ) ) ;
#16876=FACE_OUTER_BOUND ( 'NONE', #3210, .T. ) ;
#16880=CARTESIAN_POINT ( 'NONE',  ( -160.8964159109769696, -182.3084106276440650, 46.59394152635518793 ) ) ;
#16882=CARTESIAN_POINT ( 'NONE',  ( -157.2955611005346270, -178.7084106276440139, 57.67623309621198047 ) ) ;
#16887=EDGE_CURVE ( 'NONE', #1525, #4150, #11823, .T. ) ;
#16894=EDGE_CURVE ( 'NONE', #5724, #16672, #11381, .T. ) ;
#16901=CARTESIAN_POINT ( 'NONE',  ( -141.4692556286852891, -184.1391397928654783, 52.90620854394536821 ) ) ;
#16903=LINE ( 'NONE', #8550, #12516 ) ;
#16909=CARTESIAN_POINT ( 'NONE',  ( -148.5561028927606344, -171.9938272943107336, 58.62277379824867296 ) ) ;
#16911=CARTESIAN_POINT ( 'NONE',  ( -151.4692556286852891, -195.2391397928655010, 39.65701158161629536 ) ) ;
#16922=DIRECTION ( 'NONE',  ( 0.000000000000000000, 0.000000000000000000, 1.000000000000000000 ) ) ;
#16927=CARTESIAN_POINT ( 'NONE',  ( -161.4692556286852607, -166.7130981290893317, 46.40781461928724383 ) ) ;
#16936=LINE ( 'NONE', #18387, #6164 ) ;
#16939=DIRECTION ( 'NONE',  ( -0.000000000000000000, -1.000000000000000000, -0.000000000000000000 ) ) ;
#16945=CARTESIAN_POINT ( 'NONE',  ( -160.8964159109769696, -161.3084106276440082, 46.59394152635518793 ) ) ;
#16947=CARTESIAN_POINT ( 'NONE',  ( -145.6429501568359797, -179.9438272943107506, 41.63779006702063867 ) ) ;
#16949=CARTESIAN_POINT ( 'NONE',  ( -145.2889157411863721, -194.6130981290892805, 41.15050349809590102 ) ) ;
#16960=CARTESIAN_POINT ( 'NONE',  ( -143.8425227516148084, -177.3584106276440480, 44.11586579668791330 ) ) ;
#16962=CARTESIAN_POINT ( 'NONE',  ( -145.6429501568359797, -160.1084106276440480, 57.67623309621198047 ) ) ;
#16979=CARTESIAN_POINT ( 'NONE',  ( -153.0531000319306543, -191.2362167067690280, 39.65701158161628825 ) ) ;
#16980=( BOUNDED_CURVE ( )  B_SPLINE_CURVE ( 2, ( #15653, #16979, #14106, #5204, #18649, #3551, #1889, #7837, #16300, #17518, #2429, #11231, #14539 ),
 .UNSPECIFIED., .F., .T. ) 
 B_SPLINE_CURVE_WITH_KNOTS ( ( 3, 2, 2, 2, 2, 2, 3 ),
 ( 0.08928571428571425994, 0.09285714285714286031, 0.1000000000000000056, 0.1071428571428571369, 0.1142857142857142821, 0.1214285714285714274, 0.1249999999999999584 ),
 .UNSPECIFIED. ) 
 CURVE ( )  GEOMETRIC_REPRESENTATION_ITEM ( )  RATIONAL_B_SPLINE_CURVE ( ( 0.9755282581475768211, 0.9755282581475765991, 1.000000000000000000, 0.9510565162951535312, 1.000000000000000000, 0.9510565162951535312, 1.000000000000000000, 0.9510565162951535312, 1.000000000000000000, 0.9510565162951535312, 1.000000000000000000, 0.9755282581475770431, 0.9755282581475768211 ) ) 
 REPRESENTATION_ITEM ( '' )  );
#16988=CARTESIAN_POINT ( 'NONE',  ( -148.5561028927606344, -190.2584106276440536, 58.62277379824867296 ) ) ;
#16990=CARTESIAN_POINT ( 'NONE',  ( -160.8964159109769696, -173.1584106276440593, 49.65701158161630957 ) ) ;
#17007=CARTESIAN_POINT ( 'NONE',  ( -141.4692556286852891, -180.8391397928654669, 46.40781461928724383 ) ) ;
#17015=CARTESIAN_POINT ( 'NONE',  ( -160.8964159109769696, -173.0438272943107449, 46.59394152635518793 ) ) ;
#17035=CARTESIAN_POINT ( 'NONE',  ( -148.3790856849358306, -164.4630981290893317, 40.14644641866477315 ) ) ;
#17045=CARTESIAN_POINT ( 'NONE',  ( -141.4692556286852891, -186.0630981290892976, 49.65701158161630957 ) ) ;
#17056=CARTESIAN_POINT ( 'NONE',  ( -142.0420953463935803, -159.8084106276440934, 52.72008163687743831 ) ) ;
#17057=CARTESIAN_POINT ( 'NONE',  ( -148.5561028927606344, -183.9938272943107336, 58.62277379824867296 ) ) ;
#17058=CARTESIAN_POINT ( 'NONE',  ( -145.2889157411863437, -178.4391397928654044, 58.16351966513671812 ) ) ;
#17059=CARTESIAN_POINT ( 'NONE',  ( -161.4692556286852607, -193.7130981290893317, 46.40781461928724383 ) ) ;
#17060=CARTESIAN_POINT ( 'NONE',  ( -151.4692556286853176, -163.7391397928654726, 59.65701158161632378 ) ) ;
#17061=CARTESIAN_POINT ( 'NONE',  ( -154.5594255724347761, -172.8891397928654783, 59.16757674456785310 ) ) ;
#17066=CARTESIAN_POINT ( 'NONE',  ( -161.4692556286852891, -188.6391397928654783, 46.40781461928724383 ) ) ;
#17067=CARTESIAN_POINT ( 'NONE',  ( -154.3824083646099439, -175.5584106276440366, 58.62277379824867296 ) ) ;
#17091=CARTESIAN_POINT ( 'NONE',  ( -151.4692556286852891, -181.1438272943107393, 59.56931450028537967 ) ) ;
#17094=CARTESIAN_POINT ( 'NONE',  ( -148.5561028927606344, -189.0584106276440650, 40.69124936498395328 ) ) ;
#17096=CARTESIAN_POINT ( 'NONE',  ( -159.0959885057557983, -175.8584106276440480, 55.19815736654470584 ) ) ;
#17099=DIRECTION ( 'NONE',  ( 0.8660254037844388186, 0.000000000000000000, -0.4999999999999996114 ) ) ;
#17113=CARTESIAN_POINT ( 'NONE',  ( -148.3790856849358306, -166.5891397928654669, 59.16757674456786020 ) ) ;
#17123=CARTESIAN_POINT ( 'NONE',  ( -143.8425227516148084, -171.6938272943107222, 55.19815736654470584 ) ) ;
#17126=CARTESIAN_POINT ( 'NONE',  ( -159.5594255724347761, -158.7891397928654555, 43.77915905869157598 ) ) ;
#17128=CARTESIAN_POINT ( 'NONE',  ( -145.2889157411863437, -189.5391397928653987, 41.15050349809589392 ) ) ;
#17136=DIRECTION ( 'NONE',  ( -0.000000000000000000, 1.000000000000000000, -0.000000000000000000 ) ) ;
#17138=CARTESIAN_POINT ( 'NONE',  ( -142.0420953463936087, -195.5261189609773851, 49.65701158161630957 ) ) ;
#17141=CARTESIAN_POINT ( 'NONE',  ( -141.4692556286852891, -173.9130981290893203, 46.40781461928724383 ) ) ;
#17143=CARTESIAN_POINT ( 'NONE',  ( -159.5594255724347761, -166.8630981290893089, 43.77915905869157598 ) ) ;
#17160=CARTESIAN_POINT ( 'NONE',  ( -136.4581486297550441, -116.9891397928655010, 49.65701158161631668 ) ) ;
#17165=CARTESIAN_POINT ( 'NONE',  ( -143.8425227516148084, -162.3584106276440480, 44.11586579668791330 ) ) ;
#17166=CARTESIAN_POINT ( 'NONE',  ( -148.5561028927606344, -185.7938272943107449, 40.69124936498395328 ) ) ;
#17168=CARTESIAN_POINT ( 'NONE',  ( -154.5594255724347761, -192.9630981290893317, 59.16757674456785310 ) ) ;
#17169=DIRECTION ( 'NONE',  ( 1.000000000000000000, 0.000000000000000000, 0.000000000000000000 ) ) ;
#17177=CARTESIAN_POINT ( 'NONE',  ( -154.3824083646099439, -166.5584106276440366, 58.62277379824867296 ) ) ;
#17184=EDGE_LOOP ( 'NONE', ( #4795, #16501, #8951, #3013 ) ) ;
#17198=CARTESIAN_POINT ( 'NONE',  ( -157.2955611005346270, -178.4438272943107222, 57.67623309621198047 ) ) ;
#17209=EDGE_LOOP ( 'NONE', ( #10264, #1361, #18425, #2254, #3594, #12473 ) ) ;
#17210=CARTESIAN_POINT ( 'NONE',  ( -151.4692556286852607, -191.3130981290892976, 39.65701158161629536 ) ) ;
#17217=CARTESIAN_POINT ( 'NONE',  ( -145.2889157411863721, -169.4391397928654044, 58.16351966513671812 ) ) ;
#17218=CARTESIAN_POINT ( 'NONE',  ( -151.4692556286852891, -188.3130981290893260, 39.65701158161630246 ) ) ;
#17225=CARTESIAN_POINT ( 'NONE',  ( -159.0959885057557983, -178.5938272943107279, 55.19815736654470584 ) ) ;
#17241=CARTESIAN_POINT ( 'NONE',  ( -141.4692556286852891, -180.9891397928654726, 49.65701158161630957 ) ) ;
#17244=CARTESIAN_POINT ( 'NONE',  ( -151.4692556286852607, -191.3130981290892976, 39.65701158161629536 ) ) ;
#17247=CARTESIAN_POINT ( 'NONE',  ( -151.4692556286852607, -171.8130981290892976, 59.65701158161632378 ) ) ;
#17248=CARTESIAN_POINT ( 'NONE',  ( -141.4692556286852891, -171.0630981290893260, 49.65701158161630957 ) ) ;
#17255=ORIENTED_EDGE ( 'NONE', *, *, #20635, .F. ) ;
#17256=AXIS2_PLACEMENT_3D ( 'NONE', #20852, #5742, #7522 ) ;
#17265=DIRECTION ( 'NONE',  ( -0.5000000000000004441, 0.000000000000000000, -0.8660254037844383745 ) ) ;
#17270=CARTESIAN_POINT ( 'NONE',  ( -151.4692556286852891, -160.4084106276440593, 59.56931450028537967 ) ) ;
#17271=CARTESIAN_POINT ( 'NONE',  ( -143.8425227516148084, -177.6938272943107506, 55.19815736654470584 ) ) ;
#17282=CARTESIAN_POINT ( 'NONE',  ( -159.0959885057557983, -166.8584106276440480, 55.19815736654470584 ) ) ;
#17286=ADVANCED_FACE ( 'NONE', ( #5522 ), #18983, .F. ) ;
#17295=AXIS2_PLACEMENT_3D ( 'NONE', #7091, #10185, #249 ) ;
#17303=CARTESIAN_POINT ( 'NONE',  ( -153.0531000319306827, -171.8899795514095672, 59.65701158161631668 ) ) ;
#17307=CARTESIAN_POINT ( 'NONE',  ( -154.3824083646099439, -176.4938272943107336, 40.69124936498395328 ) ) ;
#17308=CARTESIAN_POINT ( 'NONE',  ( -159.0959885057557983, -193.8584106276440480, 55.19815736654470584 ) ) ;
#17310=CARTESIAN_POINT ( 'NONE',  ( -142.0420953463935803, -177.8084106276440650, 52.72008163687743831 ) ) ;
#17322=EDGE_LOOP ( 'NONE', ( #15829, #5772, #5557 ) ) ;
#17324=CYLINDRICAL_SURFACE ( 'NONE', #21444, 10.00000000000000888 ) ;
#17326=EDGE_CURVE ( 'NONE', #12850, #20510, #10964, .T. ) ;
#17332=CARTESIAN_POINT ( 'NONE',  ( -151.4692556286852891, -166.7391397928654442, 60.17163382399899518 ) ) ;
#17338=CARTESIAN_POINT ( 'NONE',  ( -157.2955611005346270, -160.4438272943106654, 57.67623309621198047 ) ) ;
#17341=CARTESIAN_POINT ( 'NONE',  ( -148.5561028927606344, -195.0584106276440650, 40.69124936498395328 ) ) ;
#17342=ORIENTED_EDGE ( 'NONE', *, *, #11249, .T. ) ;
#17347=CARTESIAN_POINT ( 'NONE',  ( -151.4692556286852891, -196.9891397928655010, 59.65701158161632378 ) ) ;
#17357=CARTESIAN_POINT ( 'NONE',  ( -149.8854112254399240, -174.7362167067690280, 59.65701158161632378 ) ) ;
#17358=CARTESIAN_POINT ( 'NONE',  ( -151.4692556286852891, -196.9891397928655010, 49.65701158161630957 ) ) ;
#17359=CARTESIAN_POINT ( 'NONE',  ( -145.2889157411863721, -159.5130981290892578, 58.16351966513671812 ) ) ;
#17364=CARTESIAN_POINT ( 'NONE',  ( -142.0420953463935803, -192.5438272943107449, 52.72008163687743831 ) ) ;
#17366=ORIENTED_EDGE ( 'NONE', *, *, #3797, .T. ) ;
#17375=CARTESIAN_POINT ( 'NONE',  ( -141.4692556286852891, -171.9891397928654726, 49.65701158161630957 ) ) ;
#17379=ADVANCED_FACE ( 'NONE', ( #8636 ), #15562, .F. ) ;
#17380=CARTESIAN_POINT ( 'NONE',  ( -151.4692556286852891, -179.6438272943107108, 39.74470866294723947 ) ) ;
#17382=CARTESIAN_POINT ( 'NONE',  ( -141.4692556286852891, -192.2130981290892748, 52.90620854394536821 ) ) ;
#17391=CARTESIAN_POINT ( 'NONE',  ( -154.5594255724347761, -189.0891397928654953, 40.14644641866476604 ) ) ;
#17392=CARTESIAN_POINT ( 'NONE',  ( -142.0420953463936087, -165.6584106276440593, 49.65701158161630957 ) ) ;
#17410=CARTESIAN_POINT ( 'NONE',  ( -151.4692556286852891, -196.9891397928655010, 39.65701158161630246 ) ) ;
#17411=CARTESIAN_POINT ( 'NONE',  ( -157.6495955161842062, -172.1130981290892805, 58.16351966513671812 ) ) ;
#17415=CARTESIAN_POINT ( 'NONE',  ( -157.2955611005346270, -184.4438272943107506, 57.67623309621198047 ) ) ;
#17416=CARTESIAN_POINT ( 'NONE',  ( -151.4692556286852891, -191.9084106276440309, 39.74470866294723947 ) ) ;
#17418=CARTESIAN_POINT ( 'NONE',  ( -159.0959885057557983, -175.8584106276440480, 55.19815736654470584 ) ) ;
#17420=CARTESIAN_POINT ( 'NONE',  ( -151.4692556286852891, -182.3130981290892976, 39.65701158161629536 ) ) ;
#17435=CARTESIAN_POINT ( 'NONE',  ( -159.5594255724347761, -170.7891397928654840, 43.77915905869157598 ) ) ;
#17438=CARTESIAN_POINT ( 'NONE',  ( -161.4692556286853176, -163.5630981290893260, 49.65701158161630957 ) ) ;
#17441=CARTESIAN_POINT ( 'NONE',  ( -143.8425227516148084, -168.0938272943107563, 44.11586579668791330 ) ) ;
#17452=EDGE_LOOP ( 'NONE', ( #2551, #19766, #20400, #9780 ) ) ;
#17465=CARTESIAN_POINT ( 'NONE',  ( -143.3790856849358306, -155.7630981290893146, 43.77915905869157598 ) ) ;
#17479=AXIS2_PLACEMENT_3D ( 'NONE', #6810, #11861, #8568 ) ;
#17485=CARTESIAN_POINT ( 'NONE',  ( -145.2889157411863437, -165.5130981290892862, 58.16351966513671812 ) ) ;
#17490=CARTESIAN_POINT ( 'NONE',  ( -157.2955611005345986, -170.3438272943107563, 41.63779006702063867 ) ) ;
#17492=CARTESIAN_POINT ( 'NONE',  ( -161.4692556286852607, -190.4130981290892919, 52.90620854394536821 ) ) ;
#17498=CARTESIAN_POINT ( 'NONE',  ( -159.0959885057557983, -164.4584106276440423, 44.11586579668791330 ) ) ;
#17499=CARTESIAN_POINT ( 'NONE',  ( -157.6495955161842062, -164.0391397928654555, 58.16351966513671812 ) ) ;
#17507=CARTESIAN_POINT ( 'NONE',  ( -151.4692556286852607, -159.8130981290892692, 59.65701158161632378 ) ) ;
#17518=CARTESIAN_POINT ( 'NONE',  ( -157.6495955161842062, -190.1130981290892805, 58.16351966513671812 ) ) ;
#17522=CARTESIAN_POINT ( 'NONE',  ( -148.5561028927606344, -177.9938272943107336, 58.62277379824867296 ) ) ;
#17524=CARTESIAN_POINT ( 'NONE',  ( -142.0420953463935803, -174.5084106276440252, 46.59394152635518793 ) ) ;
#17542=CARTESIAN_POINT ( 'NONE',  ( -157.6495955161842062, -161.0391397928654840, 58.16351966513671812 ) ) ;
#17543=CARTESIAN_POINT ( 'NONE',  ( -151.4692556286852607, -158.3130981290892692, 39.65701158161629536 ) ) ;
#17548=CARTESIAN_POINT ( 'NONE',  ( -159.0959885057557983, -160.5938272943107279, 55.19815736654470584 ) ) ;
#17551=CARTESIAN_POINT ( 'NONE',  ( -143.8425227516148084, -192.9584106276440423, 55.19815736654470584 ) ) ;
#17556=( BOUNDED_CURVE ( )  B_SPLINE_CURVE ( 1, ( #15397, #3188 ),
 .UNSPECIFIED., .F., .F. ) 
 B_SPLINE_CURVE_WITH_KNOTS ( ( 2, 2 ),
 ( 0.000000000000000000, 1.000000000000000000 ),
 .UNSPECIFIED. ) 
 CURVE ( )  GEOMETRIC_REPRESENTATION_ITEM ( )  RATIONAL_B_SPLINE_CURVE ( ( 0.9782074146920101132, 0.9782074146920101132 ) ) 
 REPRESENTATION_ITEM ( '' )  );
#17562=ORIENTED_EDGE ( 'NONE', *, *, #11962, .F. ) ;
#17573=CARTESIAN_POINT ( 'NONE',  ( -142.0420953463936087, -195.3938272943107393, 49.65701158161630957 ) ) ;
#17579=FACE_OUTER_BOUND ( 'NONE', #9306, .T. ) ;
#17589=ORIENTED_EDGE ( 'NONE', *, *, #12708, .T. ) ;
#17590=EDGE_CURVE ( 'NONE', #18280, #5724, #4068, .T. ) ;
#17593=CARTESIAN_POINT ( 'NONE',  ( -148.3790856849358306, -165.6630981290892919, 59.16757674456786020 ) ) ;
#17597=CARTESIAN_POINT ( 'NONE',  ( -154.3824083646099439, -175.2938272943107165, 58.62277379824867296 ) ) ;
#17599=CARTESIAN_POINT ( 'NONE',  ( -159.5594255724347761, -187.8630981290893089, 43.77915905869157598 ) ) ;
#17607=CARTESIAN_POINT ( 'NONE',  ( -151.4692556286852891, -167.9084106276440309, 39.74470866294723947 ) ) ;
#17613=ORIENTED_EDGE ( 'NONE', *, *, #9214, .T. ) ;
#17618=ADVANCED_FACE ( 'NONE', ( #5716, #653 ), #7390, .F. ) ;
#17625=CARTESIAN_POINT ( 'NONE',  ( -151.4692556286852607, -167.3130981290893260, 39.65701158161629536 ) ) ;
#17626=CARTESIAN_POINT ( 'NONE',  ( -153.0531000319306827, -158.2362167067690280, 39.65701158161629536 ) ) ;
#17631=CARTESIAN_POINT ( 'NONE',  ( -142.0420953463935803, -171.5438272943106881, 52.72008163687743831 ) ) ;
#17632=CARTESIAN_POINT ( 'NONE',  ( -148.5561028927606344, -193.2584106276440252, 58.62277379824867296 ) ) ;
#17634=CARTESIAN_POINT ( 'NONE',  ( -160.8964159109769696, -179.0084106276440252, 52.72008163687743121 ) ) ;
#17653=CARTESIAN_POINT ( 'NONE',  ( -161.4692556286852607, -158.3391397928654385, 52.90620854394536821 ) ) ;
#17654=CARTESIAN_POINT ( 'NONE',  ( -145.2889157411863437, -159.5130981290892862, 58.16351966513671812 ) ) ;
#17660=CARTESIAN_POINT ( 'NONE',  ( -145.6429501568359797, -161.9438272943107222, 41.63779006702063867 ) ) ;
#17662=CARTESIAN_POINT ( 'NONE',  ( -148.5561028927606344, -193.2584106276440252, 58.62277379824867296 ) ) ;
#17678=CARTESIAN_POINT ( 'NONE',  ( -161.4692556286852607, -191.6391397928654214, 46.40781461928724383 ) ) ;
#17680=CARTESIAN_POINT ( 'NONE',  ( -151.4692556286852607, -159.8130981290892692, 59.65701158161632378 ) ) ;
#17681=CARTESIAN_POINT ( 'NONE',  ( -141.4692556286852891, -162.2130981290893033, 52.90620854394536821 ) ) ;
#17687=CARTESIAN_POINT ( 'NONE',  ( -143.8425227516148084, -192.0938272943107279, 44.11586579668791330 ) ) ;
#17703=CARTESIAN_POINT ( 'NONE',  ( -151.4692556286852891, -167.6438272943106824, 39.74470866294723947 ) ) ;
#17705=CARTESIAN_POINT ( 'NONE',  ( -157.6495955161842062, -190.1130981290892805, 58.16351966513671812 ) ) ;
#17712=CARTESIAN_POINT ( 'NONE',  ( -142.0420953463935803, -159.8084106276440650, 52.72008163687743831 ) ) ;
#17713=CARTESIAN_POINT ( 'NONE',  ( -151.4692556286853176, -165.2391397928654442, 39.65701158161629536 ) ) ;
#17730=CARTESIAN_POINT ( 'NONE',  ( -161.4692556286853176, -187.5630981290892976, 49.65701158161630957 ) ) ;
#17736=CARTESIAN_POINT ( 'NONE',  ( -157.2955611005346270, -167.3438272943106995, 41.63779006702063867 ) ) ;
#17737=CARTESIAN_POINT ( 'NONE',  ( -142.0420953463936087, -183.6584106276440309, 49.65701158161630957 ) ) ;
#17740=CARTESIAN_POINT ( 'NONE',  ( -160.8964159109769696, -173.3084106276440366, 46.59394152635518793 ) ) ;
#17759=CARTESIAN_POINT ( 'NONE',  ( -145.2889157411863721, -162.5391397928654271, 41.15050349809590102 ) ) ;
#17760=CARTESIAN_POINT ( 'NONE',  ( -148.3790856849358306, -158.4630981290893317, 40.14644641866477315 ) ) ;
#17765=CARTESIAN_POINT ( 'NONE',  ( -151.4692556286852891, -163.1438272943106824, 59.56931450028537967 ) ) ;
#17767=CARTESIAN_POINT ( 'NONE',  ( -156.3976848494337162, -155.9071947501682018, 41.12080071780688684 ) ) ;
#17782=CARTESIAN_POINT ( 'NONE',  ( -148.3790856849358306, -186.3891397928654783, 40.14644641866477315 ) ) ;
#17786=CARTESIAN_POINT ( 'NONE',  ( -145.2889157411863721, -158.6130981290893089, 41.15050349809590102 ) ) ;
#17791=CARTESIAN_POINT ( 'NONE',  ( -142.0420953463935803, -192.2438272943107336, 46.59394152635518793 ) ) ;
#17809=( BOUNDED_CURVE ( )  B_SPLINE_CURVE ( 2, ( #12051, #20335, #158, #3794, #5539, #11839, #5433, #1916, #3685, #13496, #15576, #8651, #10523 ),
 .UNSPECIFIED., .F., .F. ) 
 B_SPLINE_CURVE_WITH_KNOTS ( ( 3, 2, 2, 2, 2, 2, 3 ),
 ( 0.3035714285714286031, 0.3071428571428571619, 0.3142857142857142794, 0.3214285714285714524, 0.3285714285714285698, 0.3357142857142856873, 0.3392857142857142461 ),
 .UNSPECIFIED. ) 
 CURVE ( )  GEOMETRIC_REPRESENTATION_ITEM ( )  RATIONAL_B_SPLINE_CURVE ( ( 0.9755282581475768211, 0.9755282581475769321, 1.000000000000000000, 0.9510565162951535312, 1.000000000000000000, 0.9510565162951535312, 1.000000000000000000, 0.9510565162951535312, 1.000000000000000000, 0.9510565162951535312, 1.000000000000000000, 0.9755282581475769321, 0.9755282581475768211 ) ) 
 REPRESENTATION_ITEM ( '' )  );
#17810=CARTESIAN_POINT ( 'NONE',  ( -148.5561028927606344, -174.9938272943107336, 58.62277379824867296 ) ) ;
#17812=CARTESIAN_POINT ( 'NONE',  ( -145.2889157411863721, -192.5130981290892862, 58.16351966513671812 ) ) ;
#17820=CARTESIAN_POINT ( 'NONE',  ( -160.8964159109769696, -158.0084106276439968, 52.72008163687743121 ) ) ;
#17840=CARTESIAN_POINT ( 'NONE',  ( -151.4692556286852607, -158.3130981290892692, 39.65701158161629536 ) ) ;
#17843=CARTESIAN_POINT ( 'NONE',  ( -161.4692556286852891, -187.7130981290893033, 46.40781461928724383 ) ) ;
#17847=CARTESIAN_POINT ( 'NONE',  ( -154.3824083646099439, -170.4938272943107336, 40.69124936498395328 ) ) ;
#17848=CARTESIAN_POINT ( 'NONE',  ( -143.8425227516148084, -180.9584106276440707, 55.19815736654470584 ) ) ;
#17851=CARTESIAN_POINT ( 'NONE',  ( -160.8964159109769696, -167.0084106276440536, 52.72008163687743121 ) ) ;
#17857=ORIENTED_EDGE ( 'NONE', *, *, #827, .F. ) ;
#17859=ORIENTED_EDGE ( 'NONE', *, *, #21582, .F. ) ;
#17865=MECHANICAL_DESIGN_GEOMETRIC_PRESENTATION_REPRESENTATION('',(#6635),#9130);
#17868=CARTESIAN_POINT ( 'NONE',  ( -159.5594255724347761, -164.1891397928654897, 55.53486410454104316 ) ) ;
#17870=LINE ( 'NONE', #6534, #2525 ) ;
#17871=EDGE_LOOP ( 'NONE', ( #11048, #4919 ) ) ;
#17873=CARTESIAN_POINT ( 'NONE',  ( -145.6429501568359797, -159.8438272943107563, 57.67623309621198047 ) ) ;
#17875=CARTESIAN_POINT ( 'NONE',  ( -145.6429501568359797, -186.2084106276440707, 41.63779006702063867 ) ) ;
#17880=ORIENTED_EDGE ( 'NONE', *, *, #12654, .F. ) ;
#17884=LINE ( 'NONE', #20543, #12548 ) ;
#17890=CARTESIAN_POINT ( 'NONE',  ( -154.5594255724347761, -177.0891397928654669, 40.14644641866476604 ) ) ;
#17891=CARTESIAN_POINT ( 'NONE',  ( -159.5594255724347761, -185.1891397928654612, 55.53486410454104316 ) ) ;
#17894=CARTESIAN_POINT ( 'NONE',  ( -142.0420953463935803, -186.2438272943107620, 46.59394152635518793 ) ) ;
#17899=CARTESIAN_POINT ( 'NONE',  ( -160.8964159109769696, -185.0438272943107165, 46.59394152635518793 ) ) ;
#17912=DIRECTION ( 'NONE',  ( -0.000000000000000000, 1.000000000000000000, -0.000000000000000000 ) ) ;
#17917=EDGE_CURVE ( 'NONE', #13462, #9830, #14467, .T. ) ;
#17918=CARTESIAN_POINT ( 'NONE',  ( -154.3824083646099439, -167.4938272943107336, 40.69124936498395328 ) ) ;
#17920=CARTESIAN_POINT ( 'NONE',  ( -141.4692556286852891, -176.9130981290892635, 46.40781461928724383 ) ) ;
#17936=( BOUNDED_CURVE ( )  B_SPLINE_CURVE ( 2, ( #17713, #20935, #12658, #20717, #3965, #5928, #4376, #7278, #866, #17499, #19379, #652, #12327 ),
 .UNSPECIFIED., .F., .F. ) 
 B_SPLINE_CURVE_WITH_KNOTS ( ( 3, 2, 2, 2, 2, 2, 3 ),
 ( 0.7321428571428572063, 0.7357142857142857650, 0.7428571428571428825, 0.7500000000000000000, 0.7571428571428571175, 0.7642857142857142350, 0.7678571428571427937 ),
 .UNSPECIFIED. ) 
 CURVE ( )  GEOMETRIC_REPRESENTATION_ITEM ( )  RATIONAL_B_SPLINE_CURVE ( ( 0.9755282581475768211, 0.9755282581475771542, 1.000000000000000000, 0.9510565162951535312, 1.000000000000000000, 0.9510565162951535312, 1.000000000000000000, 0.9510565162951535312, 1.000000000000000000, 0.9510565162951535312, 1.000000000000000000, 0.9755282581475771542, 0.9755282581475768211 ) ) 
 REPRESENTATION_ITEM ( '' )  );
#17945=CARTESIAN_POINT ( 'NONE',  ( -154.3824083646099439, -172.5584106276440366, 58.62277379824867296 ) ) ;
#17948=CARTESIAN_POINT ( 'NONE',  ( -154.5594255724347761, -158.1630981290892919, 40.14644641866476604 ) ) ;
#17957=CARTESIAN_POINT ( 'NONE',  ( -145.6429501568359797, -170.9438272943107222, 41.63779006702063867 ) ) ;
#17958=CARTESIAN_POINT ( 'NONE',  ( -142.0420953463935803, -180.5084106276440536, 46.59394152635518083 ) ) ;
#17961=CARTESIAN_POINT ( 'NONE',  ( -142.0420953463935803, -165.8084106276440366, 52.72008163687743831 ) ) ;
#17968=ORIENTED_EDGE ( 'NONE', *, *, #9359, .T. ) ;
#17969=VERTEX_POINT ( 'NONE', #20015 ) ;
#17977=CARTESIAN_POINT ( 'NONE',  ( -145.2889157411863721, -163.4391397928654897, 58.16351966513671812 ) ) ;
#17984=CARTESIAN_POINT ( 'NONE',  ( -151.4692556286852891, -193.4084106276440593, 59.56931450028537967 ) ) ;
#17986=CARTESIAN_POINT ( 'NONE',  ( -148.5561028927606344, -187.2584106276440536, 58.62277379824867296 ) ) ;
#17989=CYLINDRICAL_SURFACE ( 'NONE', #6035, 10.00000000000000888 ) ;
#17992=ADVANCED_FACE ( 'NONE', ( #3249 ), #1484, .T. ) ;
#18000=AXIS2_PLACEMENT_3D ( 'NONE', #3669, #17099, #10610 ) ;
#18004=CARTESIAN_POINT ( 'NONE',  ( -151.4692556286852891, -192.2391397928654726, 39.14238933923362396 ) ) ;
#18005=DIRECTION ( 'NONE',  ( -0.000000000000000000, 1.000000000000000000, -0.000000000000000000 ) ) ;
#18007=CARTESIAN_POINT ( 'NONE',  ( -142.0420953463935803, -192.5438272943107449, 52.72008163687743831 ) ) ;
#18008=PRODUCT_CONTEXT ( 'NONE', #1833, 'mechanical' ) ;
#18009=AXIS2_PLACEMENT_3D ( 'NONE', #18802, #3707, #10222 ) ;
#18013=CARTESIAN_POINT ( 'NONE',  ( -143.8425227516148084, -186.0938272943107279, 44.11586579668791330 ) ) ;
#18015=CARTESIAN_POINT ( 'NONE',  ( -151.4692556286852891, -178.7391397928654726, 59.65701158161631668 ) ) ;
#18023=VECTOR ( 'NONE', #14527, 1000.000000000000000 ) ;
#18028=CARTESIAN_POINT ( 'NONE',  ( -151.4692556286852891, -177.8130981290892976, 59.65701158161631668 ) ) ;
#18032=CARTESIAN_POINT ( 'NONE',  ( -142.0420953463936087, -156.6584106276440593, 49.65701158161630957 ) ) ;
#18033=CARTESIAN_POINT ( 'NONE',  ( -151.4692556286852891, -164.6438272943107108, 39.74470866294723947 ) ) ;
#18034=CARTESIAN_POINT ( 'NONE',  ( -149.8854112254399809, -165.3160212151857138, 39.65701158161628825 ) ) ;
#18035=CARTESIAN_POINT ( 'NONE',  ( -161.4692556286852607, -175.7130981290893317, 46.40781461928724383 ) ) ;
#18041=CARTESIAN_POINT ( 'NONE',  ( -148.5561028927606344, -156.0584106276440650, 40.69124936498395328 ) ) ;
#18045=CARTESIAN_POINT ( 'NONE',  ( -143.3790856849358306, -187.2891397928654555, 55.53486410454105027 ) ) ;
#18054=DIRECTION ( 'NONE',  ( 0.000000000000000000, 0.000000000000000000, -1.000000000000000000 ) ) ;
#18055=CARTESIAN_POINT ( 'NONE',  ( -148.5561028927606344, -163.2584106276440536, 58.62277379824867296 ) ) ;
#18058=CARTESIAN_POINT ( 'NONE',  ( -153.0531000319306543, -177.8899795514095388, 59.65701158161632378 ) ) ;
#18061=CARTESIAN_POINT ( 'NONE',  ( -151.4692556286852891, -176.3130981290892976, 39.65701158161629536 ) ) ;
#18067=CARTESIAN_POINT ( 'NONE',  ( -142.0420953463935803, -168.5438272943107165, 52.72008163687743831 ) ) ;
#18068=CARTESIAN_POINT ( 'NONE',  ( -157.2955611005345986, -184.7084106276440423, 57.67623309621197336 ) ) ;
#18071=CARTESIAN_POINT ( 'NONE',  ( -151.4692556286852891, -170.9084106276440593, 39.74470866294723947 ) ) ;
#18076=( BOUNDED_CURVE ( )  B_SPLINE_CURVE ( 2, ( #18840, #15531, #17391, #3746, #10257, #17066, #10578, #15432, #9035, #15321, #18952, #10476, #5491 ),
 .UNSPECIFIED., .F., .F. ) 
 B_SPLINE_CURVE_WITH_KNOTS ( ( 3, 2, 2, 2, 2, 2, 3 ),
 ( 0.1607142857142856707, 0.1642857142857142849, 0.1714285714285714302, 0.1785714285714285754, 0.1857142857142857206, 0.1928571428571428659, 0.1964285714285714524 ),
 .UNSPECIFIED. ) 
 CURVE ( )  GEOMETRIC_REPRESENTATION_ITEM ( )  RATIONAL_B_SPLINE_CURVE ( ( 0.9755282581475765991, 0.9755282581475763770, 1.000000000000000000, 0.9510565162951535312, 1.000000000000000000, 0.9510565162951535312, 1.000000000000000000, 0.9510565162951535312, 1.000000000000000000, 0.9510565162951535312, 1.000000000000000000, 0.9755282581475765991, 0.9755282581475767101 ) ) 
 REPRESENTATION_ITEM ( '' )  );
#18096=CARTESIAN_POINT ( 'NONE',  ( -157.2955611005346270, -191.6084106276440764, 41.63779006702063867 ) ) ;
#18098=CARTESIAN_POINT ( 'NONE',  ( -154.3824083646099439, -181.5584106276440650, 58.62277379824867296 ) ) ;
#18100=CARTESIAN_POINT ( 'NONE',  ( -151.4692556286852891, -196.9891397928655010, 49.65701158161630957 ) ) ;
#18114=CARTESIAN_POINT ( 'NONE',  ( -141.4692556286852891, -192.8391397928654669, 46.40781461928724383 ) ) ;
#18116=CARTESIAN_POINT ( 'NONE',  ( -151.4692556286852891, -196.9891397928655010, 49.65701158161630957 ) ) ;
#18117=CARTESIAN_POINT ( 'NONE',  ( -145.6429501568359797, -189.8438272943106995, 57.67623309621198047 ) ) ;
#18122=CARTESIAN_POINT ( 'NONE',  ( -157.2955611005346270, -179.3438272943107279, 41.63779006702063867 ) ) ;
#18125=VECTOR ( 'NONE', #10235, 1000.000000000000000 ) ;
#18136=CARTESIAN_POINT ( 'NONE',  ( -151.4692556286852891, -176.3130981290892976, 39.65701158161629536 ) ) ;
#18141=CARTESIAN_POINT ( 'NONE',  ( -142.0420953463936087, -159.3938272943107393, 49.65701158161630957 ) ) ;
#18143=CARTESIAN_POINT ( 'NONE',  ( -143.3790856849358306, -174.3630981290893089, 55.53486410454105027 ) ) ;
#18150=DIRECTION ( 'NONE',  ( -0.000000000000000000, 1.000000000000000000, -0.000000000000000000 ) ) ;
#18151=CARTESIAN_POINT ( 'NONE',  ( -145.6429501568359797, -157.1084106276440480, 57.67623309621197336 ) ) ;
#18153=CARTESIAN_POINT ( 'NONE',  ( -136.4581486297550441, -116.9891397928655010, 49.65701158161631668 ) ) ;
#18159=DIRECTION ( 'NONE',  ( -0.5000000000000004441, 0.000000000000000000, -0.8660254037844383745 ) ) ;
#18167=CARTESIAN_POINT ( 'NONE',  ( -148.5561028927606344, -165.0584106276440366, 40.69124936498395328 ) ) ;
#18168=ADVANCED_FACE ( 'NONE', ( #20122 ), #11723, .T. ) ;
#18169=CARTESIAN_POINT ( 'NONE',  ( -154.3824083646099439, -190.2938272943107449, 58.62277379824867296 ) ) ;
#18174=CARTESIAN_POINT ( 'NONE',  ( -145.2889157411863437, -175.4391397928654328, 58.16351966513671812 ) ) ;
#18181=CARTESIAN_POINT ( 'NONE',  ( -160.8964159109769696, -158.0438272943107165, 46.59394152635518793 ) ) ;
#18182=CARTESIAN_POINT ( 'NONE',  ( -142.0420953463935803, -186.5084106276440536, 46.59394152635518083 ) ) ;
#18185=CARTESIAN_POINT ( 'NONE',  ( -154.3824083646099439, -170.7584106276440536, 40.69124936498395328 ) ) ;
#18191=ORIENTED_EDGE ( 'NONE', *, *, #18659, .F. ) ;
#18212=CARTESIAN_POINT ( 'NONE',  ( -145.6429501568359797, -195.2084106276440707, 41.63779006702063867 ) ) ;
#18214=CARTESIAN_POINT ( 'NONE',  ( -143.8425227516148084, -186.9584106276440423, 55.19815736654470584 ) ) ;
#18231=CARTESIAN_POINT ( 'NONE',  ( -156.4692748966155591, -155.6811984188981057, 40.99676866812693277 ) ) ;
#18234=CARTESIAN_POINT ( 'NONE',  ( -161.4692556286853176, -179.4891397928654726, 49.65701158161630957 ) ) ;
#18235=ADVANCED_FACE ( 'NONE', ( #10733 ), #14128, .T. ) ;
#18238=CARTESIAN_POINT ( 'NONE',  ( -160.8964159109769696, -193.8938272943107393, 49.65701158161630957 ) ) ;
#18242=CARTESIAN_POINT ( 'NONE',  ( -148.5561028927606344, -185.7938272943107449, 40.69124936498395328 ) ) ;
#18246=VERTEX_POINT ( 'NONE', #13810 ) ;
#18260=CARTESIAN_POINT ( 'NONE',  ( -159.0959885057557983, -158.1938272943107222, 44.11586579668791330 ) ) ;
#18261=CARTESIAN_POINT ( 'NONE',  ( -141.4692556286852891, -165.9891397928654726, 49.65701158161630957 ) ) ;
#18262=CARTESIAN_POINT ( 'NONE',  ( -151.4692556286852891, -179.3130981290892407, 39.14238933923362396 ) ) ;
#18272=EDGE_CURVE ( 'NONE', #21213, #5881, #13636, .T. ) ;
#18280=VERTEX_POINT ( 'NONE', #4004 ) ;
#18286=CARTESIAN_POINT ( 'NONE',  ( -157.2955611005346270, -169.7084106276440139, 57.67623309621198047 ) ) ;
#18287=CARTESIAN_POINT ( 'NONE',  ( -142.0420953463936087, -192.3938272943107393, 49.65701158161630957 ) ) ;
#18288=CARTESIAN_POINT ( 'NONE',  ( -154.5594255724347761, -177.9630981290893033, 59.16757674456785310 ) ) ;
#18298=CARTESIAN_POINT ( 'NONE',  ( -151.4692556286852891, -163.1438272943106824, 59.56931450028537967 ) ) ;
#18299=CARTESIAN_POINT ( 'NONE',  ( -160.8964159109769696, -179.3084106276439798, 46.59394152635518083 ) ) ;
#18302=CARTESIAN_POINT ( 'NONE',  ( -142.0420953463935803, -162.5084106276440536, 46.59394152635518793 ) ) ;
#18311=ORIENTED_EDGE ( 'NONE', *, *, #9886, .F. ) ;
#18318=DIRECTION ( 'NONE',  ( 0.8660254037844390407, -0.000000000000000000, 0.4999999999999994449 ) ) ;
#18328=CARTESIAN_POINT ( 'NONE',  ( -145.6429501568359797, -155.9438272943106938, 41.63779006702063867 ) ) ;
#18330=CARTESIAN_POINT ( 'NONE',  ( -151.4692556286852891, -187.4084106276440309, 59.56931450028537967 ) ) ;
#18331=EDGE_LOOP ( 'NONE', ( #20638, #16265, #11060, #6606 ) ) ;
#18347=CARTESIAN_POINT ( 'NONE',  ( -159.5594255724347761, -179.7891397928654840, 43.77915905869157598 ) ) ;
#18353=CARTESIAN_POINT ( 'NONE',  ( -154.3824083646099439, -182.4938272943107336, 40.69124936498395328 ) ) ;
#18356=EDGE_LOOP ( 'NONE', ( #1090, #14121, #7636, #12445 ) ) ;
#18357=CARTESIAN_POINT ( 'NONE',  ( -141.4692556286852891, -189.9891397928654726, 49.65701158161630957 ) ) ;
#18366=VECTOR ( 'NONE', #7023, 1000.000000000000000 ) ;
#18370=CARTESIAN_POINT ( 'NONE',  ( -157.2955611005345986, -163.4438272943107222, 57.67623309621197336 ) ) ;
#18372=CARTESIAN_POINT ( 'NONE',  ( -157.6495955161842062, -182.0130981290893146, 41.15050349809590102 ) ) ;
#18374=LINE ( 'NONE', #6247, #18820 ) ;
#18387=CARTESIAN_POINT ( 'NONE',  ( -151.4692556286852891, -196.9891397928655010, 59.65701158161632378 ) ) ;
#18395=DIRECTION ( 'NONE',  ( -0.000000000000000000, 1.000000000000000000, -0.000000000000000000 ) ) ;
#18400=CARTESIAN_POINT ( 'NONE',  ( -143.8425227516148084, -168.3584106276440480, 44.11586579668791330 ) ) ;
#18401=CARTESIAN_POINT ( 'NONE',  ( -151.4692556286852891, -193.1438272943107393, 59.56931450028537256 ) ) ;
#18405=CARTESIAN_POINT ( 'NONE',  ( -141.4692556286852891, -177.0630981290893260, 49.65701158161630957 ) ) ;
#18411=CARTESIAN_POINT ( 'NONE',  ( -154.3824083646099439, -161.4938272943107336, 40.69124936498395328 ) ) ;
#18412=CARTESIAN_POINT ( 'NONE',  ( -159.0959885057557983, -179.4584106276440707, 44.11586579668791330 ) ) ;
#18417=( BOUNDED_CURVE ( )  B_SPLINE_CURVE ( 2, ( #19925, #11537, #21692, #14945, #6591, #13310, #12079, #12184, #2266, #20684, #20470, #3714, #12291 ),
 .UNSPECIFIED., .F., .F. ) 
 B_SPLINE_CURVE_WITH_KNOTS ( ( 3, 2, 2, 2, 2, 2, 3 ),
 ( 0.08928571428571421831, 0.09285714285714286031, 0.1000000000000000056, 0.1071428571428571369, 0.1142857142857142821, 0.1214285714285714274, 0.1249999999999999584 ),
 .UNSPECIFIED. ) 
 CURVE ( )  GEOMETRIC_REPRESENTATION_ITEM ( )  RATIONAL_B_SPLINE_CURVE ( ( 0.9755282581475768211, 0.9755282581475763770, 1.000000000000000000, 0.9510565162951535312, 1.000000000000000000, 0.9510565162951535312, 1.000000000000000000, 0.9510565162951535312, 1.000000000000000000, 0.9510565162951535312, 1.000000000000000000, 0.9755282581475770431, 0.9755282581475768211 ) ) 
 REPRESENTATION_ITEM ( '' )  );
#18418=CARTESIAN_POINT ( 'NONE',  ( -142.0420953463936087, -159.6584106276440593, 49.65701158161630957 ) ) ;
#18422=ORIENTED_EDGE ( 'NONE', *, *, #20748, .T. ) ;
#18425=ORIENTED_EDGE ( 'NONE', *, *, #15368, .F. ) ;
#18436=FACE_OUTER_BOUND ( 'NONE', #19068, .T. ) ;
#18440=CARTESIAN_POINT ( 'NONE',  ( -148.5561028927606344, -187.2584106276440536, 58.62277379824867296 ) ) ;
#18442=CARTESIAN_POINT ( 'NONE',  ( -159.0959885057557983, -179.4584106276440707, 44.11586579668791330 ) ) ;
#18446=CARTESIAN_POINT ( 'NONE',  ( -149.8854112254399240, -160.6622583705451461, 59.65701158161632378 ) ) ;
#18457=CARTESIAN_POINT ( 'NONE',  ( -151.4692556286852891, -196.9891397928655010, 49.65701158161630957 ) ) ;
#18458=CARTESIAN_POINT ( 'NONE',  ( -141.4692556286852891, -177.8391397928654385, 46.40781461928724383 ) ) ;
#18465=CARTESIAN_POINT ( 'NONE',  ( -142.0420953463935803, -171.2438272943107052, 46.59394152635518793 ) ) ;
#18469=VERTEX_POINT ( 'NONE', #1020 ) ;
#18474=ORIENTED_EDGE ( 'NONE', *, *, #5917, .F. ) ;
#18481=CARTESIAN_POINT ( 'NONE',  ( -142.0420953463935803, -165.5438272943107165, 52.72008163687743831 ) ) ;
#18483=CARTESIAN_POINT ( 'NONE',  ( -154.5594255724347761, -171.9630981290893033, 59.16757674456785310 ) ) ;
#18497=EDGE_LOOP ( 'NONE', ( #19044, #1748 ) ) ;
#18506=CARTESIAN_POINT ( 'NONE',  ( -142.0420953463935803, -159.5084106276440536, 46.59394152635518793 ) ) ;
#18507=CARTESIAN_POINT ( 'NONE',  ( -159.0959885057557983, -191.1938272943107222, 44.11586579668791330 ) ) ;
#18515=EDGE_CURVE ( 'NONE', #1525, #19662, #2371, .T. ) ;
#18519=CARTESIAN_POINT ( 'NONE',  ( -154.3824083646099439, -164.4938272943107336, 40.69124936498395328 ) ) ;
#18520=CARTESIAN_POINT ( 'NONE',  ( -148.5561028927606344, -171.0584106276440366, 40.69124936498395328 ) ) ;
#18523=CARTESIAN_POINT ( 'NONE',  ( -160.8964159109769696, -164.0084106276440536, 52.72008163687743121 ) ) ;
#18549=CARTESIAN_POINT ( 'NONE',  ( -151.4692556286852891, -182.9084106276440025, 39.74470866294723947 ) ) ;
#18550=AXIS2_PLACEMENT_3D ( 'NONE', #3740, #8816, #15206 ) ;
#18552=CARTESIAN_POINT ( 'NONE',  ( -145.6429501568359797, -174.2084106276440423, 41.63779006702063867 ) ) ;
#18556=CARTESIAN_POINT ( 'NONE',  ( -141.4692556286852891, -159.9891397928654726, 49.65701158161630957 ) ) ;
#18561=VERTEX_POINT ( 'NONE', #20 ) ;
#18568=CARTESIAN_POINT ( 'NONE',  ( -145.2889157411863721, -180.5391397928654555, 41.15050349809590102 ) ) ;
#18570=FACE_OUTER_BOUND ( 'NONE', #3999, .T. ) ;
#18575=CARTESIAN_POINT ( 'NONE',  ( -142.0420953463935803, -174.2438272943107052, 46.59394152635518793 ) ) ;
#18578=CARTESIAN_POINT ( 'NONE',  ( -145.2889157411863437, -195.5391397928654271, 41.15050349809589392 ) ) ;
#18584=VECTOR ( 'NONE', #18005, 1000.000000000000000 ) ;
#18593=CARTESIAN_POINT ( 'NONE',  ( -159.5594255724347761, -169.2630981290892862, 55.53486410454104316 ) ) ;
#18595=CARTESIAN_POINT ( 'NONE',  ( -151.4692556286852607, -167.3130981290893260, 39.65701158161629536 ) ) ;
#18596=CARTESIAN_POINT ( 'NONE',  ( -159.5594255724347761, -166.2630981290893146, 55.53486410454104316 ) ) ;
#18597=VECTOR ( 'NONE', #13386, 1000.000000000000000 ) ;
#18607=CARTESIAN_POINT ( 'NONE',  ( -141.4692556286852891, -185.9130981290892919, 46.40781461928724383 ) ) ;
#18610=CARTESIAN_POINT ( 'NONE',  ( -143.3790856849358306, -167.7630981290893146, 43.77915905869157598 ) ) ;
#18617=CARTESIAN_POINT ( 'NONE',  ( -159.5594255724347761, -194.7891397928654555, 43.77915905869157598 ) ) ;
#18618=CARTESIAN_POINT ( 'NONE',  ( -157.2955611005345986, -178.4438272943107222, 57.67623309621197336 ) ) ;
#18624=CARTESIAN_POINT ( 'NONE',  ( -161.4692556286853176, -184.5630981290892976, 49.65701158161630957 ) ) ;
#18627=CARTESIAN_POINT ( 'NONE',  ( -148.5561028927606344, -156.9938272943107052, 58.62277379824867296 ) ) ;
#18628=CARTESIAN_POINT ( 'NONE',  ( -160.8964159109769696, -179.1584106276440309, 49.65701158161630957 ) ) ;
#18631=CARTESIAN_POINT ( 'NONE',  ( -159.0959885057557983, -161.4584106276440423, 44.11586579668791330 ) ) ;
#18642=CIRCLE ( 'NONE', #7067, 10.00000000000000888 ) ;
#18649=CARTESIAN_POINT ( 'NONE',  ( -159.5594255724347761, -190.8630981290893089, 43.77915905869157598 ) ) ;
#18654=ORIENTED_EDGE ( 'NONE', *, *, #4689, .T. ) ;
#18655=CARTESIAN_POINT ( 'NONE',  ( -157.2955611005346270, -190.7084106276440423, 57.67623309621198047 ) ) ;
#18657=CARTESIAN_POINT ( 'NONE',  ( -160.8964159109769696, -173.3084106276440366, 46.59394152635518793 ) ) ;
#18658=ORIENTED_EDGE ( 'NONE', *, *, #11961, .F. ) ;
#18659=EDGE_CURVE ( 'NONE', #2272, #1525, #828, .T. ) ;
#18670=DIRECTION ( 'NONE',  ( -0.000000000000000000, 1.000000000000000000, -0.000000000000000000 ) ) ;
#18676=CARTESIAN_POINT ( 'NONE',  ( -161.4692556286852607, -182.3391397928654669, 52.90620854394536821 ) ) ;
#18683=CARTESIAN_POINT ( 'NONE',  ( -145.6429501568359797, -170.9438272943107222, 41.63779006702063867 ) ) ;
#18689=CARTESIAN_POINT ( 'NONE',  ( -141.4692556286852891, -189.8391397928655238, 46.40781461928724383 ) ) ;
#18698=CARTESIAN_POINT ( 'NONE',  ( -157.6495955161842062, -193.1130981290893089, 58.16351966513671812 ) ) ;
#18699=LINE ( 'NONE', #13834, #13955 ) ;
#18701=CARTESIAN_POINT ( 'NONE',  ( -141.4692556286852891, -174.0630981290893260, 49.65701158161630957 ) ) ;
#18703=CARTESIAN_POINT ( 'NONE',  ( -143.3790856849358306, -164.7630981290893146, 43.77915905869157598 ) ) ;
#18704=CARTESIAN_POINT ( 'NONE',  ( -151.4692556286852891, -189.2391397928654726, 39.65701158161630246 ) ) ;
#18708=CARTESIAN_POINT ( 'NONE',  ( -149.8854112254399240, -183.3160212151857422, 39.65701158161629536 ) ) ;
#18713=CARTESIAN_POINT ( 'NONE',  ( -148.3790856849358306, -186.6630981290893203, 59.16757674456786020 ) ) ;
#18722=CARTESIAN_POINT ( 'NONE',  ( -145.2889157411863721, -195.5391397928654555, 41.15050349809590102 ) ) ;
#18723=CARTESIAN_POINT ( 'NONE',  ( -160.8964159109769696, -178.7438272943106767, 52.72008163687743121 ) ) ;
#18730=CARTESIAN_POINT ( 'NONE',  ( -157.6495955161842062, -173.0391397928654840, 58.16351966513671812 ) ) ;
#18737=CARTESIAN_POINT ( 'NONE',  ( -159.0959885057557983, -170.4584106276440423, 44.11586579668791330 ) ) ;
#18743=ORIENTED_EDGE ( 'NONE', *, *, #9886, .T. ) ;
#18745=CARTESIAN_POINT ( 'NONE',  ( -143.3790856849358306, -193.2891397928654555, 55.53486410454105027 ) ) ;
#18746=ORIENTED_EDGE ( 'NONE', *, *, #16887, .F. ) ;
#18756=CARTESIAN_POINT ( 'NONE',  ( -151.4692556286853176, -174.2391397928654726, 39.65701158161629536 ) ) ;
#18761=CARTESIAN_POINT ( 'NONE',  ( -142.0420953463936087, -180.3938272943107108, 49.65701158161630957 ) ) ;
#18762=VERTEX_POINT ( 'NONE', #18756 ) ;
#18763=CARTESIAN_POINT ( 'NONE',  ( -160.8964159109769696, -188.3084106276440366, 46.59394152635518793 ) ) ;
#18765=CARTESIAN_POINT ( 'NONE',  ( -145.6429501568359797, -177.2084106276440423, 41.63779006702063867 ) ) ;
#18774=CARTESIAN_POINT ( 'NONE',  ( -142.0420953463936087, -195.6584106276440593, 49.65701158161630957 ) ) ;
#18779=CARTESIAN_POINT ( 'NONE',  ( -154.5594255724347761, -166.8891397928654499, 59.16757674456785310 ) ) ;
#18787=CARTESIAN_POINT ( 'NONE',  ( -145.6429501568359797, -174.8438272943107279, 57.67623309621198047 ) ) ;
#18791=CARTESIAN_POINT ( 'NONE',  ( -153.0531000319306827, -157.8160212151857422, 59.65701158161631668 ) ) ;
#18793=CARTESIAN_POINT ( 'NONE',  ( -151.4692556286852891, -189.2391397928654726, 39.65701158161630246 ) ) ;
#18794=CARTESIAN_POINT ( 'NONE',  ( -156.4692864601533131, -155.0638355923473455, 40.99677534440144200 ) ) ;
#18798=( BOUNDED_CURVE ( )  B_SPLINE_CURVE ( 2, ( #5048, #11759, #9797, #14950, #19706, #1519, #11425, #4938, #13197, #8136, #14839, #11541, #6476 ),
 .UNSPECIFIED., .F., .F. ) 
 B_SPLINE_CURVE_WITH_KNOTS ( ( 3, 2, 2, 2, 2, 2, 3 ),
 ( 0.3035714285714286031, 0.3071428571428571619, 0.3142857142857142794, 0.3214285714285714524, 0.3285714285714285698, 0.3357142857142856873, 0.3392857142857142461 ),
 .UNSPECIFIED. ) 
 CURVE ( )  GEOMETRIC_REPRESENTATION_ITEM ( )  RATIONAL_B_SPLINE_CURVE ( ( 0.9755282581475768211, 0.9755282581475769321, 1.000000000000000000, 0.9510565162951535312, 1.000000000000000000, 0.9510565162951535312, 1.000000000000000000, 0.9510565162951535312, 1.000000000000000000, 0.9510565162951535312, 1.000000000000000000, 0.9755282581475769321, 0.9755282581475768211 ) ) 
 REPRESENTATION_ITEM ( '' )  );
#18802=CARTESIAN_POINT ( 'NONE',  ( -151.4692556286852891, -196.9891397928655010, 49.65701158161630957 ) ) ;
#18803=CARTESIAN_POINT ( 'NONE',  ( -151.4692556286852891, -126.9891397928655010, 49.65701158161630957 ) ) ;
#18808=CARTESIAN_POINT ( 'NONE',  ( -141.4692556286852891, -170.9130981290893203, 46.40781461928724383 ) ) ;
#18818=CARTESIAN_POINT ( 'NONE',  ( -143.3790856849358306, -156.3630981290893089, 55.53486410454105027 ) ) ;
#18820=VECTOR ( 'NONE', #14834, 1000.000000000000000 ) ;
#18829=CARTESIAN_POINT ( 'NONE',  ( -142.0420953463935803, -156.8084106276440366, 52.72008163687743831 ) ) ;
#18830=CARTESIAN_POINT ( 'NONE',  ( -157.2955611005345986, -185.3438272943106995, 41.63779006702063867 ) ) ;
#18831=CARTESIAN_POINT ( 'NONE',  ( -151.4692556286853176, -193.7391397928655010, 59.65701158161632378 ) ) ;
#18840=CARTESIAN_POINT ( 'NONE',  ( -151.4692556286852891, -189.2391397928654726, 39.65701158161630246 ) ) ;
#18841=CARTESIAN_POINT ( 'NONE',  ( -154.3824083646099439, -167.7584106276440536, 40.69124936498395328 ) ) ;
#18850=EDGE_CURVE ( 'NONE', #13802, #19216, #10599, .T. ) ;
#18856=CARTESIAN_POINT ( 'NONE',  ( -158.9748091281504401, -116.9891397928655010, 36.65701158161628115 ) ) ;
#18863=CARTESIAN_POINT ( 'NONE',  ( -142.0420953463935803, -177.5438272943107165, 52.72008163687743831 ) ) ;
#18865=ORIENTED_EDGE ( 'NONE', *, *, #3207, .F. ) ;
#18866=CARTESIAN_POINT ( 'NONE',  ( -148.5561028927606344, -186.0584106276440650, 40.69124936498395328 ) ) ;
#18885=CARTESIAN_POINT ( 'NONE',  ( -148.3790856849358306, -171.3891397928654499, 40.14644641866477315 ) ) ;
#18887=CARTESIAN_POINT ( 'NONE',  ( -157.6495955161842062, -194.0391397928653987, 58.16351966513671812 ) ) ;
#18892=CARTESIAN_POINT ( 'NONE',  ( -142.0420953463936087, -177.3938272943107393, 49.65701158161630957 ) ) ;
#18894=CARTESIAN_POINT ( 'NONE',  ( -153.0531000319306827, -169.8160212151857138, 59.65701158161631668 ) ) ;
#18908=CARTESIAN_POINT ( 'NONE',  ( -149.8854112254399240, -181.6622583705451746, 59.65701158161632378 ) ) ;
#18912=CARTESIAN_POINT ( 'NONE',  ( -148.3790856849358306, -191.4630981290893317, 40.14644641866477315 ) ) ;
#18918=CARTESIAN_POINT ( 'NONE',  ( -148.3790856849358306, -168.6630981290892919, 59.16757674456786020 ) ) ;
#18942=CARTESIAN_POINT ( 'NONE',  ( -161.4692556286852607, -194.6391397928654783, 46.40781461928724383 ) ) ;
#18943=CARTESIAN_POINT ( 'NONE',  ( -151.4692556286852891, -184.1438272943107108, 59.56931450028537256 ) ) ;
#18952=CARTESIAN_POINT ( 'NONE',  ( -154.5594255724347761, -187.8891397928654783, 59.16757674456785310 ) ) ;
#18953=CARTESIAN_POINT ( 'NONE',  ( -154.3824083646099439, -164.7584106276440536, 40.69124936498395328 ) ) ;
#18959=EDGE_CURVE ( 'NONE', #12248, #19655, #3350, .T. ) ;
#18961=CARTESIAN_POINT ( 'NONE',  ( -161.4692556286853176, -160.5630981290892976, 49.65701158161630957 ) ) ;
#18975=CARTESIAN_POINT ( 'NONE',  ( -145.6429501568359797, -176.9438272943107506, 41.63779006702063867 ) ) ;
#18977=VERTEX_POINT ( 'NONE', #7513 ) ;
#18978=CARTESIAN_POINT ( 'NONE',  ( -160.8964159109769696, -179.3084106276440082, 46.59394152635518793 ) ) ;
#18983=PLANE ( 'NONE',  #18000 ) ;
#18999=CARTESIAN_POINT ( 'NONE',  ( -141.4692556286852891, -180.2130981290893033, 52.90620854394536821 ) ) ;
#19000=CARTESIAN_POINT ( 'NONE',  ( -145.2889157411863721, -165.5391397928654840, 41.15050349809590102 ) ) ;
#19006=CARTESIAN_POINT ( 'NONE',  ( -154.3824083646099439, -163.2938272943107449, 58.62277379824867296 ) ) ;
#19021=CARTESIAN_POINT ( 'NONE',  ( -151.4692556286853176, -180.2391397928654726, 39.65701158161629536 ) ) ;
#19028=CARTESIAN_POINT ( 'NONE',  ( -141.4692556286852891, -158.9130981290892919, 46.40781461928724383 ) ) ;
#19035=ORIENTED_EDGE ( 'NONE', *, *, #16887, .T. ) ;
#19040=EDGE_CURVE ( 'NONE', #20985, #20856, #4620, .T. ) ;
#19042=CYLINDRICAL_SURFACE ( 'NONE', #19542, 10.00000000000000888 ) ;
#19044=ORIENTED_EDGE ( 'NONE', *, *, #17326, .T. ) ;
#19050=CARTESIAN_POINT ( 'NONE',  ( -143.8425227516148084, -180.0938272943107279, 44.11586579668791330 ) ) ;
#19052=CARTESIAN_POINT ( 'NONE',  ( -161.4692556286853176, -190.5630981290892976, 49.65701158161630957 ) ) ;
#19061=CARTESIAN_POINT ( 'NONE',  ( -160.8964159109769696, -161.3084106276440366, 46.59394152635518083 ) ) ;
#19068=EDGE_LOOP ( 'NONE', ( #8426, #20422, #9301, #3468 ) ) ;
#19082=EDGE_CURVE ( 'NONE', #18246, #18762, #21246, .T. ) ;
#19087=CARTESIAN_POINT ( 'NONE',  ( -154.3824083646099439, -182.4938272943107336, 40.69124936498395328 ) ) ;
#19088=CARTESIAN_POINT ( 'NONE',  ( -154.3824083646099439, -193.5584106276440650, 58.62277379824867296 ) ) ;
#19090=CARTESIAN_POINT ( 'NONE',  ( -143.8425227516148084, -180.9584106276440707, 55.19815736654470584 ) ) ;
#19110=CARTESIAN_POINT ( 'NONE',  ( -161.4692556286852607, -167.3391397928654385, 52.90620854394536821 ) ) ;
#19116=CARTESIAN_POINT ( 'NONE',  ( -151.4692556286852891, -164.6438272943107108, 39.74470866294723947 ) ) ;
#19119=CARTESIAN_POINT ( 'NONE',  ( -157.2955611005346270, -193.7084106276440423, 57.67623309621198047 ) ) ;
#19135=CARTESIAN_POINT ( 'NONE',  ( -151.4692556286852891, -159.8130981290893260, 60.17163382399899518 ) ) ;
#19140=CARTESIAN_POINT ( 'NONE',  ( -145.6429501568359797, -191.9438272943106938, 41.63779006702063867 ) ) ;
#19150=CARTESIAN_POINT ( 'NONE',  ( -145.2889157411863437, -164.6130981290893089, 41.15050349809589392 ) ) ;
#19154=CARTESIAN_POINT ( 'NONE',  ( -159.0959885057557983, -173.1938272943107506, 44.11586579668791330 ) ) ;
#19156=CARTESIAN_POINT ( 'NONE',  ( -161.4692556286852607, -190.7130981290893033, 46.40781461928724383 ) ) ;
#19165=CARTESIAN_POINT ( 'NONE',  ( -142.0420953463935803, -168.5084106276440536, 46.59394152635518083 ) ) ;
#19186=CARTESIAN_POINT ( 'NONE',  ( -156.1828684652451784, -155.6591478762521206, 41.49287016839741682 ) ) ;
#19192=CARTESIAN_POINT ( 'NONE',  ( -159.0959885057557983, -181.5938272943107279, 55.19815736654470584 ) ) ;
#19193=CYLINDRICAL_SURFACE ( 'NONE', #9941, 10.00000000000000888 ) ;
#19194=ORIENTED_EDGE ( 'NONE', *, *, #9487, .F. ) ;
#19195=CARTESIAN_POINT ( 'NONE',  ( -142.0420953463935803, -174.8084106276440082, 52.72008163687743831 ) ) ;
#19197=VERTEX_POINT ( 'NONE', #17060 ) ;
#19202=EDGE_CURVE ( 'NONE', #5698, #7641, #15739, .T. ) ;
#19211=DIRECTION ( 'NONE',  ( 0.000000000000000000, -0.000000000000000000, -1.000000000000000000 ) ) ;
#19212=CARTESIAN_POINT ( 'NONE',  ( -141.4692556286852891, -171.8391397928654385, 46.40781461928724383 ) ) ;
#19215=CARTESIAN_POINT ( 'NONE',  ( -154.5594255724347761, -162.9630981290893317, 59.16757674456785310 ) ) ;
#19216=VERTEX_POINT ( 'NONE', #13864 ) ;
#19218=CARTESIAN_POINT ( 'NONE',  ( -142.0420953463935803, -162.2438272943107336, 46.59394152635518793 ) ) ;
#19221=CARTESIAN_POINT ( 'NONE',  ( -157.2955611005346270, -191.6084106276440764, 41.63779006702063867 ) ) ;
#19240=CARTESIAN_POINT ( 'NONE',  ( -141.4692556286852891, -159.0630981290892976, 49.65701158161630957 ) ) ;
#19259=CARTESIAN_POINT ( 'NONE',  ( -143.3790856849358306, -165.3630981290893089, 55.53486410454105027 ) ) ;
#19265=CARTESIAN_POINT ( 'NONE',  ( -159.0959885057557983, -170.1938272943107222, 44.11586579668791330 ) ) ;
#19267=CARTESIAN_POINT ( 'NONE',  ( -159.5594255724347761, -184.2630981290893146, 55.53486410454104316 ) ) ;
#19274=CARTESIAN_POINT ( 'NONE',  ( -160.8964159109769696, -167.0084106276440536, 52.72008163687743121 ) ) ;
#19294=CARTESIAN_POINT ( 'NONE',  ( -159.5594255724347761, -187.8630981290893089, 43.77915905869157598 ) ) ;
#19295=DIRECTION ( 'NONE',  ( 0.000000000000000000, 0.7071067811865573427, 0.7071067811865378028 ) ) ;
#19299=CARTESIAN_POINT ( 'NONE',  ( -157.2955611005346270, -175.4438272943107506, 57.67623309621198047 ) ) ;
#19303=LINE ( 'NONE', #1552, #14079 ) ;
#19307=ORIENTED_EDGE ( 'NONE', *, *, #8508, .F. ) ;
#19318=CARTESIAN_POINT ( 'NONE',  ( -151.4692556286852891, -159.2391397928654726, 39.14238933923362396 ) ) ;
#19324=CARTESIAN_POINT ( 'NONE',  ( -143.8425227516148084, -168.6938272943107222, 55.19815736654470584 ) ) ;
#19340=CARTESIAN_POINT ( 'NONE',  ( -141.4692556286852891, -186.9891397928654726, 49.65701158161630957 ) ) ;
#19343=CARTESIAN_POINT ( 'NONE',  ( -143.3790856849358306, -161.7630981290893146, 43.77915905869157598 ) ) ;
#19350=CARTESIAN_POINT ( 'NONE',  ( -151.4692556286852891, -188.6438272943107393, 39.74470866294723947 ) ) ;
#19367=( BOUNDED_CURVE ( )  B_SPLINE_CURVE ( 2, ( #9818, #5176, #14867, #21613, #6503, #11895, #18624, #10254, #4845, #8162, #13117, #8598, #211 ),
 .UNSPECIFIED., .F., .F. ) 
 B_SPLINE_CURVE_WITH_KNOTS ( ( 3, 2, 2, 2, 2, 2, 3 ),
 ( 0.2321428571428571508, 0.2357142857142857095, 0.2428571428571428548, 0.2500000000000000000, 0.2571428571428571175, 0.2642857142857142905, 0.2678571428571428492 ),
 .UNSPECIFIED. ) 
 CURVE ( )  GEOMETRIC_REPRESENTATION_ITEM ( )  RATIONAL_B_SPLINE_CURVE ( ( 0.9755282581475767101, 0.9755282581475768211, 1.000000000000000000, 0.9510565162951535312, 1.000000000000000000, 0.9510565162951535312, 1.000000000000000000, 0.9510565162951535312, 1.000000000000000000, 0.9510565162951535312, 1.000000000000000000, 0.9755282581475768211, 0.9755282581475768211 ) ) 
 REPRESENTATION_ITEM ( '' )  );
#19368=CARTESIAN_POINT ( 'NONE',  ( -160.8964159109769696, -172.7438272943107336, 52.72008163687743121 ) ) ;
#19370=CARTESIAN_POINT ( 'NONE',  ( -159.5594255724347761, -187.2630981290893146, 55.53486410454104316 ) ) ;
#19374=CARTESIAN_POINT ( 'NONE',  ( -141.4692556286852891, -162.9891397928654726, 49.65701158161630957 ) ) ;
#19378=CARTESIAN_POINT ( 'NONE',  ( -154.3824083646099439, -157.5584106276440650, 58.62277379824867296 ) ) ;
#19379=CARTESIAN_POINT ( 'NONE',  ( -154.5594255724347761, -163.8891397928654499, 59.16757674456785310 ) ) ;
#19380=CARTESIAN_POINT ( 'NONE',  ( -155.5590455049452316, -156.0406172220664303, 40.47124262348441448 ) ) ;
#19384=ORIENTED_EDGE ( 'NONE', *, *, #14612, .F. ) ;
#19386=ORIENTED_EDGE ( 'NONE', *, *, #20723, .F. ) ;
#19395=( NAMED_UNIT ( * ) PLANE_ANGLE_UNIT ( ) SI_UNIT ( $, .RADIAN. ) );
#19401=CARTESIAN_POINT ( 'NONE',  ( -148.5561028927606344, -171.9938272943107336, 58.62277379824867296 ) ) ;
#19402=CARTESIAN_POINT ( 'NONE',  ( -143.8425227516148084, -186.9584106276440423, 55.19815736654470584 ) ) ;
#19404=CARTESIAN_POINT ( 'NONE',  ( -160.8964159109769696, -173.1584106276440593, 49.65701158161630957 ) ) ;
#19422=CARTESIAN_POINT ( 'NONE',  ( -161.4692556286853176, -158.4891397928654726, 49.65701158161630957 ) ) ;
#19423=CYLINDRICAL_SURFACE ( 'NONE', #10841, 10.00000000000000888 ) ;
#19431=CARTESIAN_POINT ( 'NONE',  ( -159.0959885057557983, -167.1938272943107222, 44.11586579668791330 ) ) ;
#19433=CARTESIAN_POINT ( 'NONE',  ( -151.4692556286852891, -193.4084106276440593, 59.56931450028537967 ) ) ;
#19449=CARTESIAN_POINT ( 'NONE',  ( -148.3790856849358306, -187.5891397928654953, 59.16757674456786020 ) ) ;
#19453=CARTESIAN_POINT ( 'NONE',  ( -161.4692556286852607, -163.4130981290892635, 52.90620854394536821 ) ) ;
#19458=CARTESIAN_POINT ( 'NONE',  ( -143.8425227516148084, -192.6938272943107222, 55.19815736654470584 ) ) ;
#19470=FACE_OUTER_BOUND ( 'NONE', #18356, .T. ) ;
#19474=CARTESIAN_POINT ( 'NONE',  ( -151.4692556286852891, -169.1438272943107108, 59.56931450028537256 ) ) ;
#19476=CARTESIAN_POINT ( 'NONE',  ( -148.3790856849358306, -191.4630981290893317, 40.14644641866477315 ) ) ;
#19479=CARTESIAN_POINT ( 'NONE',  ( -143.3790856849358306, -162.6891397928654897, 43.77915905869157598 ) ) ;
#19484=CARTESIAN_POINT ( 'NONE',  ( -156.1828684652451784, -155.6591478762521206, 41.49287016839741682 ) ) ;
#19508=CARTESIAN_POINT ( 'NONE',  ( -151.4692556286852891, -173.6438272943107108, 39.74470866294723947 ) ) ;
#19509=CARTESIAN_POINT ( 'NONE',  ( -145.6429501568359797, -184.1084106276440480, 57.67623309621197336 ) ) ;
#19512=CARTESIAN_POINT ( 'NONE',  ( -151.4692556286852891, -167.9084106276440309, 39.74470866294723947 ) ) ;
#19529=CARTESIAN_POINT ( 'NONE',  ( -154.5594255724347761, -156.0891397928654953, 40.14644641866476604 ) ) ;
#19531=CARTESIAN_POINT ( 'NONE',  ( -151.4692556286852607, -184.7391397928654726, 59.65701158161632378 ) ) ;
#19534=CARTESIAN_POINT ( 'NONE',  ( -145.6429501568359797, -156.8438272943107563, 57.67623309621198047 ) ) ;
#19536=CARTESIAN_POINT ( 'NONE',  ( -145.6429501568359797, -184.1084106276440480, 57.67623309621198047 ) ) ;
#19537=ORIENTED_EDGE ( 'NONE', *, *, #7908, .F. ) ;
#19538=CARTESIAN_POINT ( 'NONE',  ( -157.6495955161842062, -161.0391397928654555, 58.16351966513671812 ) ) ;
#19539=FACE_OUTER_BOUND ( 'NONE', #8563, .T. ) ;
#19542=AXIS2_PLACEMENT_3D ( 'NONE', #10885, #415, #7147 ) ;
#19544=ORIENTED_EDGE ( 'NONE', *, *, #19749, .F. ) ;
#19552=CARTESIAN_POINT ( 'NONE',  ( -148.3790856849358306, -189.3891397928654783, 40.14644641866477315 ) ) ;
#19555=CARTESIAN_POINT ( 'NONE',  ( -142.0420953463936087, -186.3938272943107393, 49.65701158161630957 ) ) ;
#19560=CARTESIAN_POINT ( 'NONE',  ( -148.5561028927606344, -182.7938272943107449, 40.69124936498395328 ) ) ;
#19562=CARTESIAN_POINT ( 'NONE',  ( -149.8854112254399240, -161.3899795514095388, 39.65701158161629536 ) ) ;
#19576=CARTESIAN_POINT ( 'NONE',  ( -161.4692556286852891, -193.7130981290893317, 46.40781461928724383 ) ) ;
#19581=CARTESIAN_POINT ( 'NONE',  ( -151.4692556286852891, -170.6438272943107393, 39.74470866294723947 ) ) ;
#19583=CARTESIAN_POINT ( 'NONE',  ( -141.4692556286852891, -177.0630981290893260, 49.65701158161630957 ) ) ;
#19586=CARTESIAN_POINT ( 'NONE',  ( -148.3790856849358306, -163.5891397928654669, 59.16757674456786020 ) ) ;
#19591=CARTESIAN_POINT ( 'NONE',  ( -148.5561028927606344, -159.0584106276440650, 40.69124936498395328 ) ) ;
#19611=CARTESIAN_POINT ( 'NONE',  ( -141.4692556286852891, -182.9130981290893203, 46.40781461928724383 ) ) ;
#19620=CARTESIAN_POINT ( 'NONE',  ( -151.4692556286852891, -175.1438272943107393, 59.56931450028537967 ) ) ;
#19621=CARTESIAN_POINT ( 'NONE',  ( -148.5561028927606344, -183.0584106276440650, 40.69124936498395328 ) ) ;
#19623=ORIENTED_EDGE ( 'NONE', *, *, #2011, .T. ) ;
#19625=CARTESIAN_POINT ( 'NONE',  ( -148.5561028927606344, -166.2584106276440536, 58.62277379824867296 ) ) ;
#19632=ORIENTED_EDGE ( 'NONE', *, *, #19690, .T. ) ;
#19645=CARTESIAN_POINT ( 'NONE',  ( -161.4692556286853176, -164.4891397928654726, 49.65701158161630957 ) ) ;
#19650=ORIENTED_EDGE ( 'NONE', *, *, #8984, .T. ) ;
#19652=CARTESIAN_POINT ( 'NONE',  ( -142.0420953463935803, -159.2438272943107620, 46.59394152635518793 ) ) ;
#19654=CARTESIAN_POINT ( 'NONE',  ( -143.8425227516148084, -183.9584106276440707, 55.19815736654470584 ) ) ;
#19655=VERTEX_POINT ( 'NONE', #3389 ) ;
#19660=VERTEX_POINT ( 'NONE', #9682 ) ;
#19662=VERTEX_POINT ( 'NONE', #4933 ) ;
#19669=CARTESIAN_POINT ( 'NONE',  ( -161.4692556286852607, -185.6391397928654783, 46.40781461928724383 ) ) ;
#19672=CARTESIAN_POINT ( 'NONE',  ( -154.3824083646099439, -194.4938272943107336, 40.69124936498395328 ) ) ;
#19674=AXIS2_PLACEMENT_3D ( 'NONE', #2714, #17912, #16371 ) ;
#19678=CARTESIAN_POINT ( 'NONE',  ( -154.3824083646099439, -181.2938272943107449, 58.62277379824867296 ) ) ;
#19680=CARTESIAN_POINT ( 'NONE',  ( -143.9637021292201950, -116.9891397928655010, 62.65701158161630957 ) ) ;
#19690=EDGE_CURVE ( 'NONE', #5881, #4358, #18374, .T. ) ;
#19698=CARTESIAN_POINT ( 'NONE',  ( -160.8964159109769696, -161.0438272943107165, 46.59394152635518083 ) ) ;
#19699=CARTESIAN_POINT ( 'NONE',  ( -141.4692556286852891, -166.1391397928654783, 52.90620854394536821 ) ) ;
#19700=CARTESIAN_POINT ( 'NONE',  ( -159.5594255724347761, -178.2630981290893146, 55.53486410454104316 ) ) ;
#19706=CARTESIAN_POINT ( 'NONE',  ( -159.5594255724347761, -182.7891397928654840, 43.77915905869157598 ) ) ;
#19707=CARTESIAN_POINT ( 'NONE',  ( -159.0959885057557983, -157.8584106276440480, 55.19815736654470584 ) ) ;
#19711=CARTESIAN_POINT ( 'NONE',  ( -151.4692556286852891, -187.7391397928655010, 59.65701158161632378 ) ) ;
#19712=ORIENTED_EDGE ( 'NONE', *, *, #4689, .F. ) ;
#19721=CARTESIAN_POINT ( 'NONE',  ( -151.4692556286852891, -172.4084106276440309, 59.56931450028537967 ) ) ;
#19725=CARTESIAN_POINT ( 'NONE',  ( -143.3790856849358306, -189.3630981290893089, 55.53486410454105027 ) ) ;
#19732=CARTESIAN_POINT ( 'NONE',  ( -143.8425227516148084, -168.6938272943107222, 55.19815736654470584 ) ) ;
#19733=CARTESIAN_POINT ( 'NONE',  ( -159.0959885057557983, -188.4584106276440423, 44.11586579668791330 ) ) ;
#19736=CARTESIAN_POINT ( 'NONE',  ( -142.0420953463935803, -168.5084106276440536, 46.59394152635518793 ) ) ;
#19748=ADVANCED_FACE ( 'NONE', ( #13083 ), #16379, .T. ) ;
#19749=EDGE_CURVE ( 'NONE', #14572, #14601, #18417, .T. ) ;
#19754=CARTESIAN_POINT ( 'NONE',  ( -158.9748091281504401, -116.9891397928655010, 36.65701158161628115 ) ) ;
#19756=CARTESIAN_POINT ( 'NONE',  ( -159.5594255724347761, -164.7891397928654555, 43.77915905869157598 ) ) ;
#19763=CARTESIAN_POINT ( 'NONE',  ( -151.4692556286852891, -160.1438272943107393, 59.56931450028537967 ) ) ;
#19765=CARTESIAN_POINT ( 'NONE',  ( -160.8964159109769696, -182.0084106276440821, 52.72008163687743121 ) ) ;
#19766=ORIENTED_EDGE ( 'NONE', *, *, #7072, .T. ) ;
#19767=CARTESIAN_POINT ( 'NONE',  ( -151.4692556286852607, -160.7391397928654158, 59.65701158161632378 ) ) ;
#19773=CARTESIAN_POINT ( 'NONE',  ( -153.0531000319306827, -155.2362167067690280, 39.65701158161629536 ) ) ;
#19782=CARTESIAN_POINT ( 'NONE',  ( -145.2889157411863721, -187.4391397928654612, 58.16351966513671812 ) ) ;
#19785=CARTESIAN_POINT ( 'NONE',  ( -160.8964159109769696, -188.0438272943107449, 46.59394152635518793 ) ) ;
#19791=CARTESIAN_POINT ( 'NONE',  ( -142.0420953463935803, -180.2438272943107052, 46.59394152635518793 ) ) ;
#19802=VERTEX_POINT ( 'NONE', #18704 ) ;
#19809=CARTESIAN_POINT ( 'NONE',  ( -148.5561028927606344, -164.7938272943107449, 40.69124936498395328 ) ) ;
#19811=CARTESIAN_POINT ( 'NONE',  ( -157.6495955161842062, -176.0130981290893146, 41.15050349809590102 ) ) ;
#19819=LINE ( 'NONE', #18153, #9093 ) ;
#19831=ADVANCED_FACE ( 'NONE', ( #9115 ), #4539, .T. ) ;
#19832=CARTESIAN_POINT ( 'NONE',  ( -154.3824083646099439, -166.5584106276440366, 58.62277379824867296 ) ) ;
#19833=CARTESIAN_POINT ( 'NONE',  ( -145.6429501568359797, -189.8438272943106710, 57.67623309621197336 ) ) ;
#19834=CARTESIAN_POINT ( 'NONE',  ( -157.6495955161842062, -179.0130981290892862, 41.15050349809589392 ) ) ;
#19837=CARTESIAN_POINT ( 'NONE',  ( -149.8854112254399240, -175.6622583705452030, 59.65701158161632378 ) ) ;
#19840=LINE ( 'NONE', #13546, #979 ) ;
#19842=CARTESIAN_POINT ( 'NONE',  ( -154.3824083646099439, -158.4938272943107052, 40.69124936498395328 ) ) ;
#19843=CARTESIAN_POINT ( 'NONE',  ( -154.3824083646099439, -188.7584106276440536, 40.69124936498395328 ) ) ;
#19846=CARTESIAN_POINT ( 'NONE',  ( -145.6429501568359797, -171.2084106276440707, 41.63779006702063867 ) ) ;
#19848=CARTESIAN_POINT ( 'NONE',  ( -136.4581486297550441, -116.9891397928655010, 49.65701158161631668 ) ) ;
#19850=EDGE_CURVE ( 'NONE', #4977, #12281, #7353, .T. ) ;
#19864=VECTOR ( 'NONE', #15972, 1000.000000000000114 ) ;
#19872=CARTESIAN_POINT ( 'NONE',  ( -151.4692556286852891, -186.2391397928655010, 39.65701158161630246 ) ) ;
#19875=CARTESIAN_POINT ( 'NONE',  ( -148.5561028927606344, -158.7938272943107449, 40.69124936498395328 ) ) ;
#19877=CARTESIAN_POINT ( 'NONE',  ( -145.6429501568359797, -190.1084106276440195, 57.67623309621198047 ) ) ;
#19878=ORIENTED_EDGE ( 'NONE', *, *, #13823, .T. ) ;
#19894=CARTESIAN_POINT ( 'NONE',  ( -153.0531000319306827, -177.1622583705452314, 39.65701158161630957 ) ) ;
#19895=CARTESIAN_POINT ( 'NONE',  ( -161.4692556286852607, -182.6391397928654214, 46.40781461928724383 ) ) ;
#19900=CARTESIAN_POINT ( 'NONE',  ( -154.3824083646099439, -190.2938272943107449, 58.62277379824867296 ) ) ;
#19904=CARTESIAN_POINT ( 'NONE',  ( -142.0420953463935803, -183.2438272943107336, 46.59394152635518793 ) ) ;
#19908=EDGE_LOOP ( 'NONE', ( #1383, #14063, #2572, #10317 ) ) ;
#19914=ORIENTED_EDGE ( 'NONE', *, *, #4612, .F. ) ;
#19920=DIRECTION ( 'NONE',  ( 0.000000000000000000, 1.000000000000000000, 0.000000000000000000 ) ) ;
#19921=CARTESIAN_POINT ( 'NONE',  ( -159.0959885057557983, -161.1938272943107222, 44.11586579668791330 ) ) ;
#19923=CARTESIAN_POINT ( 'NONE',  ( -145.2889157411863721, -176.6130981290892805, 41.15050349809590102 ) ) ;
#19925=CARTESIAN_POINT ( 'NONE',  ( -151.4692556286852607, -192.2391397928655010, 39.65701158161629536 ) ) ;
#19933=VECTOR ( 'NONE', #18150, 1000.000000000000000 ) ;
#19938=DIRECTION ( 'NONE',  ( 0.000000000000000000, 0.000000000000000000, 1.000000000000000000 ) ) ;
#19941=VERTEX_POINT ( 'NONE', #18774 ) ;
#19943=VERTEX_POINT ( 'NONE', #17210 ) ;
#19951=CARTESIAN_POINT ( 'NONE',  ( -142.0420953463935803, -165.8084106276440366, 52.72008163687743831 ) ) ;
#19952=CARTESIAN_POINT ( 'NONE',  ( -151.4692556286852891, -194.6438272943107393, 39.74470866294723947 ) ) ;
#19954=DIRECTION ( 'NONE',  ( -0.000000000000000000, -1.000000000000000000, -0.000000000000000000 ) ) ;
#19964=CARTESIAN_POINT ( 'NONE',  ( -143.8425227516148084, -165.0938272943107279, 44.11586579668791330 ) ) ;
#19965=CARTESIAN_POINT ( 'NONE',  ( -151.4692556286852891, -170.9084106276440593, 39.74470866294723947 ) ) ;
#19968=( BOUNDED_CURVE ( )  B_SPLINE_CURVE ( 2, ( #16734, #14859, #15200, #8049, #3300, #19952, #4955, #14967, #11663, #14753, #3076, #10028, #20175, #5065, #13541, #18401, #103, #6381, #4723, #10140, #18287, #11778, #3190, #13404, #21494, #13111, #1645, #6835, #18507, #3418, #20276, #6731, #11443, #8377, #18169, #16843, #11889, #19833, #2963, #9813, #16509, #1756, #13437, #8491, #15086, #5169, #1426, #9703, #16403, #8154, #1314, #21606, #6496, #16625, #13215, #4838, #11559, #9919, #1534, #8267, #21714, #6616, #13332, #20068, #17166, #10466, #8918, #18830, #1862, #6942, #425, #7266, #12098, #3736, #12208, #18943, #17057, #20814, #3950, #3843, #20706, #8703, #528, #13967, #5589, #10570, #12314, #20598, #5704, #10676, #1969, #20382, #2183, #13648, #10354, #10248, #15423, #8592, #15621, #5279, #7375, #5483, #19050, #16947, #3522, #17380, #20493, #2080, #641, #5382, #2285, #18723, #8811, #18618, #7157, #9024, #15522, #13860, #17271, #15736, #318, #14076, #15311, #203, #11993, #7047, #3631, #13753, #7804, #6023, #21251, #14402, #14616, #4474, #17597, #14184, #17810, #747, #4165, #4055, #2503, #9346, #6131, #2827, #4366, #21139, #14510, #10783, #19154, #12860, #14290, #19368, #16273, #21035, #9462, #12536, #4265, #21354, #15944, #5918, #2720, #20923, #9567, #12428, #2608, #19581, #12646, #17490, #19265, #11097, #9245, #1178, #2400, #12754, #7591, #19474, #16050, #16162, #9136, #10894, #1074, #11203, #10993, #15836, #7913, #17703, #17918, #7482, #7703, #854, #5805, #960, #3272, #11306, #16376, #4929, #10111, #21797, #1617, #18481, #10004, #13413, #16708, #21689, #19809, #18033, #6243, #16818, #1731, #4698, #8349, #15060, #6706, #18370, #8465, #9677, #20147, #15173, #2939, #5040, #11641, #12972, #14730, #11749, #13189, #6587, #1289, #3385, #19921, #19698, #4586, #8023, #21465, #4810, #11532, #6356, #6467, #13080, #11416, #20043, #18141, #3050, #9787, #16483, #1399, #8128, #14831, #21576, #18260, #3163, #9893, #16593, #1511, #8240, #14942, #13305, #3817, #20573, #179, #13729, #12288, #7241, #3499, #504, #15598, #20466, #5359, #6914, #10441 ),
 .UNSPECIFIED., .F., .F. ) 
 B_SPLINE_CURVE_WITH_KNOTS ( ( 3, 2, 2, 2, 2, 2, 2, 2, 2, 2, 2, 2, 2, 2, 2, 2, 2, 2, 2, 2, 2, 2, 2, 2, 2, 2, 2, 2, 2, 2, 2, 2, 2, 2, 2, 2, 2, 2, 2, 2, 2, 2, 2, 2, 2, 2, 2, 2, 2, 2, 2, 2, 2, 2, 2, 2, 2, 2, 2, 2, 2, 2, 2, 2, 2, 2, 2, 2, 2, 2, 2, 2, 2, 2, 2, 2, 2, 2, 2, 2, 2, 2, 2, 2, 2, 2, 2, 2, 2, 2, 2, 2, 2, 2, 2, 2, 2, 2, 2, 2, 2, 2, 2, 2, 2, 2, 2, 2, 2, 2, 2, 2, 2, 2, 2, 2, 2, 2, 2, 2, 2, 2, 2, 2, 2, 2, 2, 2, 2, 2, 2, 2, 2, 2, 3 ),
 ( 0.000000000000000000, 0.007142857142857142634, 0.01428571428571428527, 0.02142857142857142877, 0.02857142857142857054, 0.03571428571428571230, 0.04285714285714285754, 0.05000000000000000278, 0.05714285714285714107, 0.06428571428571427937, 0.07142857142857142461, 0.07857142857142856984, 0.08571428571428571508, 0.09285714285714286031, 0.1000000000000000056, 0.1071428571428571369, 0.1142857142857142821, 0.1214285714285714274, 0.1285714285714285587, 0.1357142857142857040, 0.1428571428571428492, 0.1499999999999999944, 0.1571428571428571397, 0.1642857142857142849, 0.1714285714285714302, 0.1785714285714285754, 0.1857142857142857206, 0.1928571428571428659, 0.2000000000000000111, 0.2071428571428571841, 0.2142857142857142738, 0.2214285714285714191, 0.2285714285714285643, 0.2357142857142857373, 0.2428571428571428548, 0.2500000000000000000, 0.2571428571428571175, 0.2642857142857142905, 0.2714285714285714080, 0.2785714285714285254, 0.2857142857142856984, 0.2928571428571428714, 0.2999999999999999889, 0.3071428571428571619, 0.3142857142857142794, 0.3214285714285714524, 0.3285714285714285698, 0.3357142857142856318, 0.3428571428571428603, 0.3499999999999999778, 0.3571428571428571508, 0.3642857142857142683, 0.3714285714285714413, 0.3785714285714285587, 0.3857142857142857317, 0.3928571428571428492, 0.4000000000000000222, 0.4071428571428571397, 0.4142857142857143682, 0.4214285714285714302, 0.4285714285714285476, 0.4357142857142857206, 0.4428571428571428381, 0.4500000000000000111, 0.4571428571428571286, 0.4642857142857143016, 0.4714285714285714746, 0.4785714285714285920, 0.4857142857142857095, 0.4928571428571428825, 0.5000000000000000000, 0.5071428571428571175, 0.5142857142857142350, 0.5214285714285714635, 0.5285714285714285809, 0.5357142857142856984, 0.5428571428571428159, 0.5500000000000000444, 0.5571428571428570509, 0.5642857142857142794, 0.5714285714285713969, 0.5785714285714286254, 0.5857142857142857428, 0.5928571428571428603, 0.5999999999999999778, 0.6071428571428570953, 0.6142857142857143238, 0.6214285714285714413, 0.6285714285714285587, 0.6357142857142856762, 0.6428571428571429047, 0.6500000000000000222, 0.6571428571428571397, 0.6642857142857142572, 0.6714285714285712636, 0.6785714285714286031, 0.6857142857142857206, 0.6928571428571428381, 0.6999999999999999556, 0.7071428571428571841, 0.7142857142857143016, 0.7214285714285714191, 0.7285714285714285365, 0.7357142857142857650, 0.7428571428571428825, 0.7500000000000001110, 0.7571428571428571175, 0.7642857142857142350, 0.7714285714285714635, 0.7785714285714285809, 0.7857142857142856984, 0.7928571428571428159, 0.8000000000000000444, 0.8071428571428571619, 0.8142857142857142794, 0.8214285714285713969, 0.8285714285714287364, 0.8357142857142857428, 0.8428571428571428603, 0.8499999999999999778, 0.8571428571428570953, 0.8642857142857143238, 0.8714285714285714413, 0.8785714285714285587, 0.8857142857142856762, 0.8928571428571429047, 0.9000000000000000222, 0.9071428571428571397, 0.9142857142857142572, 0.9214285714285713746, 0.9285714285714286031, 0.9357142857142857206, 0.9428571428571429491, 0.9499999999999999556, 0.9523897199067098418 ),
 .UNSPECIFIED. ) 
 CURVE ( )  GEOMETRIC_REPRESENTATION_ITEM ( )  RATIONAL_B_SPLINE_CURVE ( ( 1.000000000000000000, 0.9510565162951535312, 1.000000000000000000, 0.9510565162951535312, 1.000000000000000000, 0.9510565162951535312, 1.000000000000000000, 0.9510565162951535312, 1.000000000000000000, 0.9510565162951535312, 1.000000000000000000, 0.9510565162951535312, 1.000000000000000000, 0.9510565162951535312, 1.000000000000000000, 0.9510565162951535312, 1.000000000000000000, 0.9510565162951535312, 1.000000000000000000, 0.9510565162951535312, 1.000000000000000000, 0.9510565162951535312, 1.000000000000000000, 0.9510565162951535312, 1.000000000000000000, 0.9510565162951535312, 1.000000000000000000, 0.9510565162951535312, 1.000000000000000000, 0.9510565162951535312, 1.000000000000000000, 0.9510565162951535312, 1.000000000000000000, 0.9510565162951535312, 1.000000000000000000, 0.9510565162951535312, 1.000000000000000000, 0.9510565162951535312, 1.000000000000000000, 0.9510565162951535312, 1.000000000000000000, 0.9510565162951535312, 1.000000000000000000, 0.9510565162951535312, 1.000000000000000000, 0.9510565162951535312, 1.000000000000000000, 0.9510565162951535312, 1.000000000000000000, 0.9510565162951535312, 1.000000000000000000, 0.9510565162951535312, 1.000000000000000000, 0.9510565162951535312, 1.000000000000000000, 0.9510565162951535312, 1.000000000000000000, 0.9510565162951535312, 1.000000000000000000, 0.9510565162951535312, 1.000000000000000000, 0.9510565162951535312, 1.000000000000000000, 0.9510565162951535312, 1.000000000000000000, 0.9510565162951535312, 1.000000000000000000, 0.9510565162951535312, 1.000000000000000000, 0.9510565162951535312, 1.000000000000000000, 0.9510565162951535312, 1.000000000000000000, 0.9510565162951535312, 1.000000000000000000, 0.9510565162951535312, 1.000000000000000000, 0.9510565162951535312, 1.000000000000000000, 0.9510565162951535312, 1.000000000000000000, 0.9510565162951535312, 1.000000000000000000, 0.9510565162951535312, 1.000000000000000000, 0.9510565162951535312, 1.000000000000000000, 0.9510565162951535312, 1.000000000000000000, 0.9510565162951535312, 1.000000000000000000, 0.9510565162951535312, 1.000000000000000000, 0.9510565162951535312, 1.000000000000000000, 0.9510565162951535312, 1.000000000000000000, 0.9510565162951535312, 1.000000000000000000, 0.9510565162951535312, 1.000000000000000000, 0.9510565162951535312, 1.000000000000000000, 0.9510565162951535312, 1.000000000000000000, 0.9510565162951535312, 1.000000000000000000, 0.9510565162951535312, 1.000000000000000000, 0.9510565162951535312, 1.000000000000000000, 0.9510565162951535312, 1.000000000000000000, 0.9510565162951535312, 1.000000000000000000, 0.9510565162951535312, 1.000000000000000000, 0.9510565162951535312, 1.000000000000000000, 0.9510565162951535312, 1.000000000000000000, 0.9510565162951535312, 1.000000000000000000, 0.9510565162951535312, 1.000000000000000000, 0.9510565162951535312, 1.000000000000000000, 0.9510565162951535312, 1.000000000000000000, 0.9510565162951535312, 1.000000000000000000, 0.9510565162951535312, 1.000000000000000000, 0.9510565162951535312, 1.000000000000000000, 0.9510565162951535312, 1.000000000000000000, 0.9510565162951535312, 1.000000000000000000, 0.9510565162951535312, 1.000000000000000000, 0.9510565162951535312, 1.000000000000000000, 0.9510565162951535312, 1.000000000000000000, 0.9510565162951535312, 1.000000000000000000, 0.9510565162951535312, 1.000000000000000000, 0.9510565162951535312, 1.000000000000000000, 0.9510565162951535312, 1.000000000000000000, 0.9510565162951535312, 1.000000000000000000, 0.9510565162951535312, 1.000000000000000000, 0.9510565162951535312, 1.000000000000000000, 0.9510565162951535312, 1.000000000000000000, 0.9510565162951535312, 1.000000000000000000, 0.9510565162951535312, 1.000000000000000000, 0.9510565162951535312, 1.000000000000000000, 0.9510565162951535312, 1.000000000000000000, 0.9510565162951535312, 1.000000000000000000, 0.9510565162951535312, 1.000000000000000000, 0.9510565162951535312, 1.000000000000000000, 0.9510565162951535312, 1.000000000000000000, 0.9510565162951535312, 1.000000000000000000, 0.9510565162951535312, 1.000000000000000000, 0.9510565162951535312, 1.000000000000000000, 0.9510565162951535312, 1.000000000000000000, 0.9510565162951535312, 1.000000000000000000, 0.9510565162951535312, 1.000000000000000000, 0.9510565162951535312, 1.000000000000000000, 0.9510565162951535312, 1.000000000000000000, 0.9510565162951535312, 1.000000000000000000, 0.9510565162951535312, 1.000000000000000000, 0.9510565162951535312, 1.000000000000000000, 0.9510565162951535312, 1.000000000000000000, 0.9510565162951535312, 1.000000000000000000, 0.9510565162951535312, 1.000000000000000000, 0.9510565162951535312, 1.000000000000000000, 0.9510565162951535312, 1.000000000000000000, 0.9510565162951535312, 1.000000000000000000, 0.9510565162951535312, 1.000000000000000000, 0.9510565162951535312, 1.000000000000000000, 0.9510565162951535312, 1.000000000000000000, 0.9510565162951535312, 1.000000000000000000, 0.9510565162951535312, 1.000000000000000000, 0.9510565162951535312, 1.000000000000000000, 0.9510565162951535312, 1.000000000000000000, 0.9510565162951535312, 1.000000000000000000, 0.9510565162951535312, 1.000000000000000000, 0.9510565162951535312, 1.000000000000000000, 0.9510565162951535312, 1.000000000000000000, 0.9510565162951535312, 1.000000000000000000, 0.9510565162951535312, 1.000000000000000000, 0.9510565162951535312, 1.000000000000000000, 0.9510565162951535312, 1.000000000000000000, 0.9510565162951535312, 1.000000000000000000, 0.9510565162951535312, 1.000000000000000000, 0.9510565162951535312, 1.000000000000000000, 0.9510565162951535312, 1.000000000000000000, 0.9510565162951535312, 1.000000000000000000, 0.9510565162951535312, 1.000000000000000000, 0.9510565162951535312, 1.000000000000000000, 0.9510565162951535312, 1.000000000000000000, 0.9510565162951535312, 1.000000000000000000, 0.9510565162951535312, 1.000000000000000000, 0.9510565162951535312, 1.000000000000000000, 0.9510565162951535312, 1.000000000000000000, 0.9510565162951535312, 1.000000000000000000, 0.9836254295761526212, 0.9782074374858980015 ) ) 
 REPRESENTATION_ITEM ( '' )  );
#19969=CARTESIAN_POINT ( 'NONE',  ( -160.8964159109769696, -161.3084106276440082, 46.59394152635518793 ) ) ;
#19971=FACE_OUTER_BOUND ( 'NONE', #20568, .T. ) ;
#19991=CARTESIAN_POINT ( 'NONE',  ( -159.5594255724347761, -185.7891397928654840, 43.77915905869157598 ) ) ;
#19994=CARTESIAN_POINT ( 'NONE',  ( -142.0420953463935803, -195.5084106276440536, 46.59394152635518793 ) ) ;
#19997=CARTESIAN_POINT ( 'NONE',  ( -142.0420953463935803, -189.8084106276440366, 52.72008163687743831 ) ) ;
#20015=CARTESIAN_POINT ( 'NONE',  ( -151.4692556286852891, -181.7391397928654726, 59.65701158161631668 ) ) ;
#20016=CARTESIAN_POINT ( 'NONE',  ( -141.4692556286852891, -183.8391397928654669, 46.40781461928724383 ) ) ;
#20019=CARTESIAN_POINT ( 'NONE',  ( -154.3824083646099439, -193.2938272943107449, 58.62277379824867296 ) ) ;
#20023=CARTESIAN_POINT ( 'NONE',  ( -143.8425227516148084, -186.6938272943107222, 55.19815736654470584 ) ) ;
#20043=CARTESIAN_POINT ( 'NONE',  ( -142.0420953463935803, -159.5438272943107449, 52.72008163687743831 ) ) ;
#20045=CARTESIAN_POINT ( 'NONE',  ( -157.6495955161842062, -178.1130981290893374, 58.16351966513671812 ) ) ;
#20062=CYLINDRICAL_SURFACE ( 'NONE', #8783, 10.00000000000000888 ) ;
#20063=ADVANCED_FACE ( 'NONE', ( #1908 ), #17324, .T. ) ;
#20067=CARTESIAN_POINT ( 'NONE',  ( -143.8425227516148084, -168.9584106276440423, 55.19815736654470584 ) ) ;
#20068=CARTESIAN_POINT ( 'NONE',  ( -145.6429501568359797, -185.9438272943107506, 41.63779006702063867 ) ) ;
#20069=CARTESIAN_POINT ( 'NONE',  ( -159.5594255724347761, -166.8630981290893089, 43.77915905869157598 ) ) ;
#20078=CARTESIAN_POINT ( 'NONE',  ( -142.0420953463936087, -159.3938272943107393, 49.65701158161630957 ) ) ;
#20079=CARTESIAN_POINT ( 'NONE',  ( -145.6429501568359797, -177.2084106276440707, 41.63779006702063867 ) ) ;
#20082=CARTESIAN_POINT ( 'NONE',  ( -145.6429501568359797, -159.2084106276439854, 41.63779006702063867 ) ) ;
#20088=ORIENTED_EDGE ( 'NONE', *, *, #14863, .F. ) ;
#20089=CARTESIAN_POINT ( 'NONE',  ( -151.4692556286852607, -161.3130981290892976, 39.65701158161629536 ) ) ;
#20105=CARTESIAN_POINT ( 'NONE',  ( -159.0959885057557983, -184.8584106276440480, 55.19815736654470584 ) ) ;
#20107=CARTESIAN_POINT ( 'NONE',  ( -143.8425227516148084, -177.9584106276440707, 55.19815736654470584 ) ) ;
#20110=CARTESIAN_POINT ( 'NONE',  ( -149.8854112254399240, -159.3160212151857422, 39.65701158161629536 ) ) ;
#20122=FACE_OUTER_BOUND ( 'NONE', #10887, .T. ) ;
#20123=CARTESIAN_POINT ( 'NONE',  ( -141.4692556286852891, -178.1391397928654499, 52.90620854394536821 ) ) ;
#20129=CARTESIAN_POINT ( 'NONE',  ( -148.5561028927606344, -176.7938272943107165, 40.69124936498395328 ) ) ;
#20132=ORIENTED_EDGE ( 'NONE', *, *, #11482, .T. ) ;
#20133=CARTESIAN_POINT ( 'NONE',  ( -145.2889157411863437, -190.4391397928654612, 58.16351966513671812 ) ) ;
#20147=CARTESIAN_POINT ( 'NONE',  ( -148.5561028927606344, -162.9938272943107336, 58.62277379824867296 ) ) ;
#20149=CARTESIAN_POINT ( 'NONE',  ( -161.4692556286853176, -169.5630981290893260, 49.65701158161630957 ) ) ;
#20156=CARTESIAN_POINT ( 'NONE',  ( -151.4692556286852891, -196.9891397928655010, 39.65701158161630246 ) ) ;
#20157=VECTOR ( 'NONE', #14203, 1000.000000000000114 ) ;
#20158=AXIS2_PLACEMENT_3D ( 'NONE', #2199, #14089, #10478 ) ;
#20162=DIRECTION ( 'NONE',  ( -0.000000000000000000, 1.000000000000000000, -0.000000000000000000 ) ) ;
#20174=CARTESIAN_POINT ( 'NONE',  ( -142.0420953463935803, -156.5084106276439968, 46.59394152635518793 ) ) ;
#20175=CARTESIAN_POINT ( 'NONE',  ( -159.0959885057557983, -193.5938272943107279, 55.19815736654470584 ) ) ;
#20177=CARTESIAN_POINT ( 'NONE',  ( -143.3790856849358306, -177.3630981290893089, 55.53486410454105027 ) ) ;
#20183=CARTESIAN_POINT ( 'NONE',  ( -160.8964159109769696, -160.8938272943107393, 49.65701158161630957 ) ) ;
#20184=CARTESIAN_POINT ( 'NONE',  ( -143.8425227516148084, -171.9584106276440423, 55.19815736654470584 ) ) ;
#20187=CARTESIAN_POINT ( 'NONE',  ( -145.6429501568359797, -162.2084106276440707, 41.63779006702063867 ) ) ;
#20190=ORIENTED_EDGE ( 'NONE', *, *, #21595, .T. ) ;
#20208=CARTESIAN_POINT ( 'NONE',  ( -148.5561028927606344, -183.0584106276440650, 40.69124936498395328 ) ) ;
#20211=CARTESIAN_POINT ( 'NONE',  ( -143.8425227516148084, -174.9584106276440707, 55.19815736654470584 ) ) ;
#20226=CARTESIAN_POINT ( 'NONE',  ( -143.9637021292201950, -126.9891397928655010, 62.65701158161630957 ) ) ;
#20228=CARTESIAN_POINT ( 'NONE',  ( -145.2889157411863721, -181.4391397928654612, 58.16351966513671812 ) ) ;
#20235=CARTESIAN_POINT ( 'NONE',  ( -160.8964159109769696, -169.7438272943106767, 52.72008163687743121 ) ) ;
#20251=CARTESIAN_POINT ( 'NONE',  ( -161.4692556286852891, -169.4130981290893203, 52.90620854394536821 ) ) ;
#20252=CARTESIAN_POINT ( 'NONE',  ( -145.2889157411863437, -173.6130981290893089, 41.15050349809589392 ) ) ;
#20254=CARTESIAN_POINT ( 'NONE',  ( -145.2889157411863721, -170.6130981290892805, 41.15050349809590102 ) ) ;
#20265=CARTESIAN_POINT ( 'NONE',  ( -143.3790856849358306, -185.7630981290893146, 43.77915905869157598 ) ) ;
#20275=CARTESIAN_POINT ( 'NONE',  ( -143.8425227516148084, -159.9584106276440423, 55.19815736654470584 ) ) ;
#20276=CARTESIAN_POINT ( 'NONE',  ( -160.8964159109769696, -190.8938272943107393, 49.65701158161630957 ) ) ;
#20279=CARTESIAN_POINT ( 'NONE',  ( -148.3790856849358306, -177.6630981290893203, 59.16757674456786020 ) ) ;
#20286=CARTESIAN_POINT ( 'NONE',  ( -160.8964159109769696, -163.8938272943107393, 49.65701158161630957 ) ) ;
#20287=CARTESIAN_POINT ( 'NONE',  ( -142.0420953463935803, -174.5084106276440252, 46.59394152635518083 ) ) ;
#20289=CARTESIAN_POINT ( 'NONE',  ( -143.8425227516148084, -162.9584106276440423, 55.19815736654470584 ) ) ;
#20310=CYLINDRICAL_SURFACE ( 'NONE', #6047, 10.00000000000000888 ) ;
#20313=CARTESIAN_POINT ( 'NONE',  ( -157.2955611005346270, -188.6084106276440764, 41.63779006702063867 ) ) ;
#20316=CARTESIAN_POINT ( 'NONE',  ( -160.8964159109769696, -176.0084106276440536, 52.72008163687743121 ) ) ;
#20333=DIRECTION ( 'NONE',  ( -0.000000000000000000, 1.000000000000000000, -0.000000000000000000 ) ) ;
#20334=CARTESIAN_POINT ( 'NONE',  ( -157.6495955161842062, -179.9391397928654328, 41.15050349809590102 ) ) ;
#20335=CARTESIAN_POINT ( 'NONE',  ( -153.0531000319306827, -182.2362167067690564, 39.65701158161630957 ) ) ;
#20341=CARTESIAN_POINT ( 'NONE',  ( -151.4692556286852891, -172.1438272943107108, 59.56931450028537967 ) ) ;
#20343=CARTESIAN_POINT ( 'NONE',  ( -151.4692556286852607, -171.2391397928654726, 39.65701158161629536 ) ) ;
#20360=CARTESIAN_POINT ( 'NONE',  ( -141.4692556286852891, -164.9130981290892919, 46.40781461928724383 ) ) ;
#20381=CARTESIAN_POINT ( 'NONE',  ( -142.0420953463935803, -162.5084106276440536, 46.59394152635518793 ) ) ;
#20382=CARTESIAN_POINT ( 'NONE',  ( -160.8964159109769696, -181.7438272943107336, 52.72008163687743121 ) ) ;
#20384=CARTESIAN_POINT ( 'NONE',  ( -159.5594255724347761, -193.8630981290893089, 43.77915905869157598 ) ) ;
#20386=CARTESIAN_POINT ( 'NONE',  ( -161.4692556286852891, -173.6391397928654499, 46.40781461928724383 ) ) ;
#20392=CARTESIAN_POINT ( 'NONE',  ( -159.0959885057557983, -175.8584106276440480, 55.19815736654470584 ) ) ;
#20393=VECTOR ( 'NONE', #17265, 1000.000000000000114 ) ;
#20395=CARTESIAN_POINT ( 'NONE',  ( -142.0420953463935803, -159.8084106276440934, 52.72008163687743831 ) ) ;
#20400=ORIENTED_EDGE ( 'NONE', *, *, #16894, .F. ) ;
#20416=CARTESIAN_POINT ( 'NONE',  ( -157.2955611005346270, -182.3438272943106995, 41.63779006702063867 ) ) ;
#20419=CARTESIAN_POINT ( 'NONE',  ( -148.5561028927606344, -184.2584106276440536, 58.62277379824867296 ) ) ;
#20421=CARTESIAN_POINT ( 'NONE',  ( -154.3824083646099439, -179.7584106276440536, 40.69124936498395328 ) ) ;
#20422=ORIENTED_EDGE ( 'NONE', *, *, #14698, .T. ) ;
#20440=CARTESIAN_POINT ( 'NONE',  ( -145.2889157411863721, -168.5391397928654840, 41.15050349809590102 ) ) ;
#20447=CARTESIAN_POINT ( 'NONE',  ( -142.0420953463935803, -177.2438272943107620, 46.59394152635518793 ) ) ;
#20450=CARTESIAN_POINT ( 'NONE',  ( -161.4692556286852891, -158.3391397928654385, 52.90620854394536821 ) ) ;
#20466=CARTESIAN_POINT ( 'NONE',  ( -151.4692556286852891, -155.6438272943107393, 39.74470866294723947 ) ) ;
#20468=CARTESIAN_POINT ( 'NONE',  ( -151.4692556286852891, -170.3130981290892692, 39.14238933923362396 ) ) ;
#20470=CARTESIAN_POINT ( 'NONE',  ( -154.5594255724347761, -190.8891397928654783, 59.16757674456785310 ) ) ;
#20476=CARTESIAN_POINT ( 'NONE',  ( -151.4692556286853176, -180.2391397928654726, 39.65701158161629536 ) ) ;
#20478=( BOUNDED_CURVE ( )  B_SPLINE_CURVE ( 2, ( #21785, #11958, #16695, #20133, #11627, #11736, #18357, #18689, #6692, #17128, #6903, #3696, #18793 ),
 .UNSPECIFIED., .F., .T. ) 
 B_SPLINE_CURVE_WITH_KNOTS ( ( 3, 2, 2, 2, 2, 2, 3 ),
 ( 0.1249999999999999584, 0.1285714285714285587, 0.1357142857142857040, 0.1428571428571428492, 0.1499999999999999944, 0.1571428571428571397, 0.1607142857142856707 ),
 .UNSPECIFIED. ) 
 CURVE ( )  GEOMETRIC_REPRESENTATION_ITEM ( )  RATIONAL_B_SPLINE_CURVE ( ( 0.9755282581475768211, 0.9755282581475765991, 1.000000000000000000, 0.9510565162951535312, 1.000000000000000000, 0.9510565162951535312, 1.000000000000000000, 0.9510565162951535312, 1.000000000000000000, 0.9510565162951535312, 1.000000000000000000, 0.9755282581475770431, 0.9755282581475765991 ) ) 
 REPRESENTATION_ITEM ( '' )  );
#20481=CARTESIAN_POINT ( 'NONE',  ( -151.4692556286852607, -156.8130981290892692, 59.65701158161632378 ) ) ;
#20492=CARTESIAN_POINT ( 'NONE',  ( -154.3824083646099439, -160.5584106276440366, 58.62277379824867296 ) ) ;
#20493=CARTESIAN_POINT ( 'NONE',  ( -154.3824083646099439, -179.4938272943107336, 40.69124936498395328 ) ) ;
#20494=CARTESIAN_POINT ( 'NONE',  ( -148.3790856849358306, -177.3891397928654783, 40.14644641866477315 ) ) ;
#20498=CARTESIAN_POINT ( 'NONE',  ( -161.4692556286852891, -173.3391397928654385, 52.90620854394536821 ) ) ;
#20505=CARTESIAN_POINT ( 'NONE',  ( -145.6429501568359797, -162.2084106276440423, 41.63779006702063867 ) ) ;
#20510=VERTEX_POINT ( 'NONE', #5162 ) ;
#20511=CARTESIAN_POINT ( 'NONE',  ( -157.6495955161842062, -179.9391397928654328, 41.15050349809589392 ) ) ;
#20525=CARTESIAN_POINT ( 'NONE',  ( -145.6429501568359797, -182.9438272943106938, 41.63779006702063867 ) ) ;
#20529=CARTESIAN_POINT ( 'NONE',  ( -142.0420953463935803, -189.8084106276440366, 52.72008163687743831 ) ) ;
#20534=ADVANCED_FACE ( 'NONE', ( #5273 ), #20062, .T. ) ;
#20543=CARTESIAN_POINT ( 'NONE',  ( -151.4692556286852891, -196.9891397928655010, 39.65701158161630246 ) ) ;
#20548=CARTESIAN_POINT ( 'NONE',  ( -145.2889157411863437, -179.6130981290892521, 41.15050349809589392 ) ) ;
#20549=CARTESIAN_POINT ( 'NONE',  ( -141.4692556286852891, -168.8391397928654385, 46.40781461928724383 ) ) ;
#20550=DIRECTION ( 'NONE',  ( 0.000000000000000000, 0.000000000000000000, 1.000000000000000000 ) ) ;
#20557=CARTESIAN_POINT ( 'NONE',  ( -160.8964159109769696, -175.8938272943107393, 49.65701158161630957 ) ) ;
#20568=EDGE_LOOP ( 'NONE', ( #9823, #15361, #14686, #16438 ) ) ;
#20573=CARTESIAN_POINT ( 'NONE',  ( -145.6429501568359797, -156.8438272943107279, 57.67623309621197336 ) ) ;
#20575=CARTESIAN_POINT ( 'NONE',  ( -143.3790856849358306, -170.7630981290892862, 43.77915905869157598 ) ) ;
#20576=EDGE_CURVE ( 'NONE', #19216, #8279, #6725, .T. ) ;
#20580=CARTESIAN_POINT ( 'NONE',  ( -145.2889157411863437, -184.4391397928654328, 58.16351966513671812 ) ) ;
#20592=CARTESIAN_POINT ( 'NONE',  ( -143.3790856849358306, -164.7630981290893146, 43.77915905869157598 ) ) ;
#20596=CARTESIAN_POINT ( 'NONE',  ( -151.4692556286852891, -195.2391397928654726, 39.14238933923362396 ) ) ;
#20598=CARTESIAN_POINT ( 'NONE',  ( -157.2955611005345986, -182.3438272943106995, 41.63779006702063867 ) ) ;
#20609=CARTESIAN_POINT ( 'NONE',  ( -142.0420953463936087, -168.6584106276440593, 49.65701158161630957 ) ) ;
#20625=CARTESIAN_POINT ( 'NONE',  ( -141.4692556286852891, -195.0630981290893260, 49.65701158161630957 ) ) ;
#20632=CARTESIAN_POINT ( 'NONE',  ( -142.0420953463935803, -183.5438272943107449, 52.72008163687743831 ) ) ;
#20633=CARTESIAN_POINT ( 'NONE',  ( -160.8964159109769696, -191.3084106276440650, 46.59394152635518083 ) ) ;
#20635=EDGE_CURVE ( 'NONE', #7574, #13720, #15324, .T. ) ;
#20636=CARTESIAN_POINT ( 'NONE',  ( -151.4692556286852891, -176.9084106276440309, 39.74470866294723947 ) ) ;
#20638=ORIENTED_EDGE ( 'NONE', *, *, #15368, .T. ) ;
#20645=AXIS2_PLACEMENT_3D ( 'NONE', #5271, #13639, #14255 ) ;
#20650=EDGE_CURVE ( 'NONE', #8279, #6960, #15832, .T. ) ;
#20654=CARTESIAN_POINT ( 'NONE',  ( -141.4692556286852891, -171.9891397928654726, 49.65701158161630957 ) ) ;
#20658=CARTESIAN_POINT ( 'NONE',  ( -151.4692556286852891, -195.9891397928654726, 39.65701158161630246 ) ) ;
#20662=CARTESIAN_POINT ( 'NONE',  ( -157.2955611005346270, -166.4438272943107506, 57.67623309621198047 ) ) ;
#20683=CARTESIAN_POINT ( 'NONE',  ( -159.5594255724347761, -163.8630981290893089, 43.77915905869157598 ) ) ;
#20684=CARTESIAN_POINT ( 'NONE',  ( -157.6495955161842062, -191.0391397928654271, 58.16351966513671812 ) ) ;
#20706=CARTESIAN_POINT ( 'NONE',  ( -142.0420953463936087, -183.3938272943107108, 49.65701158161630957 ) ) ;
#20715=CARTESIAN_POINT ( 'NONE',  ( -143.8425227516148084, -156.0938272943107279, 44.11586579668791330 ) ) ;
#20716=CARTESIAN_POINT ( 'NONE',  ( -160.8964159109769696, -167.1584106276440593, 49.65701158161630957 ) ) ;
#20717=CARTESIAN_POINT ( 'NONE',  ( -157.6495955161842062, -164.9391397928654612, 41.15050349809589392 ) ) ;
#20723=EDGE_CURVE ( 'NONE', #19662, #16205, #849, .T. ) ;
#20724=CARTESIAN_POINT ( 'NONE',  ( -154.5594255724347761, -178.8891397928654783, 59.16757674456785310 ) ) ;
#20734=CARTESIAN_POINT ( 'NONE',  ( -159.5594255724347761, -172.8630981290893089, 43.77915905869157598 ) ) ;
#20738=CARTESIAN_POINT ( 'NONE',  ( -142.0420953463936087, -183.3938272943107108, 49.65701158161630957 ) ) ;
#20739=CARTESIAN_POINT ( 'NONE',  ( -157.2955611005345986, -190.7084106276440423, 57.67623309621197336 ) ) ;
#20741=CARTESIAN_POINT ( 'NONE',  ( -142.0420953463935803, -180.8084106276440366, 52.72008163687743831 ) ) ;
#20748=EDGE_CURVE ( 'NONE', #18561, #18469, #3838, .T. ) ;
#20759=CARTESIAN_POINT ( 'NONE',  ( -143.3790856849358306, -172.2891397928654840, 55.53486410454105027 ) ) ;
#20767=CARTESIAN_POINT ( 'NONE',  ( -160.8964159109769696, -166.8938272943107393, 49.65701158161630957 ) ) ;
#20771=VERTEX_POINT ( 'NONE', #2075 ) ;
#20772=CARTESIAN_POINT ( 'NONE',  ( -161.4692556286852891, -175.4130981290893203, 52.90620854394536821 ) ) ;
#20780=AXIS2_PLACEMENT_3D ( 'NONE', #4856, #6636, #11575 ) ;
#20788=CARTESIAN_POINT ( 'NONE',  ( -148.3790856849358306, -156.6630981290892919, 59.16757674456786020 ) ) ;
#20794=CARTESIAN_POINT ( 'NONE',  ( -142.0420953463935803, -195.2438272943107336, 46.59394152635518793 ) ) ;
#20796=CARTESIAN_POINT ( 'NONE',  ( -141.4692556286852891, -162.2130981290893033, 52.90620854394536821 ) ) ;
#20797=ORIENTED_EDGE ( 'NONE', *, *, #18850, .T. ) ;
#20799=EDGE_CURVE ( 'NONE', #1989, #21208, #7859, .T. ) ;
#20814=CARTESIAN_POINT ( 'NONE',  ( -145.6429501568359797, -183.8438272943107279, 57.67623309621197336 ) ) ;
#20816=CARTESIAN_POINT ( 'NONE',  ( -145.2889157411863721, -185.6130981290892805, 41.15050349809590102 ) ) ;
#20818=CARTESIAN_POINT ( 'NONE',  ( -141.4692556286852891, -163.1391397928654783, 52.90620854394536821 ) ) ;
#20822=CARTESIAN_POINT ( 'NONE',  ( -155.3247640818418063, -155.4453048272798412, 40.99743929837026712 ) ) ;
#20823=CARTESIAN_POINT ( 'NONE',  ( -160.8964159109769696, -170.1584106276440593, 49.65701158161630957 ) ) ;
#20840=CARTESIAN_POINT ( 'NONE',  ( -161.4692556286852891, -157.4130981290893203, 52.90620854394536821 ) ) ;
#20847=CARTESIAN_POINT ( 'NONE',  ( -143.8425227516148084, -177.6938272943107506, 55.19815736654470584 ) ) ;
#20849=ORIENTED_EDGE ( 'NONE', *, *, #12606, .T. ) ;
#20850=CARTESIAN_POINT ( 'NONE',  ( -143.8425227516148084, -174.9584106276440707, 55.19815736654470584 ) ) ;
#20852=CARTESIAN_POINT ( 'NONE',  ( -151.4692556286852891, -196.9891397928655010, 49.65701158161630957 ) ) ;
#20856=VERTEX_POINT ( 'NONE', #18136 ) ;
#20867=CARTESIAN_POINT ( 'NONE',  ( -149.8854112254399240, -180.7362167067690280, 59.65701158161632378 ) ) ;
#20868=CARTESIAN_POINT ( 'NONE',  ( -148.3790856849358306, -172.5891397928654669, 59.16757674456786020 ) ) ;
#20869=CARTESIAN_POINT ( 'NONE',  ( -151.4692556286852607, -161.3130981290892976, 39.65701158161629536 ) ) ;
#20875=CARTESIAN_POINT ( 'NONE',  ( -157.2955611005346270, -164.3438272943107279, 41.63779006702063867 ) ) ;
#20878=CARTESIAN_POINT ( 'NONE',  ( -143.8425227516148084, -192.3584106276440480, 44.11586579668791330 ) ) ;
#20880=CARTESIAN_POINT ( 'NONE',  ( -157.6495955161842062, -176.0130981290893146, 41.15050349809589392 ) ) ;
#20896=CARTESIAN_POINT ( 'NONE',  ( -157.6495955161842062, -160.1130981290893089, 58.16351966513671812 ) ) ;
#20898=DIRECTION ( 'NONE',  ( -0.000000000000000000, 1.000000000000000000, -0.000000000000000000 ) ) ;
#20904=CARTESIAN_POINT ( 'NONE',  ( -143.3790856849358306, -162.3630981290893089, 55.53486410454105027 ) ) ;
#20910=CARTESIAN_POINT ( 'NONE',  ( -145.2889157411863437, -168.5391397928654840, 41.15050349809589392 ) ) ;
#20922=( BOUNDED_CURVE ( )  B_SPLINE_CURVE ( 2, ( #20089, #11799, #12446, #15538, #7288, #14096, #18961, #10587, #4073, #10802, #3972, #8832, #17507 ),
 .UNSPECIFIED., .F., .F. ) 
 B_SPLINE_CURVE_WITH_KNOTS ( ( 3, 2, 2, 2, 2, 2, 3 ),
 ( 0.8035714285714286031, 0.8071428571428571619, 0.8142857142857142794, 0.8214285714285713969, 0.8285714285714286254, 0.8357142857142857428, 0.8392857142857143016 ),
 .UNSPECIFIED. ) 
 CURVE ( )  GEOMETRIC_REPRESENTATION_ITEM ( )  RATIONAL_B_SPLINE_CURVE ( ( 0.9755282581475768211, 0.9755282581475768211, 1.000000000000000000, 0.9510565162951535312, 1.000000000000000000, 0.9510565162951535312, 1.000000000000000000, 0.9510565162951535312, 1.000000000000000000, 0.9510565162951535312, 1.000000000000000000, 0.9755282581475768211, 0.9755282581475768211 ) ) 
 REPRESENTATION_ITEM ( '' )  );
#20923=CARTESIAN_POINT ( 'NONE',  ( -142.0420953463935803, -171.2438272943107052, 46.59394152635518083 ) ) ;
#20925=CARTESIAN_POINT ( 'NONE',  ( -143.3790856849358306, -186.3630981290893089, 55.53486410454105027 ) ) ;
#20934=CARTESIAN_POINT ( 'NONE',  ( -145.6429501568359797, -166.1084106276440195, 57.67623309621197336 ) ) ;
#20935=CARTESIAN_POINT ( 'NONE',  ( -153.0531000319307111, -165.1622583705451746, 39.65701158161631668 ) ) ;
#20958=CARTESIAN_POINT ( 'NONE',  ( -142.0420953463936087, -171.3938272943107393, 49.65701158161630957 ) ) ;
#20959=CARTESIAN_POINT ( 'NONE',  ( -160.8964159109769696, -191.1584106276440593, 49.65701158161630957 ) ) ;
#20960=ORIENTED_EDGE ( 'NONE', *, *, #6074, .F. ) ;
#20961=CARTESIAN_POINT ( 'NONE',  ( -143.8425227516148084, -180.3584106276440480, 44.11586579668791330 ) ) ;
#20972=ADVANCED_FACE ( 'NONE', ( #19470 ), #14610, .T. ) ;
#20978=CARTESIAN_POINT ( 'NONE',  ( -148.3790856849358306, -157.5891397928654953, 59.16757674456786020 ) ) ;
#20982=DIRECTION ( 'NONE',  ( -0.8660254037844384856, 0.000000000000000000, -0.5000000000000003331 ) ) ;
#20985=VERTEX_POINT ( 'NONE', #18028 ) ;
#20987=CARTESIAN_POINT ( 'NONE',  ( -142.0420953463936087, -168.3938272943107393, 49.65701158161630957 ) ) ;
#20989=CARTESIAN_POINT ( 'NONE',  ( -157.2955611005346270, -190.7084106276440423, 57.67623309621198047 ) ) ;
#21006=CARTESIAN_POINT ( 'NONE',  ( -159.5594255724347761, -194.1891397928654897, 55.53486410454104316 ) ) ;
#21010=CARTESIAN_POINT ( 'NONE',  ( -148.3790856849358306, -162.6630981290892919, 59.16757674456786020 ) ) ;
#21016=CARTESIAN_POINT ( 'NONE',  ( -143.8425227516148084, -189.0938272943107279, 44.11586579668791330 ) ) ;
#21025=CARTESIAN_POINT ( 'NONE',  ( -148.3790856849358306, -168.3891397928654499, 40.14644641866477315 ) ) ;
#21028=VERTEX_POINT ( 'NONE', #4694 ) ;
#21030=CARTESIAN_POINT ( 'NONE',  ( -151.4692556286852891, -196.9891397928655010, 39.65701158161630246 ) ) ;
#21035=CARTESIAN_POINT ( 'NONE',  ( -157.2955611005345986, -172.4438272943107222, 57.67623309621197336 ) ) ;
#21037=CARTESIAN_POINT ( 'NONE',  ( -143.3790856849358306, -183.3630981290893374, 55.53486410454105027 ) ) ;
#21044=CARTESIAN_POINT ( 'NONE',  ( -145.6429501568359797, -160.1084106276440480, 57.67623309621197336 ) ) ;
#21056=( BOUNDED_CURVE ( )  B_SPLINE_CURVE ( 2, ( #1099, #2854, #9165, #6155, #777, #4393, #7512, #19611, #7619, #9490, #7834, #5944, #21277 ),
 .UNSPECIFIED., .F., .T. ) 
 B_SPLINE_CURVE_WITH_KNOTS ( ( 3, 2, 2, 2, 2, 2, 3 ),
 ( 0.2678571428571428492, 0.2714285714285714080, 0.2785714285714285809, 0.2857142857142856984, 0.2928571428571428714, 0.2999999999999999889, 0.3035714285714286031 ),
 .UNSPECIFIED. ) 
 CURVE ( )  GEOMETRIC_REPRESENTATION_ITEM ( )  RATIONAL_B_SPLINE_CURVE ( ( 0.9755282581475768211, 0.9755282581475768211, 1.000000000000000000, 0.9510565162951535312, 1.000000000000000000, 0.9510565162951535312, 1.000000000000000000, 0.9510565162951535312, 1.000000000000000000, 0.9510565162951535312, 1.000000000000000000, 0.9755282581475765991, 0.9755282581475768211 ) ) 
 REPRESENTATION_ITEM ( '' )  );
#21058=CARTESIAN_POINT ( 'NONE',  ( -151.4692556286852891, -196.9891397928655010, 49.65701158161630957 ) ) ;
#21064=( LENGTH_UNIT ( ) NAMED_UNIT ( * ) SI_UNIT ( .MILLI., .METRE. ) );
#21070=CARTESIAN_POINT ( 'NONE',  ( -151.4692556286852891, -172.1438272943107108, 59.56931450028537967 ) ) ;
#21071=DIRECTION ( 'NONE',  ( -0.000000000000000000, 1.000000000000000000, -0.000000000000000000 ) ) ;
#21073=CARTESIAN_POINT ( 'NONE',  ( -145.6429501568359797, -180.2084106276440707, 41.63779006702063867 ) ) ;
#21075=ORIENTED_EDGE ( 'NONE', *, *, #4067, .F. ) ;
#21084=EDGE_CURVE ( 'NONE', #14442, #18977, #10110, .T. ) ;
#21092=CARTESIAN_POINT ( 'NONE',  ( -143.3790856849358306, -156.6891397928654612, 43.77915905869157598 ) ) ;
#21095=CARTESIAN_POINT ( 'NONE',  ( -161.4692556286852891, -163.7130981290892748, 46.40781461928724383 ) ) ;
#21098=CARTESIAN_POINT ( 'NONE',  ( -160.8964159109769696, -164.0438272943107449, 46.59394152635518793 ) ) ;
#21100=DIRECTION ( 'NONE',  ( -0.4999746373018760792, 0.000000000000000000, -0.8660400464498494433 ) ) ;
#21114=CARTESIAN_POINT ( 'NONE',  ( -159.5594255724347761, -188.1891397928654612, 55.53486410454104316 ) ) ;
#21116=DIRECTION ( 'NONE',  ( 0.000000000000000000, -1.000000000000000000, 0.000000000000000000 ) ) ;
#21117=CARTESIAN_POINT ( 'NONE',  ( -154.5594255724347761, -158.1630981290892919, 40.14644641866476604 ) ) ;
#21118=SHAPE_DEFINITION_REPRESENTATION ( #12013, #8609 ) ;
#21124=CARTESIAN_POINT ( 'NONE',  ( -151.4692556286853176, -162.8130981290893260, 59.65701158161632378 ) ) ;
#21133=ORIENTED_EDGE ( 'NONE', *, *, #7576, .T. ) ;
#21139=CARTESIAN_POINT ( 'NONE',  ( -151.4692556286852891, -173.6438272943107108, 39.74470866294723947 ) ) ;
#21141=CARTESIAN_POINT ( 'NONE',  ( -143.3790856849358306, -192.3630981290893089, 55.53486410454105027 ) ) ;
#21143=CARTESIAN_POINT ( 'NONE',  ( -148.3790856849358306, -162.3891397928654499, 40.14644641866477315 ) ) ;
#21149=CARTESIAN_POINT ( 'NONE',  ( -154.3824083646099439, -158.7584106276440536, 40.69124936498395328 ) ) ;
#21151=CARTESIAN_POINT ( 'NONE',  ( -154.5594255724347761, -156.0891397928654953, 40.14644641866476604 ) ) ;
#21156=CARTESIAN_POINT ( 'NONE',  ( -151.4692556286852891, -196.9891397928655010, 59.65701158161632378 ) ) ;
#21171=CARTESIAN_POINT ( 'NONE',  ( -160.8964159109769696, -166.7438272943107336, 52.72008163687743121 ) ) ;
#21172=CARTESIAN_POINT ( 'NONE',  ( -145.6429501568359797, -186.2084106276440423, 41.63779006702063867 ) ) ;
#21174=CARTESIAN_POINT ( 'NONE',  ( -160.8964159109769696, -170.0084106276440252, 52.72008163687743121 ) ) ;
#21181=ORIENTED_EDGE ( 'NONE', *, *, #3207, .T. ) ;
#21189=AXIS2_PLACEMENT_3D ( 'NONE', #1839, #13619, #10003 ) ;
#21196=CARTESIAN_POINT ( 'NONE',  ( -154.5594255724347761, -162.0891397928654669, 40.14644641866476604 ) ) ;
#21203=CARTESIAN_POINT ( 'NONE',  ( -157.2955611005346270, -194.6084106276440195, 41.63779006702063867 ) ) ;
#21204=ADVANCED_FACE ( 'NONE', ( #1728 ), #1835, .T. ) ;
#21206=PLANE ( 'NONE',  #15720 ) ;
#21208=VERTEX_POINT ( 'NONE', #13300 ) ;
#21209=CARTESIAN_POINT ( 'NONE',  ( -161.4692556286852891, -161.3391397928654669, 52.90620854394536821 ) ) ;
#21213=VERTEX_POINT ( 'NONE', #8671 ) ;
#21217=DIRECTION ( 'NONE',  ( -0.000000000000000000, 1.000000000000000000, -0.000000000000000000 ) ) ;
#21224=CARTESIAN_POINT ( 'NONE',  ( -161.4692556286853176, -185.4891397928654726, 49.65701158161630957 ) ) ;
#21227=CARTESIAN_POINT ( 'NONE',  ( -160.8964159109769696, -187.8938272943107393, 49.65701158161630957 ) ) ;
#21233=CARTESIAN_POINT ( 'NONE',  ( -160.8964159109769696, -194.0438272943107165, 46.59394152635518793 ) ) ;
#21246=( BOUNDED_CURVE ( )  B_SPLINE_CURVE ( 2, ( #21499, #19837, #3080, #18174, #21610, #16513, #3305, #5068, #2968, #9707, #1318, #9924, #13115 ),
 .UNSPECIFIED., .F., .F. ) 
 B_SPLINE_CURVE_WITH_KNOTS ( ( 3, 2, 2, 2, 2, 2, 3 ),
 ( 0.4821428571428571508, 0.4857142857142857095, 0.4928571428571428825, 0.5000000000000000000, 0.5071428571428571175, 0.5142857142857142350, 0.5178571428571429047 ),
 .UNSPECIFIED. ) 
 CURVE ( )  GEOMETRIC_REPRESENTATION_ITEM ( )  RATIONAL_B_SPLINE_CURVE ( ( 0.9755282581475768211, 0.9755282581475768211, 1.000000000000000000, 0.9510565162951535312, 1.000000000000000000, 0.9510565162951535312, 1.000000000000000000, 0.9510565162951535312, 1.000000000000000000, 0.9510565162951535312, 1.000000000000000000, 0.9755282581475763770, 0.9755282581475768211 ) ) 
 REPRESENTATION_ITEM ( '' )  );
#21247=CARTESIAN_POINT ( 'NONE',  ( -154.5594255724347761, -194.1630981290892919, 40.14644641866476604 ) ) ;
#21251=CARTESIAN_POINT ( 'NONE',  ( -160.8964159109769696, -175.8938272943107393, 49.65701158161630957 ) ) ;
#21253=CARTESIAN_POINT ( 'NONE',  ( -161.4692556286852607, -178.7130981290893317, 46.40781461928724383 ) ) ;
#21277=CARTESIAN_POINT ( 'NONE',  ( -151.4692556286852891, -182.3130981290892976, 39.65701158161629536 ) ) ;
#21286=CARTESIAN_POINT ( 'NONE',  ( -160.8964159109769696, -175.8938272943107393, 49.65701158161630957 ) ) ;
#21287=CARTESIAN_POINT ( 'NONE',  ( -142.0420953463935803, -183.5084106276440252, 46.59394152635518083 ) ) ;
#21291=CARTESIAN_POINT ( 'NONE',  ( -159.0959885057557983, -166.8584106276440480, 55.19815736654470584 ) ) ;
#21305=CARTESIAN_POINT ( 'NONE',  ( -141.4692556286852891, -162.8391397928654101, 46.40781461928724383 ) ) ;
#21311=CARTESIAN_POINT ( 'NONE',  ( -145.6429501568359797, -158.9438272943107222, 41.63779006702063867 ) ) ;
#21313=CARTESIAN_POINT ( 'NONE',  ( -151.4692556286852891, -185.9084106276440025, 39.74470866294723947 ) ) ;
#21316=EDGE_CURVE ( 'NONE', #19655, #19660, #4132, .T. ) ;
#21319=ORIENTED_EDGE ( 'NONE', *, *, #20799, .F. ) ;
#21322=EDGE_CURVE ( 'NONE', #17969, #4022, #10689, .T. ) ;
#21325=CARTESIAN_POINT ( 'NONE',  ( -151.4692556286852891, -196.9891397928655010, 49.65701158161630957 ) ) ;
#21327=EDGE_CURVE ( 'NONE', #7201, #9959, #17556, .T. ) ;
#21328=LINE ( 'NONE', #13162, #14314 ) ;
#21330=CARTESIAN_POINT ( 'NONE',  ( -153.0531000319306827, -175.8160212151857422, 59.65701158161631668 ) ) ;
#21331=CARTESIAN_POINT ( 'NONE',  ( -151.4692556286852891, -187.7391397928654726, 60.17163382399899518 ) ) ;
#21333=CARTESIAN_POINT ( 'NONE',  ( -145.6429501568359797, -186.8438272943106995, 57.67623309621198047 ) ) ;
#21337=CARTESIAN_POINT ( 'NONE',  ( -160.8964159109769696, -184.7438272943107052, 52.72008163687743121 ) ) ;
#21348=VECTOR ( 'NONE', #1909, 1000.000000000000000 ) ;
#21354=CARTESIAN_POINT ( 'NONE',  ( -145.6429501568359797, -171.8438272943107279, 57.67623309621197336 ) ) ;
#21356=CARTESIAN_POINT ( 'NONE',  ( -141.4692556286852891, -182.9130981290893203, 46.40781461928724383 ) ) ;
#21363=CARTESIAN_POINT ( 'NONE',  ( -157.2955611005345986, -157.7084106276440423, 57.67623309621197336 ) ) ;
#21365=VECTOR ( 'NONE', #13047, 1000.000000000000000 ) ;
#21382=CARTESIAN_POINT ( 'NONE',  ( -154.3824083646099439, -163.5584106276440366, 58.62277379824867296 ) ) ;
#21386=( NAMED_UNIT ( * ) SI_UNIT ( $, .STERADIAN. ) SOLID_ANGLE_UNIT ( ) );
#21393=CARTESIAN_POINT ( 'NONE',  ( -148.5561028927606344, -170.7938272943107165, 40.69124936498395328 ) ) ;
#21394=CARTESIAN_POINT ( 'NONE',  ( -148.5561028927606344, -180.0584106276440366, 40.69124936498395328 ) ) ;
#21395=ORIENTED_EDGE ( 'NONE', *, *, #9100, .F. ) ;
#21397=CARTESIAN_POINT ( 'NONE',  ( -148.5561028927606344, -165.0584106276440366, 40.69124936498395328 ) ) ;
#21423=CARTESIAN_POINT ( 'NONE',  ( -151.4692556286852891, -191.9084106276440025, 39.74470866294723947 ) ) ;
#21425=CARTESIAN_POINT ( 'NONE',  ( -154.3824083646099439, -182.7584106276440536, 40.69124936498395328 ) ) ;
#21434=CARTESIAN_POINT ( 'NONE',  ( -158.9748091281504401, -116.9891397928655010, 62.65701158161630957 ) ) ;
#21439=CARTESIAN_POINT ( 'NONE',  ( -151.4692556286852891, -193.7391397928654442, 60.17163382399899518 ) ) ;
#21443=CARTESIAN_POINT ( 'NONE',  ( -143.8425227516148084, -195.0938272943107279, 44.11586579668791330 ) ) ;
#21444=AXIS2_PLACEMENT_3D ( 'NONE', #21058, #5938, #9367 ) ;
#21448=CARTESIAN_POINT ( 'NONE',  ( -159.0959885057557983, -181.5938272943107279, 55.19815736654470584 ) ) ;
#21455=EDGE_CURVE ( 'NONE', #7641, #20771, #18642, .T. ) ;
#21465=CARTESIAN_POINT ( 'NONE',  ( -159.0959885057557983, -160.5938272943107279, 55.19815736654470584 ) ) ;
#21467=CARTESIAN_POINT ( 'NONE',  ( -145.2889157411863721, -174.5130981290892578, 58.16351966513671812 ) ) ;
#21474=LINE ( 'NONE', #20156, #3021 ) ;
#21485=CARTESIAN_POINT ( 'NONE',  ( -149.8854112254399240, -156.3160212151857422, 39.65701158161629536 ) ) ;
#21493=CARTESIAN_POINT ( 'NONE',  ( -154.3824083646099439, -170.7584106276440536, 40.69124936498395328 ) ) ;
#21494=CARTESIAN_POINT ( 'NONE',  ( -148.5561028927606344, -191.7938272943107449, 40.69124936498395328 ) ) ;
#21497=CARTESIAN_POINT ( 'NONE',  ( -145.2889157411863437, -188.6130981290893374, 41.15050349809589392 ) ) ;
#21499=CARTESIAN_POINT ( 'NONE',  ( -151.4692556286853176, -175.7391397928654726, 59.65701158161632378 ) ) ;
#21505=CARTESIAN_POINT ( 'NONE',  ( -145.6429501568359797, -158.9438272943107222, 41.63779006702063867 ) ) ;
#21506=CARTESIAN_POINT ( 'NONE',  ( -159.0959885057557983, -187.8584106276440480, 55.19815736654470584 ) ) ;
#21510=( BOUNDED_CURVE ( )  B_SPLINE_CURVE ( 2, ( #8054, #8974, #908, #17654, #4006, #10846, #16116, #7430, #11044, #584, #17760, #2662, #17543 ),
 .UNSPECIFIED., .F., .F. ) 
 B_SPLINE_CURVE_WITH_KNOTS ( ( 3, 2, 2, 2, 2, 2, 3 ),
 ( 0.8392857142857143016, 0.8428571428571428603, 0.8499999999999999778, 0.8571428571428570953, 0.8642857142857143238, 0.8714285714285714413, 0.8750000000000000000 ),
 .UNSPECIFIED. ) 
 CURVE ( )  GEOMETRIC_REPRESENTATION_ITEM ( )  RATIONAL_B_SPLINE_CURVE ( ( 0.9755282581475768211, 0.9755282581475768211, 1.000000000000000000, 0.9510565162951535312, 1.000000000000000000, 0.9510565162951535312, 1.000000000000000000, 0.9510565162951535312, 1.000000000000000000, 0.9510565162951535312, 1.000000000000000000, 0.9755282581475768211, 0.9755282581475768211 ) ) 
 REPRESENTATION_ITEM ( '' )  );
#21511=CARTESIAN_POINT ( 'NONE',  ( -148.5561028927606344, -168.0584106276440366, 40.69124936498395328 ) ) ;
#21527=LINE ( 'NONE', #8191, #6213 ) ;
#21534=CARTESIAN_POINT ( 'NONE',  ( -156.1828684652451500, -155.3945645429188005, 41.49287016839741682 ) ) ;
#21536=CARTESIAN_POINT ( 'NONE',  ( -143.8425227516148084, -180.9584106276440707, 55.19815736654470584 ) ) ;
#21551=CARTESIAN_POINT ( 'NONE',  ( -143.3790856849358306, -183.6891397928654612, 43.77915905869157598 ) ) ;
#21554=CARTESIAN_POINT ( 'NONE',  ( -151.4692556286852891, -187.1438272943106824, 59.56931450028537967 ) ) ;
#21560=CARTESIAN_POINT ( 'NONE',  ( -154.3824083646099439, -179.4938272943107336, 40.69124936498395328 ) ) ;
#21575=CARTESIAN_POINT ( 'NONE',  ( -145.6429501568359797, -156.2084106276440423, 41.63779006702063867 ) ) ;
#21576=CARTESIAN_POINT ( 'NONE',  ( -157.2955611005345986, -158.3438272943106995, 41.63779006702063867 ) ) ;
#21578=CARTESIAN_POINT ( 'NONE',  ( -154.5594255724347761, -180.9630981290893033, 59.16757674456785310 ) ) ;
#21582=EDGE_CURVE ( 'NONE', #18977, #19943, #2498, .T. ) ;
#21586=CARTESIAN_POINT ( 'NONE',  ( -159.5594255724347761, -167.7891397928654840, 43.77915905869157598 ) ) ;
#21592=CARTESIAN_POINT ( 'NONE',  ( -141.4692556286852891, -186.8391397928654669, 46.40781461928724383 ) ) ;
#21595=EDGE_CURVE ( 'NONE', #11010, #14442, #13765, .T. ) ;
#21596=CARTESIAN_POINT ( 'NONE',  ( -151.4692556286852891, -196.9891397928655010, 58.65701158161631668 ) ) ;
#21605=CARTESIAN_POINT ( 'NONE',  ( -151.4692556286852891, -167.9084106276440309, 39.74470866294723947 ) ) ;
#21606=CARTESIAN_POINT ( 'NONE',  ( -160.8964159109769696, -187.7438272943107336, 52.72008163687743121 ) ) ;
#21607=CARTESIAN_POINT ( 'NONE',  ( -157.6495955161842062, -178.1130981290893089, 58.16351966513671812 ) ) ;
#21610=CARTESIAN_POINT ( 'NONE',  ( -143.3790856849358306, -175.2891397928654840, 55.53486410454105027 ) ) ;
#21613=CARTESIAN_POINT ( 'NONE',  ( -157.6495955161842062, -185.0130981290893146, 41.15050349809589392 ) ) ;
#21616=CARTESIAN_POINT ( 'NONE',  ( -157.2955611005346270, -158.3438272943106995, 41.63779006702063867 ) ) ;
#21617=CARTESIAN_POINT ( 'NONE',  ( -157.2955611005345986, -182.6084106276440480, 41.63779006702063867 ) ) ;
#21620=CARTESIAN_POINT ( 'NONE',  ( -157.2955611005346270, -170.6084106276440480, 41.63779006702063867 ) ) ;
#21626=ORIENTED_EDGE ( 'NONE', *, *, #17590, .T. ) ;
#21628=CARTESIAN_POINT ( 'NONE',  ( -149.8854112254399240, -192.3160212151857422, 39.65701158161631668 ) ) ;
#21631=CARTESIAN_POINT ( 'NONE',  ( -151.4692556286852891, -195.9891397928654726, 49.65701158161630957 ) ) ;
#21638=CARTESIAN_POINT ( 'NONE',  ( -151.4692556286852607, -170.3130981290892692, 39.65701158161629536 ) ) ;
#21646=CARTESIAN_POINT ( 'NONE',  ( -143.8425227516148084, -156.0938272943107279, 44.11586579668791330 ) ) ;
#21648=CARTESIAN_POINT ( 'NONE',  ( -143.8425227516148084, -189.3584106276440480, 44.11586579668791330 ) ) ;
#21649=ORIENTED_EDGE ( 'NONE', *, *, #8984, .F. ) ;
#21666=CARTESIAN_POINT ( 'NONE',  ( -159.5594255724347761, -182.7891397928654840, 43.77915905869157598 ) ) ;
#21669=CARTESIAN_POINT ( 'NONE',  ( -143.8425227516148084, -189.6938272943107222, 55.19815736654470584 ) ) ;
#21673=CARTESIAN_POINT ( 'NONE',  ( -159.0959885057557983, -188.1938272943107222, 44.11586579668791330 ) ) ;
#21683=ORIENTED_EDGE ( 'NONE', *, *, #12699, .T. ) ;
#21689=CARTESIAN_POINT ( 'NONE',  ( -145.6429501568359797, -164.9438272943106938, 41.63779006702063867 ) ) ;
#21691=CARTESIAN_POINT ( 'NONE',  ( -141.4692556286852891, -180.2130981290893033, 52.90620854394536821 ) ) ;
#21692=CARTESIAN_POINT ( 'NONE',  ( -154.5594255724347761, -192.0891397928654953, 40.14644641866476604 ) ) ;
#21713=CARTESIAN_POINT ( 'NONE',  ( -160.8964159109769696, -164.1584106276440593, 49.65701158161630957 ) ) ;
#21714=CARTESIAN_POINT ( 'NONE',  ( -142.0420953463936087, -186.3938272943107393, 49.65701158161630957 ) ) ;
#21723=CARTESIAN_POINT ( 'NONE',  ( -143.8425227516148084, -165.6938272943107222, 55.19815736654470584 ) ) ;
#21724=CARTESIAN_POINT ( 'NONE',  ( -151.4692556286852891, -172.4084106276440309, 59.56931450028537256 ) ) ;
#21727=CARTESIAN_POINT ( 'NONE',  ( -151.4692556286852891, -158.9084106276440025, 39.74470866294723947 ) ) ;
#21748=DIRECTION ( 'NONE',  ( -0.000000000000000000, 1.000000000000000000, -0.000000000000000000 ) ) ;
#21751=CARTESIAN_POINT ( 'NONE',  ( -154.3824083646099439, -184.5584106276440650, 58.62277379824867296 ) ) ;
#21753=CARTESIAN_POINT ( 'NONE',  ( -148.5561028927606344, -190.2584106276440536, 58.62277379824867296 ) ) ;
#21756=EDGE_CURVE ( 'NONE', #4358, #18246, #9150, .T. ) ;
#21757=DIRECTION ( 'NONE',  ( -0.000000000000000000, 1.000000000000000000, -0.000000000000000000 ) ) ;
#21773=CARTESIAN_POINT ( 'NONE',  ( -154.5594255724347761, -180.0891397928654669, 40.14644641866476604 ) ) ;
#21781=CARTESIAN_POINT ( 'NONE',  ( -142.0420953463935803, -183.5438272943107449, 52.72008163687743831 ) ) ;
#21785=CARTESIAN_POINT ( 'NONE',  ( -151.4692556286852891, -190.7391397928654726, 59.65701158161632378 ) ) ;
#21797=CARTESIAN_POINT ( 'NONE',  ( -145.6429501568359797, -165.8438272943107279, 57.67623309621197336 ) ) ;
#21799=CARTESIAN_POINT ( 'NONE',  ( -148.3790856849358306, -167.4630981290893033, 40.14644641866477315 ) ) ;
#21818=CARTESIAN_POINT ( 'NONE',  ( -148.5561028927606344, -165.9938272943107336, 58.62277379824867296 ) ) ;
ENDSEC;
END-ISO-10303-21;
